ISO-10303-21;
HEADER;
/* Generated by software containing ST-Developer
 * from STEP Tools, Inc. (www.steptools.com) 
 */

FILE_DESCRIPTION(
/* description */ (''),
/* implementation_level */ '2;1');

FILE_NAME(
/* name */ '18_Manifold_Bolt_ISO_4017_M8x55.step',
/* time_stamp */ '2026-10-26T06:13:19-07:00',
/* author */ (''),
/* organization */ (''),
/* preprocessor_version */ 'ST-DEVELOPER v20.2',
/* originating_system */ 'Autodesk Translation Framework v15.15.0.0',
/* authorisation */ '');

FILE_SCHEMA (('AUTOMOTIVE_DESIGN { 1 0 10303 214 3 1 1 }','TECHNICAL_DATA_PACKAGING'));
ENDSEC;

DATA;
#10=MECHANICAL_DESIGN_GEOMETRIC_PRESENTATION_REPRESENTATION('',(#314),#56639);
#274=SHAPE_REPRESENTATION_RELATIONSHIP('SRR','None',#56762,#294);
#294=ADVANCED_BREP_SHAPE_REPRESENTATION('',(#334),#56636);
#314=STYLED_ITEM('',(#56922),#334);
#334=MANIFOLD_SOLID_BREP('Body1',#16966);
#357=B_SPLINE_SURFACE_WITH_KNOTS('',3,3,((#41620,#41621,#41622,#41623,#41624,
#41625,#41626,#41627,#41628,#41629,#41630,#41631,#41632,#41633,#41634,#41635,
#41636,#41637,#41638,#41639,#41640,#41641,#41642,#41643,#41644,#41645,#41646,
#41647,#41648,#41649,#41650,#41651,#41652,#41653,#41654,#41655,#41656,#41657,
#41658,#41659,#41660,#41661,#41662,#41663,#41664,#41665,#41666,#41667,#41668,
#41669,#41670,#41671,#41672,#41673,#41674,#41675,#41676,#41677,#41678,#41679,
#41680,#41681,#41682,#41683,#41684,#41685,#41686,#41687,#41688,#41689,#41690,
#41691,#41692,#41693,#41694,#41695,#41696,#41697,#41698,#41699,#41700,#41701,
#41702,#41703,#41704,#41705,#41706,#41707,#41708,#41709,#41710,#41711,#41712,
#41713,#41714,#41715,#41716,#41717,#41718,#41719,#41720,#41721,#41722,#41723,
#41724,#41725,#41726,#41727,#41728,#41729,#41730,#41731,#41732,#41733,#41734,
#41735,#41736,#41737,#41738,#41739,#41740,#41741,#41742,#41743,#41744,#41745,
#41746,#41747,#41748,#41749,#41750,#41751,#41752,#41753,#41754,#41755,#41756,
#41757,#41758,#41759,#41760,#41761,#41762,#41763,#41764,#41765,#41766,#41767,
#41768,#41769,#41770,#41771,#41772,#41773,#41774,#41775,#41776,#41777,#41778,
#41779,#41780,#41781,#41782,#41783,#41784,#41785,#41786,#41787,#41788,#41789,
#41790,#41791,#41792,#41793,#41794,#41795,#41796,#41797,#41798,#41799,#41800,
#41801,#41802,#41803,#41804,#41805,#41806,#41807,#41808,#41809,#41810,#41811,
#41812,#41813,#41814,#41815,#41816,#41817,#41818,#41819,#41820,#41821,#41822,
#41823,#41824,#41825,#41826,#41827,#41828,#41829,#41830,#41831,#41832,#41833,
#41834,#41835,#41836,#41837,#41838,#41839,#41840,#41841,#41842,#41843,#41844,
#41845,#41846,#41847,#41848,#41849,#41850,#41851,#41852,#41853,#41854,#41855,
#41856,#41857,#41858,#41859,#41860,#41861,#41862,#41863,#41864,#41865,#41866,
#41867,#41868,#41869,#41870,#41871,#41872,#41873,#41874,#41875,#41876,#41877,
#41878,#41879,#41880,#41881,#41882,#41883,#41884,#41885,#41886,#41887,#41888,
#41889,#41890,#41891,#41892,#41893,#41894,#41895,#41896,#41897,#41898,#41899),
(#41900,#41901,#41902,#41903,#41904,#41905,#41906,#41907,#41908,#41909,
#41910,#41911,#41912,#41913,#41914,#41915,#41916,#41917,#41918,#41919,#41920,
#41921,#41922,#41923,#41924,#41925,#41926,#41927,#41928,#41929,#41930,#41931,
#41932,#41933,#41934,#41935,#41936,#41937,#41938,#41939,#41940,#41941,#41942,
#41943,#41944,#41945,#41946,#41947,#41948,#41949,#41950,#41951,#41952,#41953,
#41954,#41955,#41956,#41957,#41958,#41959,#41960,#41961,#41962,#41963,#41964,
#41965,#41966,#41967,#41968,#41969,#41970,#41971,#41972,#41973,#41974,#41975,
#41976,#41977,#41978,#41979,#41980,#41981,#41982,#41983,#41984,#41985,#41986,
#41987,#41988,#41989,#41990,#41991,#41992,#41993,#41994,#41995,#41996,#41997,
#41998,#41999,#42000,#42001,#42002,#42003,#42004,#42005,#42006,#42007,#42008,
#42009,#42010,#42011,#42012,#42013,#42014,#42015,#42016,#42017,#42018,#42019,
#42020,#42021,#42022,#42023,#42024,#42025,#42026,#42027,#42028,#42029,#42030,
#42031,#42032,#42033,#42034,#42035,#42036,#42037,#42038,#42039,#42040,#42041,
#42042,#42043,#42044,#42045,#42046,#42047,#42048,#42049,#42050,#42051,#42052,
#42053,#42054,#42055,#42056,#42057,#42058,#42059,#42060,#42061,#42062,#42063,
#42064,#42065,#42066,#42067,#42068,#42069,#42070,#42071,#42072,#42073,#42074,
#42075,#42076,#42077,#42078,#42079,#42080,#42081,#42082,#42083,#42084,#42085,
#42086,#42087,#42088,#42089,#42090,#42091,#42092,#42093,#42094,#42095,#42096,
#42097,#42098,#42099,#42100,#42101,#42102,#42103,#42104,#42105,#42106,#42107,
#42108,#42109,#42110,#42111,#42112,#42113,#42114,#42115,#42116,#42117,#42118,
#42119,#42120,#42121,#42122,#42123,#42124,#42125,#42126,#42127,#42128,#42129,
#42130,#42131,#42132,#42133,#42134,#42135,#42136,#42137,#42138,#42139,#42140,
#42141,#42142,#42143,#42144,#42145,#42146,#42147,#42148,#42149,#42150,#42151,
#42152,#42153,#42154,#42155,#42156,#42157,#42158,#42159,#42160,#42161,#42162,
#42163,#42164,#42165,#42166,#42167,#42168,#42169,#42170,#42171,#42172,#42173,
#42174,#42175,#42176,#42177,#42178,#42179),(#42180,#42181,#42182,#42183,
#42184,#42185,#42186,#42187,#42188,#42189,#42190,#42191,#42192,#42193,#42194,
#42195,#42196,#42197,#42198,#42199,#42200,#42201,#42202,#42203,#42204,#42205,
#42206,#42207,#42208,#42209,#42210,#42211,#42212,#42213,#42214,#42215,#42216,
#42217,#42218,#42219,#42220,#42221,#42222,#42223,#42224,#42225,#42226,#42227,
#42228,#42229,#42230,#42231,#42232,#42233,#42234,#42235,#42236,#42237,#42238,
#42239,#42240,#42241,#42242,#42243,#42244,#42245,#42246,#42247,#42248,#42249,
#42250,#42251,#42252,#42253,#42254,#42255,#42256,#42257,#42258,#42259,#42260,
#42261,#42262,#42263,#42264,#42265,#42266,#42267,#42268,#42269,#42270,#42271,
#42272,#42273,#42274,#42275,#42276,#42277,#42278,#42279,#42280,#42281,#42282,
#42283,#42284,#42285,#42286,#42287,#42288,#42289,#42290,#42291,#42292,#42293,
#42294,#42295,#42296,#42297,#42298,#42299,#42300,#42301,#42302,#42303,#42304,
#42305,#42306,#42307,#42308,#42309,#42310,#42311,#42312,#42313,#42314,#42315,
#42316,#42317,#42318,#42319,#42320,#42321,#42322,#42323,#42324,#42325,#42326,
#42327,#42328,#42329,#42330,#42331,#42332,#42333,#42334,#42335,#42336,#42337,
#42338,#42339,#42340,#42341,#42342,#42343,#42344,#42345,#42346,#42347,#42348,
#42349,#42350,#42351,#42352,#42353,#42354,#42355,#42356,#42357,#42358,#42359,
#42360,#42361,#42362,#42363,#42364,#42365,#42366,#42367,#42368,#42369,#42370,
#42371,#42372,#42373,#42374,#42375,#42376,#42377,#42378,#42379,#42380,#42381,
#42382,#42383,#42384,#42385,#42386,#42387,#42388,#42389,#42390,#42391,#42392,
#42393,#42394,#42395,#42396,#42397,#42398,#42399,#42400,#42401,#42402,#42403,
#42404,#42405,#42406,#42407,#42408,#42409,#42410,#42411,#42412,#42413,#42414,
#42415,#42416,#42417,#42418,#42419,#42420,#42421,#42422,#42423,#42424,#42425,
#42426,#42427,#42428,#42429,#42430,#42431,#42432,#42433,#42434,#42435,#42436,
#42437,#42438,#42439,#42440,#42441,#42442,#42443,#42444,#42445,#42446,#42447,
#42448,#42449,#42450,#42451,#42452,#42453,#42454,#42455,#42456,#42457,#42458,
#42459),(#42460,#42461,#42462,#42463,#42464,#42465,#42466,#42467,#42468,
#42469,#42470,#42471,#42472,#42473,#42474,#42475,#42476,#42477,#42478,#42479,
#42480,#42481,#42482,#42483,#42484,#42485,#42486,#42487,#42488,#42489,#42490,
#42491,#42492,#42493,#42494,#42495,#42496,#42497,#42498,#42499,#42500,#42501,
#42502,#42503,#42504,#42505,#42506,#42507,#42508,#42509,#42510,#42511,#42512,
#42513,#42514,#42515,#42516,#42517,#42518,#42519,#42520,#42521,#42522,#42523,
#42524,#42525,#42526,#42527,#42528,#42529,#42530,#42531,#42532,#42533,#42534,
#42535,#42536,#42537,#42538,#42539,#42540,#42541,#42542,#42543,#42544,#42545,
#42546,#42547,#42548,#42549,#42550,#42551,#42552,#42553,#42554,#42555,#42556,
#42557,#42558,#42559,#42560,#42561,#42562,#42563,#42564,#42565,#42566,#42567,
#42568,#42569,#42570,#42571,#42572,#42573,#42574,#42575,#42576,#42577,#42578,
#42579,#42580,#42581,#42582,#42583,#42584,#42585,#42586,#42587,#42588,#42589,
#42590,#42591,#42592,#42593,#42594,#42595,#42596,#42597,#42598,#42599,#42600,
#42601,#42602,#42603,#42604,#42605,#42606,#42607,#42608,#42609,#42610,#42611,
#42612,#42613,#42614,#42615,#42616,#42617,#42618,#42619,#42620,#42621,#42622,
#42623,#42624,#42625,#42626,#42627,#42628,#42629,#42630,#42631,#42632,#42633,
#42634,#42635,#42636,#42637,#42638,#42639,#42640,#42641,#42642,#42643,#42644,
#42645,#42646,#42647,#42648,#42649,#42650,#42651,#42652,#42653,#42654,#42655,
#42656,#42657,#42658,#42659,#42660,#42661,#42662,#42663,#42664,#42665,#42666,
#42667,#42668,#42669,#42670,#42671,#42672,#42673,#42674,#42675,#42676,#42677,
#42678,#42679,#42680,#42681,#42682,#42683,#42684,#42685,#42686,#42687,#42688,
#42689,#42690,#42691,#42692,#42693,#42694,#42695,#42696,#42697,#42698,#42699,
#42700,#42701,#42702,#42703,#42704,#42705,#42706,#42707,#42708,#42709,#42710,
#42711,#42712,#42713,#42714,#42715,#42716,#42717,#42718,#42719,#42720,#42721,
#42722,#42723,#42724,#42725,#42726,#42727,#42728,#42729,#42730,#42731,#42732,
#42733,#42734,#42735,#42736,#42737,#42738,#42739)),.UNSPECIFIED.,.F.,.F.,
 .F.,(4,4),(4,1,1,1,1,1,1,1,1,1,1,1,1,1,1,1,1,1,1,1,1,1,1,1,1,1,1,1,1,1,
1,1,1,1,1,1,1,1,1,1,1,1,1,1,1,1,1,1,1,1,1,1,1,1,1,1,1,1,1,1,1,1,1,1,1,1,
1,1,1,1,1,1,1,1,1,1,1,1,1,1,1,1,1,1,1,1,1,1,1,1,1,1,1,1,1,1,1,1,1,1,1,1,
1,1,1,1,1,1,1,1,1,1,1,1,1,1,1,1,1,1,1,1,1,1,1,1,1,1,1,1,1,1,1,1,1,1,1,1,
1,1,1,1,1,1,1,1,1,1,1,1,1,1,1,1,1,1,1,1,1,1,1,1,1,1,1,1,1,1,1,1,1,1,1,1,
1,1,1,1,1,1,1,1,1,1,1,1,1,1,1,1,1,1,1,1,1,1,1,1,1,1,1,1,1,1,1,1,1,1,1,1,
1,1,1,1,1,1,1,1,1,1,1,1,1,1,1,1,1,1,1,1,1,1,1,1,1,1,1,1,1,1,1,1,1,1,1,1,
1,1,1,1,1,1,1,1,1,1,1,1,1,1,1,1,1,1,1,1,1,1,1,1,1,1,1,1,1,1,1,4),(0.,0.0820126057383863),
(8.31473274985836,9.31236762250461,10.3100024951509,11.3076373677971,12.3052722404433,
13.3029071130896,14.3005419857358,15.2981768583821,16.2958117310283,17.2934466036746,
18.2910814763208,19.2887163489671,20.2863512216133,21.2839860942596,22.2816209669058,
23.2792558395521,24.2768907121983,25.2745255848446,26.2721604574908,27.2697953301371,
28.2674302027833,29.2650650754296,30.2626999480758,31.2603348207221,32.2579696933683,
33.2556045660146,34.2532394386608,35.2508743113071,36.2485091839533,37.2461440565995,
38.2437789292458,39.241413801892,40.2390486745383,41.2366835471845,42.2343184198308,
43.231953292477,44.2295881651233,45.2272230377695,46.2248579104158,47.222492783062,
48.2201276557083,49.2177625283545,50.2153974010008,51.213032273647,52.2106671462933,
53.2083020189395,54.2059368915858,55.203571764232,56.2012066368783,57.1988415095245,
58.1964763821708,59.194111254817,60.1917461274632,61.1893810001095,62.1870158727557,
63.184650745402,64.1822856180482,65.1799204906945,66.1775553633407,67.175190235987,
68.1728251086332,69.1704599812795,70.1680948539257,71.165729726572,72.1633645992182,
73.1609994718645,74.1586343445107,75.156269217157,76.1539040898032,77.1515389624495,
78.1491738350957,79.146808707742,80.1444435803882,81.1420784530345,82.1397133256807,
83.1373481983269,84.1349830709732,85.1326179436194,86.1302528162657,87.1278876889119,
88.1255225615582,89.1231574342044,90.1207923068507,91.1184271794969,92.1160620521432,
93.1136969247894,94.1113317974357,95.1089666700819,96.1066015427282,97.1042364153744,
98.1018712880207,99.0995061606669,100.097141033313,101.094775905959,102.092410778606,
103.090045651252,104.087680523898,105.085315396544,106.082950269191,107.080585141837,
108.078220014483,109.075854887129,110.073489759776,111.071124632422,112.068759505068,
113.066394377714,114.064029250361,115.061664123007,116.059298995653,117.056933868299,
118.054568740946,119.052203613592,120.049838486238,121.047473358884,122.045108231531,
123.042743104177,124.040377976823,125.038012849469,126.035647722116,127.033282594762,
128.030917467408,129.028552340054,130.026187212701,131.023822085347,132.021456957993,
133.019091830639,134.016726703286,135.014361575932,136.011996448578,137.009631321224,
138.007266193871,139.004901066517,140.002535939163,141.000170811809,141.997805684456,
142.995440557102,143.993075429748,144.990710302394,145.988345175041,146.985980047687,
147.983614920333,148.981249792979,149.978884665626,150.976519538272,151.974154410918,
152.971789283564,153.969424156211,154.967059028857,155.964693901503,156.962328774149,
157.959963646796,158.957598519442,159.955233392088,160.952868264734,161.950503137381,
162.948138010027,163.945772882673,164.943407755319,165.941042627966,166.938677500612,
167.936312373258,168.933947245904,169.931582118551,170.929216991197,171.926851863843,
172.924486736489,173.922121609136,174.919756481782,175.917391354428,176.915026227074,
177.912661099721,178.910295972367,179.907930845013,180.905565717659,181.903200590305,
182.900835462952,183.898470335598,184.896105208244,185.89374008089,186.891374953537,
187.889009826183,188.886644698829,189.884279571475,190.881914444122,191.879549316768,
192.877184189414,193.87481906206,194.872453934707,195.870088807353,196.867723679999,
197.865358552645,198.862993425292,199.860628297938,200.858263170584,201.85589804323,
202.853532915877,203.851167788523,204.848802661169,205.846437533815,206.844072406462,
207.841707279108,208.839342151754,209.8369770244,210.834611897047,211.832246769693,
212.829881642339,213.827516514985,214.825151387632,215.822786260278,216.820421132924,
217.81805600557,218.815690878217,219.813325750863,220.810960623509,221.808595496155,
222.806230368802,223.803865241448,224.801500114094,225.79913498674,226.796769859387,
227.794404732033,228.792039604679,229.789674477325,230.787309349972,231.784944222618,
232.782579095264,233.78021396791,234.777848840557,235.775483713203,236.773118585849,
237.770753458495,238.768388331142,239.766023203788,240.763658076434,241.76129294908,
242.758927821727,243.756562694373,244.754197567019,245.751832439665,246.749467312312,
247.747102184958,248.744737057604,249.74237193025,250.740006802897,251.737641675543,
252.735276548189,253.732911420835,254.730546293482,255.728181166128,256.725816038774,
257.72345091142,258.721085784067,259.718720656713,260.716355529359,261.713990402005,
262.711625274652,263.709260147298,264.706895019944,265.70452989259,266.702164765237,
267.699799637883,268.697434510529,269.695069383175,270.692704255822,271.690339128468,
272.687974001114,273.68560887376,274.683243746407,275.680878619053,276.678513491699,
277.676148364345,278.673783236992,279.671418109638,280.669052982284,281.66668785493,
282.664322727577,283.661957600223,284.659592472869),.UNSPECIFIED.);
#358=B_SPLINE_SURFACE_WITH_KNOTS('',3,3,((#43073,#43074,#43075,#43076,#43077,
#43078,#43079,#43080,#43081,#43082,#43083,#43084,#43085,#43086,#43087,#43088,
#43089,#43090,#43091,#43092,#43093,#43094,#43095,#43096,#43097,#43098,#43099,
#43100,#43101,#43102,#43103,#43104,#43105,#43106,#43107,#43108,#43109,#43110,
#43111,#43112,#43113,#43114,#43115,#43116,#43117,#43118,#43119,#43120,#43121,
#43122,#43123,#43124,#43125,#43126,#43127,#43128,#43129,#43130,#43131,#43132,
#43133,#43134,#43135,#43136,#43137,#43138,#43139,#43140,#43141,#43142,#43143,
#43144,#43145,#43146,#43147,#43148,#43149,#43150,#43151,#43152,#43153,#43154,
#43155,#43156,#43157,#43158,#43159,#43160,#43161,#43162,#43163,#43164,#43165,
#43166,#43167,#43168,#43169,#43170,#43171,#43172,#43173,#43174,#43175,#43176,
#43177,#43178,#43179,#43180,#43181,#43182,#43183,#43184,#43185,#43186,#43187,
#43188,#43189,#43190,#43191,#43192,#43193,#43194,#43195,#43196,#43197,#43198,
#43199,#43200,#43201,#43202,#43203,#43204,#43205,#43206,#43207,#43208,#43209,
#43210,#43211,#43212,#43213,#43214,#43215,#43216,#43217,#43218,#43219,#43220,
#43221,#43222,#43223,#43224,#43225,#43226,#43227,#43228,#43229,#43230,#43231,
#43232,#43233,#43234,#43235,#43236,#43237,#43238,#43239,#43240,#43241,#43242,
#43243,#43244,#43245,#43246,#43247,#43248,#43249,#43250,#43251,#43252,#43253,
#43254,#43255,#43256,#43257,#43258,#43259,#43260,#43261,#43262,#43263,#43264,
#43265,#43266,#43267,#43268,#43269,#43270,#43271,#43272,#43273,#43274,#43275,
#43276,#43277,#43278,#43279,#43280,#43281,#43282,#43283,#43284,#43285,#43286,
#43287,#43288,#43289,#43290,#43291,#43292,#43293,#43294,#43295,#43296,#43297,
#43298,#43299,#43300,#43301,#43302,#43303,#43304,#43305,#43306,#43307,#43308,
#43309,#43310,#43311,#43312,#43313,#43314,#43315,#43316,#43317,#43318,#43319,
#43320,#43321,#43322,#43323,#43324,#43325,#43326,#43327,#43328,#43329,#43330,
#43331,#43332,#43333,#43334,#43335,#43336,#43337,#43338,#43339,#43340,#43341,
#43342,#43343,#43344,#43345,#43346,#43347,#43348,#43349,#43350,#43351,#43352),
(#43353,#43354,#43355,#43356,#43357,#43358,#43359,#43360,#43361,#43362,
#43363,#43364,#43365,#43366,#43367,#43368,#43369,#43370,#43371,#43372,#43373,
#43374,#43375,#43376,#43377,#43378,#43379,#43380,#43381,#43382,#43383,#43384,
#43385,#43386,#43387,#43388,#43389,#43390,#43391,#43392,#43393,#43394,#43395,
#43396,#43397,#43398,#43399,#43400,#43401,#43402,#43403,#43404,#43405,#43406,
#43407,#43408,#43409,#43410,#43411,#43412,#43413,#43414,#43415,#43416,#43417,
#43418,#43419,#43420,#43421,#43422,#43423,#43424,#43425,#43426,#43427,#43428,
#43429,#43430,#43431,#43432,#43433,#43434,#43435,#43436,#43437,#43438,#43439,
#43440,#43441,#43442,#43443,#43444,#43445,#43446,#43447,#43448,#43449,#43450,
#43451,#43452,#43453,#43454,#43455,#43456,#43457,#43458,#43459,#43460,#43461,
#43462,#43463,#43464,#43465,#43466,#43467,#43468,#43469,#43470,#43471,#43472,
#43473,#43474,#43475,#43476,#43477,#43478,#43479,#43480,#43481,#43482,#43483,
#43484,#43485,#43486,#43487,#43488,#43489,#43490,#43491,#43492,#43493,#43494,
#43495,#43496,#43497,#43498,#43499,#43500,#43501,#43502,#43503,#43504,#43505,
#43506,#43507,#43508,#43509,#43510,#43511,#43512,#43513,#43514,#43515,#43516,
#43517,#43518,#43519,#43520,#43521,#43522,#43523,#43524,#43525,#43526,#43527,
#43528,#43529,#43530,#43531,#43532,#43533,#43534,#43535,#43536,#43537,#43538,
#43539,#43540,#43541,#43542,#43543,#43544,#43545,#43546,#43547,#43548,#43549,
#43550,#43551,#43552,#43553,#43554,#43555,#43556,#43557,#43558,#43559,#43560,
#43561,#43562,#43563,#43564,#43565,#43566,#43567,#43568,#43569,#43570,#43571,
#43572,#43573,#43574,#43575,#43576,#43577,#43578,#43579,#43580,#43581,#43582,
#43583,#43584,#43585,#43586,#43587,#43588,#43589,#43590,#43591,#43592,#43593,
#43594,#43595,#43596,#43597,#43598,#43599,#43600,#43601,#43602,#43603,#43604,
#43605,#43606,#43607,#43608,#43609,#43610,#43611,#43612,#43613,#43614,#43615,
#43616,#43617,#43618,#43619,#43620,#43621,#43622,#43623,#43624,#43625,#43626,
#43627,#43628,#43629,#43630,#43631,#43632),(#43633,#43634,#43635,#43636,
#43637,#43638,#43639,#43640,#43641,#43642,#43643,#43644,#43645,#43646,#43647,
#43648,#43649,#43650,#43651,#43652,#43653,#43654,#43655,#43656,#43657,#43658,
#43659,#43660,#43661,#43662,#43663,#43664,#43665,#43666,#43667,#43668,#43669,
#43670,#43671,#43672,#43673,#43674,#43675,#43676,#43677,#43678,#43679,#43680,
#43681,#43682,#43683,#43684,#43685,#43686,#43687,#43688,#43689,#43690,#43691,
#43692,#43693,#43694,#43695,#43696,#43697,#43698,#43699,#43700,#43701,#43702,
#43703,#43704,#43705,#43706,#43707,#43708,#43709,#43710,#43711,#43712,#43713,
#43714,#43715,#43716,#43717,#43718,#43719,#43720,#43721,#43722,#43723,#43724,
#43725,#43726,#43727,#43728,#43729,#43730,#43731,#43732,#43733,#43734,#43735,
#43736,#43737,#43738,#43739,#43740,#43741,#43742,#43743,#43744,#43745,#43746,
#43747,#43748,#43749,#43750,#43751,#43752,#43753,#43754,#43755,#43756,#43757,
#43758,#43759,#43760,#43761,#43762,#43763,#43764,#43765,#43766,#43767,#43768,
#43769,#43770,#43771,#43772,#43773,#43774,#43775,#43776,#43777,#43778,#43779,
#43780,#43781,#43782,#43783,#43784,#43785,#43786,#43787,#43788,#43789,#43790,
#43791,#43792,#43793,#43794,#43795,#43796,#43797,#43798,#43799,#43800,#43801,
#43802,#43803,#43804,#43805,#43806,#43807,#43808,#43809,#43810,#43811,#43812,
#43813,#43814,#43815,#43816,#43817,#43818,#43819,#43820,#43821,#43822,#43823,
#43824,#43825,#43826,#43827,#43828,#43829,#43830,#43831,#43832,#43833,#43834,
#43835,#43836,#43837,#43838,#43839,#43840,#43841,#43842,#43843,#43844,#43845,
#43846,#43847,#43848,#43849,#43850,#43851,#43852,#43853,#43854,#43855,#43856,
#43857,#43858,#43859,#43860,#43861,#43862,#43863,#43864,#43865,#43866,#43867,
#43868,#43869,#43870,#43871,#43872,#43873,#43874,#43875,#43876,#43877,#43878,
#43879,#43880,#43881,#43882,#43883,#43884,#43885,#43886,#43887,#43888,#43889,
#43890,#43891,#43892,#43893,#43894,#43895,#43896,#43897,#43898,#43899,#43900,
#43901,#43902,#43903,#43904,#43905,#43906,#43907,#43908,#43909,#43910,#43911,
#43912),(#43913,#43914,#43915,#43916,#43917,#43918,#43919,#43920,#43921,
#43922,#43923,#43924,#43925,#43926,#43927,#43928,#43929,#43930,#43931,#43932,
#43933,#43934,#43935,#43936,#43937,#43938,#43939,#43940,#43941,#43942,#43943,
#43944,#43945,#43946,#43947,#43948,#43949,#43950,#43951,#43952,#43953,#43954,
#43955,#43956,#43957,#43958,#43959,#43960,#43961,#43962,#43963,#43964,#43965,
#43966,#43967,#43968,#43969,#43970,#43971,#43972,#43973,#43974,#43975,#43976,
#43977,#43978,#43979,#43980,#43981,#43982,#43983,#43984,#43985,#43986,#43987,
#43988,#43989,#43990,#43991,#43992,#43993,#43994,#43995,#43996,#43997,#43998,
#43999,#44000,#44001,#44002,#44003,#44004,#44005,#44006,#44007,#44008,#44009,
#44010,#44011,#44012,#44013,#44014,#44015,#44016,#44017,#44018,#44019,#44020,
#44021,#44022,#44023,#44024,#44025,#44026,#44027,#44028,#44029,#44030,#44031,
#44032,#44033,#44034,#44035,#44036,#44037,#44038,#44039,#44040,#44041,#44042,
#44043,#44044,#44045,#44046,#44047,#44048,#44049,#44050,#44051,#44052,#44053,
#44054,#44055,#44056,#44057,#44058,#44059,#44060,#44061,#44062,#44063,#44064,
#44065,#44066,#44067,#44068,#44069,#44070,#44071,#44072,#44073,#44074,#44075,
#44076,#44077,#44078,#44079,#44080,#44081,#44082,#44083,#44084,#44085,#44086,
#44087,#44088,#44089,#44090,#44091,#44092,#44093,#44094,#44095,#44096,#44097,
#44098,#44099,#44100,#44101,#44102,#44103,#44104,#44105,#44106,#44107,#44108,
#44109,#44110,#44111,#44112,#44113,#44114,#44115,#44116,#44117,#44118,#44119,
#44120,#44121,#44122,#44123,#44124,#44125,#44126,#44127,#44128,#44129,#44130,
#44131,#44132,#44133,#44134,#44135,#44136,#44137,#44138,#44139,#44140,#44141,
#44142,#44143,#44144,#44145,#44146,#44147,#44148,#44149,#44150,#44151,#44152,
#44153,#44154,#44155,#44156,#44157,#44158,#44159,#44160,#44161,#44162,#44163,
#44164,#44165,#44166,#44167,#44168,#44169,#44170,#44171,#44172,#44173,#44174,
#44175,#44176,#44177,#44178,#44179,#44180,#44181,#44182,#44183,#44184,#44185,
#44186,#44187,#44188,#44189,#44190,#44191,#44192)),.UNSPECIFIED.,.F.,.F.,
 .F.,(4,4),(4,1,1,1,1,1,1,1,1,1,1,1,1,1,1,1,1,1,1,1,1,1,1,1,1,1,1,1,1,1,
1,1,1,1,1,1,1,1,1,1,1,1,1,1,1,1,1,1,1,1,1,1,1,1,1,1,1,1,1,1,1,1,1,1,1,1,
1,1,1,1,1,1,1,1,1,1,1,1,1,1,1,1,1,1,1,1,1,1,1,1,1,1,1,1,1,1,1,1,1,1,1,1,
1,1,1,1,1,1,1,1,1,1,1,1,1,1,1,1,1,1,1,1,1,1,1,1,1,1,1,1,1,1,1,1,1,1,1,1,
1,1,1,1,1,1,1,1,1,1,1,1,1,1,1,1,1,1,1,1,1,1,1,1,1,1,1,1,1,1,1,1,1,1,1,1,
1,1,1,1,1,1,1,1,1,1,1,1,1,1,1,1,1,1,1,1,1,1,1,1,1,1,1,1,1,1,1,1,1,1,1,1,
1,1,1,1,1,1,1,1,1,1,1,1,1,1,1,1,1,1,1,1,1,1,1,1,1,1,1,1,1,1,1,1,1,1,1,1,
1,1,1,1,1,1,1,1,1,1,1,1,1,1,1,1,1,1,1,1,1,1,1,1,1,1,1,1,1,1,1,4),(0.,0.0820126057383863),
(11.6152142277551,12.6128491004014,13.6104839730476,14.6081188456939,15.6057537183401,
16.6033885909864,17.6010234636326,18.5986583362789,19.5962932089251,20.5939280815713,
21.5915629542176,22.5891978268638,23.5868326995101,24.5844675721563,25.5821024448026,
26.5797373174488,27.5773721900951,28.5750070627413,29.5726419353876,30.5702768080338,
31.5679116806801,32.5655465533263,33.5631814259726,34.5608162986188,35.5584511712651,
36.5560860439113,37.5537209165576,38.5513557892038,39.54899066185,40.5466255344963,
41.5442604071425,42.5418952797888,43.539530152435,44.5371650250813,45.5347998977275,
46.5324347703738,47.53006964302,48.5277045156663,49.5253393883125,50.5229742609588,
51.520609133605,52.5182440062513,53.5158788788975,54.5135137515438,55.51114862419,
56.5087834968363,57.5064183694825,58.5040532421287,59.501688114775,60.4993229874212,
61.4969578600675,62.4945927327137,63.49222760536,64.4898624780062,65.4874973506525,
66.4851322232987,67.482767095945,68.4804019685912,69.4780368412375,70.4756717138837,
71.47330658653,72.4709414591762,73.4685763318225,74.4662112044687,75.463846077115,
76.4614809497612,77.4591158224074,78.4567506950537,79.4543855676999,80.4520204403462,
81.4496553129924,82.4472901856387,83.4449250582849,84.4425599309312,85.4401948035774,
86.4378296762237,87.4354645488699,88.4330994215162,89.4307342941624,90.4283691668087,
91.4260040394549,92.4236389121012,93.4212737847474,94.4189086573937,95.4165435300399,
96.4141784026861,97.4118132753324,98.4094481479786,99.4070830206249,100.404717893271,
101.402352765917,102.399987638564,103.39762251121,104.395257383856,105.392892256502,
106.390527129149,107.388162001795,108.385796874441,109.383431747087,110.381066619734,
111.37870149238,112.376336365026,113.373971237672,114.371606110319,115.369240982965,
116.366875855611,117.364510728257,118.362145600904,119.35978047355,120.357415346196,
121.355050218842,122.352685091489,123.350319964135,124.347954836781,125.345589709427,
126.343224582074,127.34085945472,128.338494327366,129.336129200012,130.333764072659,
131.331398945305,132.329033817951,133.326668690597,134.324303563244,135.32193843589,
136.319573308536,137.317208181182,138.314843053829,139.312477926475,140.310112799121,
141.307747671767,142.305382544414,143.30301741706,144.300652289706,145.298287162352,
146.295922034999,147.293556907645,148.291191780291,149.288826652937,150.286461525584,
151.28409639823,152.281731270876,153.279366143522,154.277001016168,155.274635888815,
156.272270761461,157.269905634107,158.267540506754,159.2651753794,160.262810252046,
161.260445124692,162.258079997338,163.255714869985,164.253349742631,165.250984615277,
166.248619487923,167.24625436057,168.243889233216,169.241524105862,170.239158978508,
171.236793851155,172.234428723801,173.232063596447,174.229698469093,175.22733334174,
176.224968214386,177.222603087032,178.220237959678,179.217872832325,180.215507704971,
181.213142577617,182.210777450263,183.20841232291,184.206047195556,185.203682068202,
186.201316940848,187.198951813495,188.196586686141,189.194221558787,190.191856431433,
191.18949130408,192.187126176726,193.184761049372,194.182395922018,195.180030794665,
196.177665667311,197.175300539957,198.172935412603,199.17057028525,200.168205157896,
201.165840030542,202.163474903188,203.161109775835,204.158744648481,205.156379521127,
206.154014393773,207.15164926642,208.149284139066,209.146919011712,210.144553884358,
211.142188757005,212.139823629651,213.137458502297,214.135093374943,215.13272824759,
216.130363120236,217.127997992882,218.125632865528,219.123267738175,220.120902610821,
221.118537483467,222.116172356113,223.11380722876,224.111442101406,225.109076974052,
226.106711846698,227.104346719345,228.101981591991,229.099616464637,230.097251337283,
231.09488620993,232.092521082576,233.090155955222,234.087790827868,235.085425700515,
236.083060573161,237.080695445807,238.078330318453,239.0759651911,240.073600063746,
241.071234936392,242.068869809038,243.066504681685,244.064139554331,245.061774426977,
246.059409299623,247.05704417227,248.054679044916,249.052313917562,250.049948790208,
251.047583662854,252.045218535501,253.042853408147,254.040488280793,255.038123153439,
256.035758026086,257.033392898732,258.031027771378,259.028662644024,260.026297516671,
261.023932389317,262.021567261963,263.019202134609,264.016837007256,265.014471879902,
266.012106752548,267.009741625194,268.007376497841,269.005011370487,270.002646243133,
271.000281115779,271.997915988426,272.995550861072,273.993185733718,274.990820606364,
275.988455479011,276.986090351657,277.983725224303,278.981360096949,279.978994969596,
280.976629842242,281.974264714888,282.971899587534,283.969534460181,284.967169332827,
285.964804205473,286.962439078119,287.960073950766),.UNSPECIFIED.);
#560=FACE_BOUND('',#3661,.T.);
#648=CONICAL_SURFACE('',#18472,7.25527674973257,1.046630884618);
#649=CONICAL_SURFACE('',#18485,3.75,0.785398163397451);
#1196=CIRCLE('',#18377,3.933);
#1197=CIRCLE('',#18422,3.22275);
#1198=CIRCLE('',#18424,3.22275);
#1199=CIRCLE('',#18468,3.933);
#1200=CIRCLE('',#18469,3.933);
#1201=CIRCLE('',#18470,3.22275);
#1202=CIRCLE('',#18473,6.17797863635533);
#1203=CIRCLE('',#18478,3.933);
#1204=CIRCLE('',#18484,3.5);
#1492=CYLINDRICAL_SURFACE('',#18376,3.933);
#1493=CYLINDRICAL_SURFACE('',#18378,3.933);
#1494=CYLINDRICAL_SURFACE('',#18379,3.933);
#1495=CYLINDRICAL_SURFACE('',#18380,3.933);
#1496=CYLINDRICAL_SURFACE('',#18381,3.933);
#1497=CYLINDRICAL_SURFACE('',#18382,3.933);
#1498=CYLINDRICAL_SURFACE('',#18383,3.933);
#1499=CYLINDRICAL_SURFACE('',#18384,3.933);
#1500=CYLINDRICAL_SURFACE('',#18385,3.933);
#1501=CYLINDRICAL_SURFACE('',#18386,3.933);
#1502=CYLINDRICAL_SURFACE('',#18387,3.933);
#1503=CYLINDRICAL_SURFACE('',#18388,3.933);
#1504=CYLINDRICAL_SURFACE('',#18389,3.933);
#1505=CYLINDRICAL_SURFACE('',#18390,3.933);
#1506=CYLINDRICAL_SURFACE('',#18391,3.933);
#1507=CYLINDRICAL_SURFACE('',#18392,3.933);
#1508=CYLINDRICAL_SURFACE('',#18393,3.933);
#1509=CYLINDRICAL_SURFACE('',#18394,3.933);
#1510=CYLINDRICAL_SURFACE('',#18395,3.933);
#1511=CYLINDRICAL_SURFACE('',#18396,3.933);
#1512=CYLINDRICAL_SURFACE('',#18397,3.933);
#1513=CYLINDRICAL_SURFACE('',#18398,3.933);
#1514=CYLINDRICAL_SURFACE('',#18399,3.933);
#1515=CYLINDRICAL_SURFACE('',#18400,3.933);
#1516=CYLINDRICAL_SURFACE('',#18401,3.933);
#1517=CYLINDRICAL_SURFACE('',#18402,3.933);
#1518=CYLINDRICAL_SURFACE('',#18403,3.933);
#1519=CYLINDRICAL_SURFACE('',#18404,3.933);
#1520=CYLINDRICAL_SURFACE('',#18405,3.933);
#1521=CYLINDRICAL_SURFACE('',#18406,3.933);
#1522=CYLINDRICAL_SURFACE('',#18407,3.933);
#1523=CYLINDRICAL_SURFACE('',#18408,3.933);
#1524=CYLINDRICAL_SURFACE('',#18409,3.933);
#1525=CYLINDRICAL_SURFACE('',#18410,3.933);
#1526=CYLINDRICAL_SURFACE('',#18411,3.933);
#1527=CYLINDRICAL_SURFACE('',#18412,3.933);
#1528=CYLINDRICAL_SURFACE('',#18413,3.933);
#1529=CYLINDRICAL_SURFACE('',#18414,3.933);
#1530=CYLINDRICAL_SURFACE('',#18415,3.933);
#1531=CYLINDRICAL_SURFACE('',#18416,3.933);
#1532=CYLINDRICAL_SURFACE('',#18417,3.933);
#1533=CYLINDRICAL_SURFACE('',#18418,3.933);
#1534=CYLINDRICAL_SURFACE('',#18419,3.933);
#1535=CYLINDRICAL_SURFACE('',#18420,3.933);
#1536=CYLINDRICAL_SURFACE('',#18421,3.22275);
#1537=CYLINDRICAL_SURFACE('',#18423,3.22275);
#1538=CYLINDRICAL_SURFACE('',#18425,3.22275);
#1539=CYLINDRICAL_SURFACE('',#18426,3.22275);
#1540=CYLINDRICAL_SURFACE('',#18427,3.22275);
#1541=CYLINDRICAL_SURFACE('',#18428,3.22275);
#1542=CYLINDRICAL_SURFACE('',#18429,3.22275);
#1543=CYLINDRICAL_SURFACE('',#18430,3.22275);
#1544=CYLINDRICAL_SURFACE('',#18431,3.22275);
#1545=CYLINDRICAL_SURFACE('',#18432,3.22275);
#1546=CYLINDRICAL_SURFACE('',#18433,3.22275);
#1547=CYLINDRICAL_SURFACE('',#18434,3.22275);
#1548=CYLINDRICAL_SURFACE('',#18435,3.22275);
#1549=CYLINDRICAL_SURFACE('',#18436,3.22275);
#1550=CYLINDRICAL_SURFACE('',#18437,3.22275);
#1551=CYLINDRICAL_SURFACE('',#18438,3.22275);
#1552=CYLINDRICAL_SURFACE('',#18439,3.22275);
#1553=CYLINDRICAL_SURFACE('',#18440,3.22275);
#1554=CYLINDRICAL_SURFACE('',#18441,3.22275);
#1555=CYLINDRICAL_SURFACE('',#18442,3.22275);
#1556=CYLINDRICAL_SURFACE('',#18443,3.22275);
#1557=CYLINDRICAL_SURFACE('',#18444,3.22275);
#1558=CYLINDRICAL_SURFACE('',#18445,3.22275);
#1559=CYLINDRICAL_SURFACE('',#18446,3.22275);
#1560=CYLINDRICAL_SURFACE('',#18447,3.22275);
#1561=CYLINDRICAL_SURFACE('',#18448,3.22275);
#1562=CYLINDRICAL_SURFACE('',#18449,3.22275);
#1563=CYLINDRICAL_SURFACE('',#18450,3.22275);
#1564=CYLINDRICAL_SURFACE('',#18451,3.22275);
#1565=CYLINDRICAL_SURFACE('',#18452,3.22275);
#1566=CYLINDRICAL_SURFACE('',#18453,3.22275);
#1567=CYLINDRICAL_SURFACE('',#18454,3.22275);
#1568=CYLINDRICAL_SURFACE('',#18455,3.22275);
#1569=CYLINDRICAL_SURFACE('',#18456,3.22275);
#1570=CYLINDRICAL_SURFACE('',#18457,3.22275);
#1571=CYLINDRICAL_SURFACE('',#18458,3.22275);
#1572=CYLINDRICAL_SURFACE('',#18459,3.22275);
#1573=CYLINDRICAL_SURFACE('',#18460,3.22275);
#1574=CYLINDRICAL_SURFACE('',#18461,3.22275);
#1575=CYLINDRICAL_SURFACE('',#18462,3.22275);
#1576=CYLINDRICAL_SURFACE('',#18463,3.22275);
#1577=CYLINDRICAL_SURFACE('',#18464,3.22275);
#1578=CYLINDRICAL_SURFACE('',#18465,3.22275);
#1579=CYLINDRICAL_SURFACE('',#18466,3.22275);
#1580=CYLINDRICAL_SURFACE('',#18471,3.22275);
#1581=CYLINDRICAL_SURFACE('',#18486,3.933);
#1778=(
BOUNDED_CURVE()
B_SPLINE_CURVE(2,(#44307,#44308,#44309),.UNSPECIFIED.,.F.,.F.)
B_SPLINE_CURVE_WITH_KNOTS((3,3),(0.149747849205877,0.971656649213287),
 .UNSPECIFIED.)
CURVE()
GEOMETRIC_REPRESENTATION_ITEM()
RATIONAL_B_SPLINE_CURVE((1.07140024848293,1.23714644374248,1.07140024848293))
REPRESENTATION_ITEM('')
);
#1779=(
BOUNDED_CURVE()
B_SPLINE_CURVE(2,(#44311,#44312,#44313),.UNSPECIFIED.,.F.,.F.)
B_SPLINE_CURVE_WITH_KNOTS((3,3),(0.149747849205876,0.971656649213287),
 .UNSPECIFIED.)
CURVE()
GEOMETRIC_REPRESENTATION_ITEM()
RATIONAL_B_SPLINE_CURVE((1.07140024848293,1.23714644374248,1.07140024848293))
REPRESENTATION_ITEM('')
);
#1780=(
BOUNDED_CURVE()
B_SPLINE_CURVE(2,(#44315,#44316,#44317),.UNSPECIFIED.,.F.,.F.)
B_SPLINE_CURVE_WITH_KNOTS((3,3),(0.149747849205877,0.971656649213287),
 .UNSPECIFIED.)
CURVE()
GEOMETRIC_REPRESENTATION_ITEM()
RATIONAL_B_SPLINE_CURVE((1.07140024848293,1.23714644374248,1.07140024848293))
REPRESENTATION_ITEM('')
);
#1781=(
BOUNDED_CURVE()
B_SPLINE_CURVE(2,(#44319,#44320,#44321),.UNSPECIFIED.,.F.,.F.)
B_SPLINE_CURVE_WITH_KNOTS((3,3),(0.149747849205876,0.971656649213287),
 .UNSPECIFIED.)
CURVE()
GEOMETRIC_REPRESENTATION_ITEM()
RATIONAL_B_SPLINE_CURVE((1.07140024848293,1.23714644374248,1.07140024848293))
REPRESENTATION_ITEM('')
);
#1782=(
BOUNDED_CURVE()
B_SPLINE_CURVE(2,(#44323,#44324,#44325),.UNSPECIFIED.,.F.,.F.)
B_SPLINE_CURVE_WITH_KNOTS((3,3),(0.560702249209475,0.971656649213286),
 .UNSPECIFIED.)
CURVE()
GEOMETRIC_REPRESENTATION_ITEM()
RATIONAL_B_SPLINE_CURVE((1.1542733461127,1.15427334611272,1.07140024848293))
REPRESENTATION_ITEM('')
);
#1783=(
BOUNDED_CURVE()
B_SPLINE_CURVE(2,(#44330,#44331,#44332),.UNSPECIFIED.,.F.,.F.)
B_SPLINE_CURVE_WITH_KNOTS((3,3),(0.149747849205877,0.560702249209475),
 .UNSPECIFIED.)
CURVE()
GEOMETRIC_REPRESENTATION_ITEM()
RATIONAL_B_SPLINE_CURVE((1.07140024848293,1.15427334611268,1.1542733461127))
REPRESENTATION_ITEM('')
);
#1784=(
BOUNDED_CURVE()
B_SPLINE_CURVE(2,(#44333,#44334,#44335),.UNSPECIFIED.,.F.,.F.)
B_SPLINE_CURVE_WITH_KNOTS((3,3),(0.149747849205877,0.971656649213287),
 .UNSPECIFIED.)
CURVE()
GEOMETRIC_REPRESENTATION_ITEM()
RATIONAL_B_SPLINE_CURVE((1.07140024848293,1.23714644374248,1.07140024848293))
REPRESENTATION_ITEM('')
);
#2445=FACE_OUTER_BOUND('',#3564,.T.);
#2446=FACE_OUTER_BOUND('',#3565,.T.);
#2447=FACE_OUTER_BOUND('',#3566,.T.);
#2448=FACE_OUTER_BOUND('',#3567,.T.);
#2449=FACE_OUTER_BOUND('',#3568,.T.);
#2450=FACE_OUTER_BOUND('',#3569,.T.);
#2451=FACE_OUTER_BOUND('',#3570,.T.);
#2452=FACE_OUTER_BOUND('',#3571,.T.);
#2453=FACE_OUTER_BOUND('',#3572,.T.);
#2454=FACE_OUTER_BOUND('',#3573,.T.);
#2455=FACE_OUTER_BOUND('',#3574,.T.);
#2456=FACE_OUTER_BOUND('',#3575,.T.);
#2457=FACE_OUTER_BOUND('',#3576,.T.);
#2458=FACE_OUTER_BOUND('',#3577,.T.);
#2459=FACE_OUTER_BOUND('',#3578,.T.);
#2460=FACE_OUTER_BOUND('',#3579,.T.);
#2461=FACE_OUTER_BOUND('',#3580,.T.);
#2462=FACE_OUTER_BOUND('',#3581,.T.);
#2463=FACE_OUTER_BOUND('',#3582,.T.);
#2464=FACE_OUTER_BOUND('',#3583,.T.);
#2465=FACE_OUTER_BOUND('',#3584,.T.);
#2466=FACE_OUTER_BOUND('',#3585,.T.);
#2467=FACE_OUTER_BOUND('',#3586,.T.);
#2468=FACE_OUTER_BOUND('',#3587,.T.);
#2469=FACE_OUTER_BOUND('',#3588,.T.);
#2470=FACE_OUTER_BOUND('',#3589,.T.);
#2471=FACE_OUTER_BOUND('',#3590,.T.);
#2472=FACE_OUTER_BOUND('',#3591,.T.);
#2473=FACE_OUTER_BOUND('',#3592,.T.);
#2474=FACE_OUTER_BOUND('',#3593,.T.);
#2475=FACE_OUTER_BOUND('',#3594,.T.);
#2476=FACE_OUTER_BOUND('',#3595,.T.);
#2477=FACE_OUTER_BOUND('',#3596,.T.);
#2478=FACE_OUTER_BOUND('',#3597,.T.);
#2479=FACE_OUTER_BOUND('',#3598,.T.);
#2480=FACE_OUTER_BOUND('',#3599,.T.);
#2481=FACE_OUTER_BOUND('',#3600,.T.);
#2482=FACE_OUTER_BOUND('',#3601,.T.);
#2483=FACE_OUTER_BOUND('',#3602,.T.);
#2484=FACE_OUTER_BOUND('',#3603,.T.);
#2485=FACE_OUTER_BOUND('',#3604,.T.);
#2486=FACE_OUTER_BOUND('',#3605,.T.);
#2487=FACE_OUTER_BOUND('',#3606,.T.);
#2488=FACE_OUTER_BOUND('',#3607,.T.);
#2489=FACE_OUTER_BOUND('',#3608,.T.);
#2490=FACE_OUTER_BOUND('',#3609,.T.);
#2491=FACE_OUTER_BOUND('',#3610,.T.);
#2492=FACE_OUTER_BOUND('',#3611,.T.);
#2493=FACE_OUTER_BOUND('',#3612,.T.);
#2494=FACE_OUTER_BOUND('',#3613,.T.);
#2495=FACE_OUTER_BOUND('',#3614,.T.);
#2496=FACE_OUTER_BOUND('',#3615,.T.);
#2497=FACE_OUTER_BOUND('',#3616,.T.);
#2498=FACE_OUTER_BOUND('',#3617,.T.);
#2499=FACE_OUTER_BOUND('',#3618,.T.);
#2500=FACE_OUTER_BOUND('',#3619,.T.);
#2501=FACE_OUTER_BOUND('',#3620,.T.);
#2502=FACE_OUTER_BOUND('',#3621,.T.);
#2503=FACE_OUTER_BOUND('',#3622,.T.);
#2504=FACE_OUTER_BOUND('',#3623,.T.);
#2505=FACE_OUTER_BOUND('',#3624,.T.);
#2506=FACE_OUTER_BOUND('',#3625,.T.);
#2507=FACE_OUTER_BOUND('',#3626,.T.);
#2508=FACE_OUTER_BOUND('',#3627,.T.);
#2509=FACE_OUTER_BOUND('',#3628,.T.);
#2510=FACE_OUTER_BOUND('',#3629,.T.);
#2511=FACE_OUTER_BOUND('',#3630,.T.);
#2512=FACE_OUTER_BOUND('',#3631,.T.);
#2513=FACE_OUTER_BOUND('',#3632,.T.);
#2514=FACE_OUTER_BOUND('',#3633,.T.);
#2515=FACE_OUTER_BOUND('',#3634,.T.);
#2516=FACE_OUTER_BOUND('',#3635,.T.);
#2517=FACE_OUTER_BOUND('',#3636,.T.);
#2518=FACE_OUTER_BOUND('',#3637,.T.);
#2519=FACE_OUTER_BOUND('',#3638,.T.);
#2520=FACE_OUTER_BOUND('',#3639,.T.);
#2521=FACE_OUTER_BOUND('',#3640,.T.);
#2522=FACE_OUTER_BOUND('',#3641,.T.);
#2523=FACE_OUTER_BOUND('',#3642,.T.);
#2524=FACE_OUTER_BOUND('',#3643,.T.);
#2525=FACE_OUTER_BOUND('',#3644,.T.);
#2526=FACE_OUTER_BOUND('',#3645,.T.);
#2527=FACE_OUTER_BOUND('',#3646,.T.);
#2528=FACE_OUTER_BOUND('',#3647,.T.);
#2529=FACE_OUTER_BOUND('',#3648,.T.);
#2530=FACE_OUTER_BOUND('',#3649,.T.);
#2531=FACE_OUTER_BOUND('',#3650,.T.);
#2532=FACE_OUTER_BOUND('',#3651,.T.);
#2533=FACE_OUTER_BOUND('',#3652,.T.);
#2534=FACE_OUTER_BOUND('',#3653,.T.);
#2535=FACE_OUTER_BOUND('',#3654,.T.);
#2536=FACE_OUTER_BOUND('',#3655,.T.);
#2537=FACE_OUTER_BOUND('',#3656,.T.);
#2538=FACE_OUTER_BOUND('',#3657,.T.);
#2539=FACE_OUTER_BOUND('',#3658,.T.);
#2540=FACE_OUTER_BOUND('',#3659,.T.);
#2541=FACE_OUTER_BOUND('',#3660,.T.);
#2542=FACE_OUTER_BOUND('',#3662,.T.);
#2543=FACE_OUTER_BOUND('',#3663,.T.);
#2544=FACE_OUTER_BOUND('',#3664,.T.);
#2545=FACE_OUTER_BOUND('',#3665,.T.);
#2546=FACE_OUTER_BOUND('',#3666,.T.);
#2547=FACE_OUTER_BOUND('',#3667,.T.);
#2548=FACE_OUTER_BOUND('',#3668,.T.);
#3564=EDGE_LOOP('',(#13812,#13813,#13814,#13815));
#3565=EDGE_LOOP('',(#13816,#13817,#13818,#13819));
#3566=EDGE_LOOP('',(#13820,#13821,#13822,#13823));
#3567=EDGE_LOOP('',(#13824,#13825,#13826,#13827));
#3568=EDGE_LOOP('',(#13828,#13829,#13830,#13831));
#3569=EDGE_LOOP('',(#13832,#13833,#13834,#13835));
#3570=EDGE_LOOP('',(#13836,#13837,#13838,#13839));
#3571=EDGE_LOOP('',(#13840,#13841,#13842,#13843));
#3572=EDGE_LOOP('',(#13844,#13845,#13846,#13847));
#3573=EDGE_LOOP('',(#13848,#13849,#13850,#13851));
#3574=EDGE_LOOP('',(#13852,#13853,#13854,#13855));
#3575=EDGE_LOOP('',(#13856,#13857,#13858,#13859));
#3576=EDGE_LOOP('',(#13860,#13861,#13862,#13863));
#3577=EDGE_LOOP('',(#13864,#13865,#13866,#13867));
#3578=EDGE_LOOP('',(#13868,#13869,#13870,#13871));
#3579=EDGE_LOOP('',(#13872,#13873,#13874,#13875));
#3580=EDGE_LOOP('',(#13876,#13877,#13878,#13879));
#3581=EDGE_LOOP('',(#13880,#13881,#13882,#13883));
#3582=EDGE_LOOP('',(#13884,#13885,#13886,#13887));
#3583=EDGE_LOOP('',(#13888,#13889,#13890,#13891));
#3584=EDGE_LOOP('',(#13892,#13893,#13894,#13895));
#3585=EDGE_LOOP('',(#13896,#13897,#13898,#13899));
#3586=EDGE_LOOP('',(#13900,#13901,#13902,#13903));
#3587=EDGE_LOOP('',(#13904,#13905,#13906,#13907));
#3588=EDGE_LOOP('',(#13908,#13909,#13910,#13911));
#3589=EDGE_LOOP('',(#13912,#13913,#13914,#13915));
#3590=EDGE_LOOP('',(#13916,#13917,#13918,#13919));
#3591=EDGE_LOOP('',(#13920,#13921,#13922,#13923));
#3592=EDGE_LOOP('',(#13924,#13925,#13926,#13927));
#3593=EDGE_LOOP('',(#13928,#13929,#13930,#13931));
#3594=EDGE_LOOP('',(#13932,#13933,#13934,#13935));
#3595=EDGE_LOOP('',(#13936,#13937,#13938,#13939));
#3596=EDGE_LOOP('',(#13940,#13941,#13942,#13943));
#3597=EDGE_LOOP('',(#13944,#13945,#13946,#13947));
#3598=EDGE_LOOP('',(#13948,#13949,#13950,#13951));
#3599=EDGE_LOOP('',(#13952,#13953,#13954,#13955));
#3600=EDGE_LOOP('',(#13956,#13957,#13958,#13959));
#3601=EDGE_LOOP('',(#13960,#13961,#13962,#13963));
#3602=EDGE_LOOP('',(#13964,#13965,#13966,#13967));
#3603=EDGE_LOOP('',(#13968,#13969,#13970,#13971));
#3604=EDGE_LOOP('',(#13972,#13973,#13974,#13975));
#3605=EDGE_LOOP('',(#13976,#13977,#13978,#13979));
#3606=EDGE_LOOP('',(#13980,#13981,#13982,#13983));
#3607=EDGE_LOOP('',(#13984,#13985,#13986,#13987));
#3608=EDGE_LOOP('',(#13988,#13989,#13990));
#3609=EDGE_LOOP('',(#13991,#13992,#13993,#13994,#13995));
#3610=EDGE_LOOP('',(#13996,#13997,#13998,#13999));
#3611=EDGE_LOOP('',(#14000,#14001,#14002,#14003));
#3612=EDGE_LOOP('',(#14004,#14005,#14006,#14007));
#3613=EDGE_LOOP('',(#14008,#14009,#14010,#14011));
#3614=EDGE_LOOP('',(#14012,#14013,#14014,#14015));
#3615=EDGE_LOOP('',(#14016,#14017,#14018,#14019));
#3616=EDGE_LOOP('',(#14020,#14021,#14022,#14023));
#3617=EDGE_LOOP('',(#14024,#14025,#14026,#14027));
#3618=EDGE_LOOP('',(#14028,#14029,#14030,#14031));
#3619=EDGE_LOOP('',(#14032,#14033,#14034,#14035));
#3620=EDGE_LOOP('',(#14036,#14037,#14038,#14039));
#3621=EDGE_LOOP('',(#14040,#14041,#14042,#14043));
#3622=EDGE_LOOP('',(#14044,#14045,#14046,#14047));
#3623=EDGE_LOOP('',(#14048,#14049,#14050,#14051));
#3624=EDGE_LOOP('',(#14052,#14053,#14054,#14055));
#3625=EDGE_LOOP('',(#14056,#14057,#14058,#14059));
#3626=EDGE_LOOP('',(#14060,#14061,#14062,#14063));
#3627=EDGE_LOOP('',(#14064,#14065,#14066,#14067));
#3628=EDGE_LOOP('',(#14068,#14069,#14070,#14071));
#3629=EDGE_LOOP('',(#14072,#14073,#14074,#14075));
#3630=EDGE_LOOP('',(#14076,#14077,#14078,#14079));
#3631=EDGE_LOOP('',(#14080,#14081,#14082,#14083));
#3632=EDGE_LOOP('',(#14084,#14085,#14086,#14087));
#3633=EDGE_LOOP('',(#14088,#14089,#14090,#14091));
#3634=EDGE_LOOP('',(#14092,#14093,#14094,#14095));
#3635=EDGE_LOOP('',(#14096,#14097,#14098,#14099));
#3636=EDGE_LOOP('',(#14100,#14101,#14102,#14103));
#3637=EDGE_LOOP('',(#14104,#14105,#14106,#14107));
#3638=EDGE_LOOP('',(#14108,#14109,#14110,#14111));
#3639=EDGE_LOOP('',(#14112,#14113,#14114,#14115));
#3640=EDGE_LOOP('',(#14116,#14117,#14118,#14119));
#3641=EDGE_LOOP('',(#14120,#14121,#14122,#14123));
#3642=EDGE_LOOP('',(#14124,#14125,#14126,#14127));
#3643=EDGE_LOOP('',(#14128,#14129,#14130,#14131));
#3644=EDGE_LOOP('',(#14132,#14133,#14134,#14135));
#3645=EDGE_LOOP('',(#14136,#14137,#14138,#14139));
#3646=EDGE_LOOP('',(#14140,#14141,#14142,#14143));
#3647=EDGE_LOOP('',(#14144,#14145,#14146,#14147));
#3648=EDGE_LOOP('',(#14148,#14149,#14150,#14151));
#3649=EDGE_LOOP('',(#14152,#14153,#14154,#14155));
#3650=EDGE_LOOP('',(#14156,#14157,#14158,#14159));
#3651=EDGE_LOOP('',(#14160,#14161,#14162,#14163));
#3652=EDGE_LOOP('',(#14164,#14165,#14166,#14167,#14168,#14169,#14170,#14171,
#14172,#14173,#14174,#14175,#14176,#14177,#14178,#14179,#14180,#14181,#14182,
#14183,#14184,#14185,#14186,#14187,#14188,#14189,#14190,#14191,#14192,#14193,
#14194,#14195,#14196,#14197,#14198,#14199,#14200,#14201,#14202,#14203,#14204,
#14205,#14206,#14207,#14208,#14209,#14210,#14211,#14212,#14213,#14214,#14215,
#14216,#14217,#14218,#14219,#14220,#14221,#14222,#14223,#14224,#14225,#14226,
#14227,#14228,#14229,#14230,#14231,#14232,#14233,#14234,#14235,#14236,#14237,
#14238,#14239,#14240,#14241,#14242,#14243,#14244,#14245,#14246,#14247,#14248,
#14249,#14250,#14251,#14252,#14253,#14254));
#3653=EDGE_LOOP('',(#14255,#14256,#14257,#14258,#14259));
#3654=EDGE_LOOP('',(#14260,#14261,#14262,#14263));
#3655=EDGE_LOOP('',(#14264,#14265,#14266,#14267,#14268,#14269,#14270,#14271,
#14272,#14273,#14274,#14275,#14276,#14277,#14278,#14279,#14280,#14281,#14282,
#14283,#14284,#14285,#14286,#14287,#14288,#14289,#14290,#14291,#14292,#14293,
#14294,#14295,#14296,#14297,#14298,#14299,#14300,#14301,#14302,#14303,#14304,
#14305,#14306,#14307,#14308,#14309,#14310,#14311,#14312,#14313,#14314,#14315,
#14316,#14317,#14318,#14319,#14320,#14321,#14322,#14323,#14324,#14325,#14326,
#14327,#14328,#14329,#14330,#14331,#14332,#14333,#14334,#14335,#14336,#14337,
#14338,#14339,#14340,#14341,#14342,#14343,#14344,#14345,#14346,#14347,#14348,
#14349,#14350,#14351,#14352,#14353,#14354,#14355));
#3656=EDGE_LOOP('',(#14356,#14357,#14358,#14359,#14360,#14361,#14362,#14363,
#14364,#14365));
#3657=EDGE_LOOP('',(#14366,#14367,#14368,#14369));
#3658=EDGE_LOOP('',(#14370,#14371,#14372,#14373));
#3659=EDGE_LOOP('',(#14374,#14375,#14376,#14377));
#3660=EDGE_LOOP('',(#14378,#14379,#14380,#14381,#14382,#14383));
#3661=EDGE_LOOP('',(#14384,#14385,#14386,#14387,#14388));
#3662=EDGE_LOOP('',(#14389,#14390,#14391,#14392));
#3663=EDGE_LOOP('',(#14393,#14394,#14395,#14396));
#3664=EDGE_LOOP('',(#14397,#14398,#14399,#14400,#14401));
#3665=EDGE_LOOP('',(#14402));
#3666=EDGE_LOOP('',(#14403));
#3667=EDGE_LOOP('',(#14404,#14405,#14406,#14407,#14408,#14409));
#3668=EDGE_LOOP('',(#14410,#14411,#14412,#14413));
#4540=LINE('',#38396,#5494);
#4541=LINE('',#38420,#5495);
#4542=LINE('',#38468,#5496);
#4543=LINE('',#38516,#5497);
#4544=LINE('',#38567,#5498);
#4545=LINE('',#38618,#5499);
#4546=LINE('',#38666,#5500);
#4547=LINE('',#38714,#5501);
#4548=LINE('',#38768,#5502);
#4549=LINE('',#38816,#5503);
#4550=LINE('',#38864,#5504);
#4551=LINE('',#38918,#5505);
#4552=LINE('',#38966,#5506);
#4553=LINE('',#39014,#5507);
#4554=LINE('',#39062,#5508);
#4555=LINE('',#39116,#5509);
#4556=LINE('',#39164,#5510);
#4557=LINE('',#39212,#5511);
#4558=LINE('',#39266,#5512);
#4559=LINE('',#39314,#5513);
#4560=LINE('',#39362,#5514);
#4561=LINE('',#39416,#5515);
#4562=LINE('',#39464,#5516);
#4563=LINE('',#39512,#5517);
#4564=LINE('',#39560,#5518);
#4565=LINE('',#39614,#5519);
#4566=LINE('',#39662,#5520);
#4567=LINE('',#39710,#5521);
#4568=LINE('',#39764,#5522);
#4569=LINE('',#39812,#5523);
#4570=LINE('',#39860,#5524);
#4571=LINE('',#39914,#5525);
#4572=LINE('',#39962,#5526);
#4573=LINE('',#40010,#5527);
#4574=LINE('',#40058,#5528);
#4575=LINE('',#40112,#5529);
#4576=LINE('',#40160,#5530);
#4577=LINE('',#40208,#5531);
#4578=LINE('',#40262,#5532);
#4579=LINE('',#40310,#5533);
#4580=LINE('',#40358,#5534);
#4581=LINE('',#40412,#5535);
#4582=LINE('',#40460,#5536);
#4583=LINE('',#40508,#5537);
#4584=LINE('',#40556,#5538);
#4585=LINE('',#40566,#5539);
#4586=LINE('',#40591,#5540);
#4587=LINE('',#40615,#5541);
#4588=LINE('',#40639,#5542);
#4589=LINE('',#40664,#5543);
#4590=LINE('',#40689,#5544);
#4591=LINE('',#40713,#5545);
#4592=LINE('',#40738,#5546);
#4593=LINE('',#40763,#5547);
#4594=LINE('',#40787,#5548);
#4595=LINE('',#40812,#5549);
#4596=LINE('',#40837,#5550);
#4597=LINE('',#40861,#5551);
#4598=LINE('',#40885,#5552);
#4599=LINE('',#40910,#5553);
#4600=LINE('',#40935,#5554);
#4601=LINE('',#40959,#5555);
#4602=LINE('',#40984,#5556);
#4603=LINE('',#41009,#5557);
#4604=LINE('',#41033,#5558);
#4605=LINE('',#41058,#5559);
#4606=LINE('',#41083,#5560);
#4607=LINE('',#41107,#5561);
#4608=LINE('',#41131,#5562);
#4609=LINE('',#41156,#5563);
#4610=LINE('',#41181,#5564);
#4611=LINE('',#41205,#5565);
#4612=LINE('',#41230,#5566);
#4613=LINE('',#41255,#5567);
#4614=LINE('',#41279,#5568);
#4615=LINE('',#41304,#5569);
#4616=LINE('',#41329,#5570);
#4617=LINE('',#41353,#5571);
#4618=LINE('',#41377,#5572);
#4619=LINE('',#41402,#5573);
#4620=LINE('',#41427,#5574);
#4621=LINE('',#41451,#5575);
#4622=LINE('',#41476,#5576);
#4623=LINE('',#41501,#5577);
#4624=LINE('',#41525,#5578);
#4625=LINE('',#41550,#5579);
#4626=LINE('',#41574,#5580);
#4627=LINE('',#41599,#5581);
#4628=LINE('',#44327,#5582);
#4629=LINE('',#44338,#5583);
#4630=LINE('',#44340,#5584);
#4631=LINE('',#44341,#5585);
#4632=LINE('',#44344,#5586);
#4633=LINE('',#44345,#5587);
#4634=LINE('',#44348,#5588);
#4635=LINE('',#44349,#5589);
#4636=LINE('',#44352,#5590);
#4637=LINE('',#44354,#5591);
#4638=LINE('',#44355,#5592);
#4639=LINE('',#44358,#5593);
#4640=LINE('',#44360,#5594);
#4641=LINE('',#44367,#5595);
#5494=VECTOR('',#21802,4.);
#5495=VECTOR('',#21807,4.);
#5496=VECTOR('',#21810,4.);
#5497=VECTOR('',#21813,4.);
#5498=VECTOR('',#21816,4.);
#5499=VECTOR('',#21819,4.);
#5500=VECTOR('',#21822,4.);
#5501=VECTOR('',#21825,4.);
#5502=VECTOR('',#21828,4.);
#5503=VECTOR('',#21831,4.);
#5504=VECTOR('',#21834,4.);
#5505=VECTOR('',#21837,4.);
#5506=VECTOR('',#21840,4.);
#5507=VECTOR('',#21843,4.);
#5508=VECTOR('',#21846,4.);
#5509=VECTOR('',#21849,4.);
#5510=VECTOR('',#21852,4.);
#5511=VECTOR('',#21855,4.);
#5512=VECTOR('',#21858,4.);
#5513=VECTOR('',#21861,4.);
#5514=VECTOR('',#21864,4.);
#5515=VECTOR('',#21867,4.);
#5516=VECTOR('',#21870,4.);
#5517=VECTOR('',#21873,4.);
#5518=VECTOR('',#21876,4.);
#5519=VECTOR('',#21879,4.);
#5520=VECTOR('',#21882,4.);
#5521=VECTOR('',#21885,4.);
#5522=VECTOR('',#21888,4.);
#5523=VECTOR('',#21891,4.);
#5524=VECTOR('',#21894,4.);
#5525=VECTOR('',#21897,4.);
#5526=VECTOR('',#21900,4.);
#5527=VECTOR('',#21903,4.);
#5528=VECTOR('',#21906,4.);
#5529=VECTOR('',#21909,4.);
#5530=VECTOR('',#21912,4.);
#5531=VECTOR('',#21915,4.);
#5532=VECTOR('',#21918,4.);
#5533=VECTOR('',#21921,4.);
#5534=VECTOR('',#21924,4.);
#5535=VECTOR('',#21927,4.);
#5536=VECTOR('',#21930,4.);
#5537=VECTOR('',#21933,4.);
#5538=VECTOR('',#21936,3.22275);
#5539=VECTOR('',#21941,3.22275);
#5540=VECTOR('',#21946,3.22275);
#5541=VECTOR('',#21949,3.22275);
#5542=VECTOR('',#21952,3.22275);
#5543=VECTOR('',#21955,3.22275);
#5544=VECTOR('',#21958,3.22275);
#5545=VECTOR('',#21961,3.22275);
#5546=VECTOR('',#21964,3.22275);
#5547=VECTOR('',#21967,3.22275);
#5548=VECTOR('',#21970,3.22275);
#5549=VECTOR('',#21973,3.22275);
#5550=VECTOR('',#21976,3.22275);
#5551=VECTOR('',#21979,3.22275);
#5552=VECTOR('',#21982,3.22275);
#5553=VECTOR('',#21985,3.22275);
#5554=VECTOR('',#21988,3.22275);
#5555=VECTOR('',#21991,3.22275);
#5556=VECTOR('',#21994,3.22275);
#5557=VECTOR('',#21997,3.22275);
#5558=VECTOR('',#22000,3.22275);
#5559=VECTOR('',#22003,3.22275);
#5560=VECTOR('',#22006,3.22275);
#5561=VECTOR('',#22009,3.22275);
#5562=VECTOR('',#22012,3.22275);
#5563=VECTOR('',#22015,3.22275);
#5564=VECTOR('',#22018,3.22275);
#5565=VECTOR('',#22021,3.22275);
#5566=VECTOR('',#22024,3.22275);
#5567=VECTOR('',#22027,3.22275);
#5568=VECTOR('',#22030,3.22275);
#5569=VECTOR('',#22033,3.22275);
#5570=VECTOR('',#22036,3.22275);
#5571=VECTOR('',#22039,3.22275);
#5572=VECTOR('',#22042,3.22275);
#5573=VECTOR('',#22045,3.22275);
#5574=VECTOR('',#22048,3.22275);
#5575=VECTOR('',#22051,3.22275);
#5576=VECTOR('',#22054,3.22275);
#5577=VECTOR('',#22057,3.22275);
#5578=VECTOR('',#22060,3.22275);
#5579=VECTOR('',#22063,3.22275);
#5580=VECTOR('',#22066,3.22275);
#5581=VECTOR('',#22069,3.22275);
#5582=VECTOR('',#22082,7.25527674973257);
#5583=VECTOR('',#22087,10.);
#5584=VECTOR('',#22088,10.);
#5585=VECTOR('',#22089,10.);
#5586=VECTOR('',#22092,10.);
#5587=VECTOR('',#22093,10.);
#5588=VECTOR('',#22096,10.);
#5589=VECTOR('',#22097,10.);
#5590=VECTOR('',#22100,10.);
#5591=VECTOR('',#22101,10.);
#5592=VECTOR('',#22102,10.);
#5593=VECTOR('',#22107,10.);
#5594=VECTOR('',#22110,10.);
#5595=VECTOR('',#22121,3.75);
#6130=B_SPLINE_CURVE_WITH_KNOTS('',3,(#38398,#38399,#38400,#38401,#38402,
#38403,#38404,#38405,#38406,#38407),.UNSPECIFIED.,.F.,.F.,(4,3,3,4),(-4.09274904019427,
-3.99053949058499,-2.99290461793874,-2.06120159751576),.UNSPECIFIED.);
#6131=B_SPLINE_CURVE_WITH_KNOTS('',3,(#38410,#38411,#38412,#38413,#38414,
#38415,#38416),.UNSPECIFIED.,.F.,.F.,(4,3,4),(0.,0.997634872646276,1.11004521091191),
 .UNSPECIFIED.);
#6132=B_SPLINE_CURVE_WITH_KNOTS('',3,(#38421,#38422,#38423,#38424,#38425,
#38426,#38427,#38428,#38429,#38430,#38431,#38432,#38433,#38434,#38435,#38436,
#38437,#38438,#38439,#38440,#38441,#38442),.UNSPECIFIED.,.F.,.F.,(4,3,3,
3,3,3,3,4),(-10.3759343473739,-9.97634872646248,-8.97871385381623,-7.98107898116998,
-6.98344410852373,-5.98580923587749,-4.98817436323124,-4.09274904019427),
 .UNSPECIFIED.);
#6133=B_SPLINE_CURVE_WITH_KNOTS('',3,(#38443,#38444,#38445,#38446,#38447,
#38448,#38449,#38450,#38451,#38452,#38453,#38454,#38455,#38456,#38457,#38458,
#38459,#38460,#38461,#38462,#38463,#38464),.UNSPECIFIED.,.F.,.F.,(4,3,3,
3,3,3,3,4),(1.11004521091191,1.99526974529252,2.99290461793875,3.99053949058499,
4.98817436323123,5.98580923587746,6.9834441085237,7.3932305180915),
 .UNSPECIFIED.);
#6134=B_SPLINE_CURVE_WITH_KNOTS('',3,(#38469,#38470,#38471,#38472,#38473,
#38474,#38475,#38476,#38477,#38478,#38479,#38480,#38481,#38482,#38483,#38484,
#38485,#38486,#38487,#38488,#38489,#38490),.UNSPECIFIED.,.F.,.F.,(4,3,3,
3,3,3,3,4),(-16.6591196545534,-15.96215796234,-14.9645230896937,-13.9668882170475,
-12.9692533444012,-11.971618471755,-10.9739835991087,-10.3759343473739),
 .UNSPECIFIED.);
#6135=B_SPLINE_CURVE_WITH_KNOTS('',3,(#38491,#38492,#38493,#38494,#38495,
#38496,#38497,#38498,#38499,#38500,#38501,#38502,#38503,#38504,#38505,#38506,
#38507,#38508,#38509,#38510,#38511,#38512),.UNSPECIFIED.,.F.,.F.,(4,3,3,
3,3,3,3,4),(7.3932305180915,7.98107898116995,8.97871385381621,9.97634872646246,
10.9739835991087,11.971618471755,12.9692533444012,13.6764158252711),
 .UNSPECIFIED.);
#6136=B_SPLINE_CURVE_WITH_KNOTS('',3,(#38517,#38518,#38519,#38520,#38521,
#38522,#38523,#38524,#38525,#38526,#38527,#38528,#38529,#38530,#38531,#38532,
#38533,#38534,#38535,#38536,#38537,#38538),.UNSPECIFIED.,.F.,.F.,(4,3,3,
3,3,3,3,4),(-22.942304961733,-21.9479671982174,-20.9503323255712,-19.952697452925,
-18.9550625802787,-17.9574277076325,-16.9597928349862,-16.6591196545534),
 .UNSPECIFIED.);
#6137=B_SPLINE_CURVE_WITH_KNOTS('',3,(#38539,#38540,#38541,#38542,#38543,
#38544,#38545,#38546,#38547,#38548,#38549,#38550,#38551,#38552,#38553,#38554,
#38555,#38556,#38557,#38558,#38559,#38560,#38561,#38562,#38563),
 .UNSPECIFIED.,.F.,.F.,(4,3,3,3,3,3,3,3,4),(13.6764158252711,13.9668882170475,
14.9645230896937,15.96215796234,16.9597928349862,17.9574277076325,18.9550625802787,
19.9526974529249,19.9596011324507),.UNSPECIFIED.);
#6138=B_SPLINE_CURVE_WITH_KNOTS('',3,(#38568,#38569,#38570,#38571,#38572,
#38573,#38574,#38575,#38576,#38577,#38578,#38579,#38580,#38581,#38582,#38583,
#38584,#38585,#38586,#38587,#38588,#38589,#38590,#38591,#38592),
 .UNSPECIFIED.,.F.,.F.,(4,3,3,3,3,3,3,3,4),(-29.2254902689126,-28.9314113067412,
-27.9337764340949,-26.9361415614487,-25.9385066888024,-24.9408718161562,
-23.9432369435099,-22.9456020708637,-22.942304961733),.UNSPECIFIED.);
#6139=B_SPLINE_CURVE_WITH_KNOTS('',3,(#38593,#38594,#38595,#38596,#38597,
#38598,#38599,#38600,#38601,#38602,#38603,#38604,#38605,#38606,#38607,#38608,
#38609,#38610,#38611,#38612,#38613,#38614),.UNSPECIFIED.,.F.,.F.,(4,3,3,
3,3,3,3,4),(19.9596011324507,20.9503323255712,21.9479671982174,22.9456020708637,
23.9432369435099,24.9408718161562,25.9385066888024,26.2427864396303),
 .UNSPECIFIED.);
#6140=B_SPLINE_CURVE_WITH_KNOTS('',3,(#38619,#38620,#38621,#38622,#38623,
#38624,#38625,#38626,#38627,#38628,#38629,#38630,#38631,#38632,#38633,#38634,
#38635,#38636,#38637,#38638,#38639,#38640),.UNSPECIFIED.,.F.,.F.,(4,3,3,
3,3,3,3,4),(-35.5086755760922,-34.9172205426187,-33.9195856699724,-32.9219507973262,
-31.9243159246799,-30.9266810520337,-29.9290461793874,-29.2254902689126),
 .UNSPECIFIED.);
#6141=B_SPLINE_CURVE_WITH_KNOTS('',3,(#38641,#38642,#38643,#38644,#38645,
#38646,#38647,#38648,#38649,#38650,#38651,#38652,#38653,#38654,#38655,#38656,
#38657,#38658,#38659,#38660,#38661,#38662),.UNSPECIFIED.,.F.,.F.,(4,3,3,
3,3,3,3,4),(26.2427864396303,26.9361415614487,27.9337764340949,28.9314113067412,
29.9290461793874,30.9266810520337,31.92431592468,32.5259717468098),
 .UNSPECIFIED.);
#6142=B_SPLINE_CURVE_WITH_KNOTS('',3,(#38667,#38668,#38669,#38670,#38671,
#38672,#38673,#38674,#38675,#38676,#38677,#38678,#38679,#38680,#38681,#38682,
#38683,#38684,#38685,#38686,#38687,#38688),.UNSPECIFIED.,.F.,.F.,(4,3,3,
3,3,3,3,4),(-41.7918608832718,-40.9030297784961,-39.9053949058499,-38.9077600332037,
-37.9101251605574,-36.9124902879112,-35.9148554152649,-35.5086755760922),
 .UNSPECIFIED.);
#6143=B_SPLINE_CURVE_WITH_KNOTS('',3,(#38689,#38690,#38691,#38692,#38693,
#38694,#38695,#38696,#38697,#38698,#38699,#38700,#38701,#38702,#38703,#38704,
#38705,#38706,#38707,#38708,#38709,#38710),.UNSPECIFIED.,.F.,.F.,(4,3,3,
3,3,3,3,4),(32.5259717468098,32.9219507973262,33.9195856699724,34.9172205426187,
35.9148554152649,36.9124902879112,37.9101251605574,38.8091570539894),
 .UNSPECIFIED.);
#6144=B_SPLINE_CURVE_WITH_KNOTS('',3,(#38715,#38716,#38717,#38718,#38719,
#38720,#38721,#38722,#38723,#38724,#38725,#38726,#38727,#38728,#38729,#38730,
#38731,#38732,#38733,#38734,#38735,#38736,#38737,#38738,#38739),
 .UNSPECIFIED.,.F.,.F.,(4,3,3,3,3,3,3,3,4),(-48.0750461904514,-47.8864738870199,
-46.8888390143736,-45.8912041417274,-44.8935692690811,-43.8959343964349,
-42.8982995237886,-41.9006646511424,-41.7918608832718),.UNSPECIFIED.);
#6145=B_SPLINE_CURVE_WITH_KNOTS('',3,(#38740,#38741,#38742,#38743,#38744,
#38745,#38746,#38747,#38748,#38749,#38750,#38751,#38752,#38753,#38754,#38755,
#38756,#38757,#38758,#38759,#38760,#38761,#38762,#38763,#38764),
 .UNSPECIFIED.,.F.,.F.,(4,3,3,3,3,3,3,3,4),(38.8091570539894,38.9077600332037,
39.9053949058499,40.9030297784962,41.9006646511424,42.8982995237887,43.8959343964349,
44.8935692690811,45.092342361169),.UNSPECIFIED.);
#6146=B_SPLINE_CURVE_WITH_KNOTS('',3,(#38769,#38770,#38771,#38772,#38773,
#38774,#38775,#38776,#38777,#38778,#38779,#38780,#38781,#38782,#38783,#38784,
#38785,#38786,#38787,#38788,#38789,#38790),.UNSPECIFIED.,.F.,.F.,(4,3,3,
3,3,3,3,4),(-54.358231497631,-53.8722831228974,-52.8746482502511,-51.8770133776049,
-50.8793785049586,-49.8817436323124,-48.8841087596661,-48.0750461904514),
 .UNSPECIFIED.);
#6147=B_SPLINE_CURVE_WITH_KNOTS('',3,(#38791,#38792,#38793,#38794,#38795,
#38796,#38797,#38798,#38799,#38800,#38801,#38802,#38803,#38804,#38805,#38806,
#38807,#38808,#38809,#38810,#38811,#38812),.UNSPECIFIED.,.F.,.F.,(4,3,3,
3,3,3,3,4),(45.092342361169,45.8912041417274,46.8888390143737,47.8864738870199,
48.8841087596661,49.8817436323124,50.8793785049587,51.3755276683486),
 .UNSPECIFIED.);
#6148=B_SPLINE_CURVE_WITH_KNOTS('',3,(#38817,#38818,#38819,#38820,#38821,
#38822,#38823,#38824,#38825,#38826,#38827,#38828,#38829,#38830,#38831,#38832,
#38833,#38834,#38835,#38836,#38837,#38838),.UNSPECIFIED.,.F.,.F.,(4,3,3,
3,3,3,3,4),(-60.6414168048106,-59.8580923587748,-58.8604574861286,-57.8628226134824,
-56.8651877408361,-55.8675528681899,-54.8699179955436,-54.358231497631),
 .UNSPECIFIED.);
#6149=B_SPLINE_CURVE_WITH_KNOTS('',3,(#38839,#38840,#38841,#38842,#38843,
#38844,#38845,#38846,#38847,#38848,#38849,#38850,#38851,#38852,#38853,#38854,
#38855,#38856,#38857,#38858,#38859,#38860),.UNSPECIFIED.,.F.,.F.,(4,3,3,
3,3,3,3,4),(51.3755276683486,51.8770133776049,52.8746482502512,53.8722831228974,
54.8699179955437,55.8675528681899,56.8651877408361,57.6587129755282),
 .UNSPECIFIED.);
#6150=B_SPLINE_CURVE_WITH_KNOTS('',3,(#38865,#38866,#38867,#38868,#38869,
#38870,#38871,#38872,#38873,#38874,#38875,#38876,#38877,#38878,#38879,#38880,
#38881,#38882,#38883,#38884,#38885,#38886,#38887,#38888,#38889),
 .UNSPECIFIED.,.F.,.F.,(4,3,3,3,3,3,3,3,4),(-66.9246021119902,-66.8415364672986,
-65.8439015946523,-64.8462667220061,-63.8486318493598,-62.8509969767136,
-61.8533621040674,-60.8557272314211,-60.6414168048106),.UNSPECIFIED.);
#6151=B_SPLINE_CURVE_WITH_KNOTS('',3,(#38890,#38891,#38892,#38893,#38894,
#38895,#38896,#38897,#38898,#38899,#38900,#38901,#38902,#38903,#38904,#38905,
#38906,#38907,#38908,#38909,#38910,#38911,#38912,#38913,#38914),
 .UNSPECIFIED.,.F.,.F.,(4,3,3,3,3,3,3,3,4),(57.6587129755282,57.8628226134824,
58.8604574861286,59.8580923587749,60.8557272314211,61.8533621040674,62.8509969767136,
63.8486318493599,63.9418982827078),.UNSPECIFIED.);
#6152=B_SPLINE_CURVE_WITH_KNOTS('',3,(#38919,#38920,#38921,#38922,#38923,
#38924,#38925,#38926,#38927,#38928,#38929,#38930,#38931,#38932,#38933,#38934,
#38935,#38936,#38937,#38938,#38939,#38940),.UNSPECIFIED.,.F.,.F.,(4,3,3,
3,3,3,3,4),(-73.2077874191698,-72.8273457031761,-71.8297108305298,-70.8320759578836,
-69.8344410852373,-68.8368062125911,-67.8391713399448,-66.9246021119902),
 .UNSPECIFIED.);
#6153=B_SPLINE_CURVE_WITH_KNOTS('',3,(#38941,#38942,#38943,#38944,#38945,
#38946,#38947,#38948,#38949,#38950,#38951,#38952,#38953,#38954,#38955,#38956,
#38957,#38958,#38959,#38960,#38961,#38962),.UNSPECIFIED.,.F.,.F.,(4,3,3,
3,3,3,3,4),(63.9418982827078,64.8462667220061,65.8439015946524,66.8415364672986,
67.8391713399448,68.8368062125911,69.8344410852373,70.2250835898874),
 .UNSPECIFIED.);
#6154=B_SPLINE_CURVE_WITH_KNOTS('',3,(#38967,#38968,#38969,#38970,#38971,
#38972,#38973,#38974,#38975,#38976,#38977,#38978,#38979,#38980,#38981,#38982,
#38983,#38984,#38985,#38986,#38987,#38988),.UNSPECIFIED.,.F.,.F.,(4,3,3,
3,3,3,3,4),(-79.4909727263494,-78.8131549390536,-77.8155200664073,-76.8178851937611,
-75.8202503211148,-74.8226154484686,-73.8249805758223,-73.2077874191698),
 .UNSPECIFIED.);
#6155=B_SPLINE_CURVE_WITH_KNOTS('',3,(#38989,#38990,#38991,#38992,#38993,
#38994,#38995,#38996,#38997,#38998,#38999,#39000,#39001,#39002,#39003,#39004,
#39005,#39006,#39007,#39008,#39009,#39010),.UNSPECIFIED.,.F.,.F.,(4,3,3,
3,3,3,3,4),(70.2250835898874,70.8320759578836,71.8297108305298,72.8273457031761,
73.8249805758223,74.8226154484686,75.8202503211148,76.508268897067),
 .UNSPECIFIED.);
#6156=B_SPLINE_CURVE_WITH_KNOTS('',3,(#39015,#39016,#39017,#39018,#39019,
#39020,#39021,#39022,#39023,#39024,#39025,#39026,#39027,#39028,#39029,#39030,
#39031,#39032,#39033,#39034,#39035,#39036),.UNSPECIFIED.,.F.,.F.,(4,3,3,
3,3,3,3,4),(-85.7741580335289,-84.798964174931,-83.8013293022848,-82.8036944296386,
-81.8060595569923,-80.8084246843461,-79.8107898116998,-79.4909727263494),
 .UNSPECIFIED.);
#6157=B_SPLINE_CURVE_WITH_KNOTS('',3,(#39037,#39038,#39039,#39040,#39041,
#39042,#39043,#39044,#39045,#39046,#39047,#39048,#39049,#39050,#39051,#39052,
#39053,#39054,#39055,#39056,#39057,#39058),.UNSPECIFIED.,.F.,.F.,(4,3,3,
3,3,3,3,4),(76.508268897067,76.8178851937611,77.8155200664073,78.8131549390536,
79.8107898116998,80.8084246843461,81.8060595569923,82.7914542042466),
 .UNSPECIFIED.);
#6158=B_SPLINE_CURVE_WITH_KNOTS('',3,(#39063,#39064,#39065,#39066,#39067,
#39068,#39069,#39070,#39071,#39072,#39073,#39074,#39075,#39076,#39077,#39078,
#39079,#39080,#39081,#39082,#39083,#39084,#39085,#39086,#39087),
 .UNSPECIFIED.,.F.,.F.,(4,3,3,3,3,3,3,3,4),(-92.0573433407085,-91.7824082834548,
-90.7847734108085,-89.7871385381623,-88.789503665516,-87.7918687928698,
-86.7942339202235,-85.7965990475773,-85.7741580335289),.UNSPECIFIED.);
#6159=B_SPLINE_CURVE_WITH_KNOTS('',3,(#39088,#39089,#39090,#39091,#39092,
#39093,#39094,#39095,#39096,#39097,#39098,#39099,#39100,#39101,#39102,#39103,
#39104,#39105,#39106,#39107,#39108,#39109,#39110,#39111,#39112),
 .UNSPECIFIED.,.F.,.F.,(4,3,3,3,3,3,3,3,4),(82.7914542042466,82.8036944296386,
83.8013293022848,84.7989641749311,85.7965990475773,86.7942339202236,87.7918687928698,
88.789503665516,89.0746395114262),.UNSPECIFIED.);
#6160=B_SPLINE_CURVE_WITH_KNOTS('',3,(#39117,#39118,#39119,#39120,#39121,
#39122,#39123,#39124,#39125,#39126,#39127,#39128,#39129,#39130,#39131,#39132,
#39133,#39134,#39135,#39136,#39137,#39138),.UNSPECIFIED.,.F.,.F.,(4,3,3,
3,3,3,3,4),(-98.3405286478881,-97.7682175193322,-96.770582646686,-95.7729477740397,
-94.7753129013935,-93.7776780287473,-92.780043156101,-92.0573433407085),
 .UNSPECIFIED.);
#6161=B_SPLINE_CURVE_WITH_KNOTS('',3,(#39139,#39140,#39141,#39142,#39143,
#39144,#39145,#39146,#39147,#39148,#39149,#39150,#39151,#39152,#39153,#39154,
#39155,#39156,#39157,#39158,#39159,#39160),.UNSPECIFIED.,.F.,.F.,(4,3,3,
3,3,3,3,4),(89.0746395114262,89.7871385381623,90.7847734108086,91.7824082834548,
92.780043156101,93.7776780287473,94.7753129013935,95.3578248186058),
 .UNSPECIFIED.);
#6162=B_SPLINE_CURVE_WITH_KNOTS('',3,(#39165,#39166,#39167,#39168,#39169,
#39170,#39171,#39172,#39173,#39174,#39175,#39176,#39177,#39178,#39179,#39180,
#39181,#39182,#39183,#39184,#39185,#39186),.UNSPECIFIED.,.F.,.F.,(4,3,3,
3,3,3,3,4),(-104.623713955068,-103.75402675521,-102.756391882563,-101.758757009917,
-100.761122137271,-99.7634872646247,-98.7658523919785,-98.3405286478881),
 .UNSPECIFIED.);
#6163=B_SPLINE_CURVE_WITH_KNOTS('',3,(#39187,#39188,#39189,#39190,#39191,
#39192,#39193,#39194,#39195,#39196,#39197,#39198,#39199,#39200,#39201,#39202,
#39203,#39204,#39205,#39206,#39207,#39208),.UNSPECIFIED.,.F.,.F.,(4,3,3,
3,3,3,3,4),(95.3578248186058,95.7729477740397,96.770582646686,97.7682175193323,
98.7658523919785,99.7634872646248,100.761122137271,101.641010125785),
 .UNSPECIFIED.);
#6164=B_SPLINE_CURVE_WITH_KNOTS('',3,(#39213,#39214,#39215,#39216,#39217,
#39218,#39219,#39220,#39221,#39222,#39223,#39224,#39225,#39226,#39227,#39228,
#39229,#39230,#39231,#39232,#39233,#39234,#39235,#39236,#39237),
 .UNSPECIFIED.,.F.,.F.,(4,3,3,3,3,3,3,3,4),(-110.906899262247,-110.737470863733,
-109.739835991087,-108.742201118441,-107.744566245795,-106.746931373148,
-105.749296500502,-104.751661627856,-104.623713955068),.UNSPECIFIED.);
#6165=B_SPLINE_CURVE_WITH_KNOTS('',3,(#39238,#39239,#39240,#39241,#39242,
#39243,#39244,#39245,#39246,#39247,#39248,#39249,#39250,#39251,#39252,#39253,
#39254,#39255,#39256,#39257,#39258,#39259,#39260,#39261,#39262),
 .UNSPECIFIED.,.F.,.F.,(4,3,3,3,3,3,3,3,4),(101.641010125785,101.758757009917,
102.756391882564,103.75402675521,104.751661627856,105.749296500502,106.746931373149,
107.744566245795,107.924195432965),.UNSPECIFIED.);
#6166=B_SPLINE_CURVE_WITH_KNOTS('',3,(#39267,#39268,#39269,#39270,#39271,
#39272,#39273,#39274,#39275,#39276,#39277,#39278,#39279,#39280,#39281,#39282,
#39283,#39284,#39285,#39286,#39287,#39288),.UNSPECIFIED.,.F.,.F.,(4,3,3,
3,3,3,3,4),(-117.190084569427,-116.723280099611,-115.725645226965,-114.728010354318,
-113.730375481672,-112.732740609026,-111.73510573638,-110.906899262247),
 .UNSPECIFIED.);
#6167=B_SPLINE_CURVE_WITH_KNOTS('',3,(#39289,#39290,#39291,#39292,#39293,
#39294,#39295,#39296,#39297,#39298,#39299,#39300,#39301,#39302,#39303,#39304,
#39305,#39306,#39307,#39308,#39309,#39310),.UNSPECIFIED.,.F.,.F.,(4,3,3,
3,3,3,3,4),(107.924195432965,108.742201118441,109.739835991087,110.737470863734,
111.73510573638,112.732740609026,113.730375481672,114.207380740145),
 .UNSPECIFIED.);
#6168=B_SPLINE_CURVE_WITH_KNOTS('',3,(#39315,#39316,#39317,#39318,#39319,
#39320,#39321,#39322,#39323,#39324,#39325,#39326,#39327,#39328,#39329,#39330,
#39331,#39332,#39333,#39334,#39335,#39336),.UNSPECIFIED.,.F.,.F.,(4,3,3,
3,3,3,3,4),(-123.473269876607,-122.709089335488,-121.711454462842,-120.713819590196,
-119.71618471755,-118.718549844903,-117.720914972257,-117.190084569427),
 .UNSPECIFIED.);
#6169=B_SPLINE_CURVE_WITH_KNOTS('',3,(#39337,#39338,#39339,#39340,#39341,
#39342,#39343,#39344,#39345,#39346,#39347,#39348,#39349,#39350,#39351,#39352,
#39353,#39354,#39355,#39356,#39357,#39358),.UNSPECIFIED.,.F.,.F.,(4,3,3,
3,3,3,3,4),(114.207380740145,114.728010354318,115.725645226965,116.723280099611,
117.720914972257,118.718549844904,119.71618471755,120.490566047324),
 .UNSPECIFIED.);
#6170=B_SPLINE_CURVE_WITH_KNOTS('',3,(#39363,#39364,#39365,#39366,#39367,
#39368,#39369,#39370,#39371,#39372,#39373,#39374,#39375,#39376,#39377,#39378,
#39379,#39380,#39381,#39382,#39383,#39384,#39385,#39386,#39387),
 .UNSPECIFIED.,.F.,.F.,(4,3,3,3,3,3,3,3,4),(-129.756455183786,-129.692533444012,
-128.694898571366,-127.69726369872,-126.699628826073,-125.701993953427,
-124.704359080781,-123.706724208135,-123.473269876607),.UNSPECIFIED.);
#6171=B_SPLINE_CURVE_WITH_KNOTS('',3,(#39388,#39389,#39390,#39391,#39392,
#39393,#39394,#39395,#39396,#39397,#39398,#39399,#39400,#39401,#39402,#39403,
#39404,#39405,#39406,#39407,#39408,#39409,#39410,#39411,#39412),
 .UNSPECIFIED.,.F.,.F.,(4,3,3,3,3,3,3,3,4),(120.490566047324,120.713819590196,
121.711454462842,122.709089335488,123.706724208135,124.704359080781,125.701993953427,
126.699628826073,126.773751354504),.UNSPECIFIED.);
#6172=B_SPLINE_CURVE_WITH_KNOTS('',3,(#39417,#39418,#39419,#39420,#39421,
#39422,#39423,#39424,#39425,#39426,#39427,#39428,#39429,#39430,#39431,#39432,
#39433,#39434,#39435,#39436,#39437,#39438),.UNSPECIFIED.,.F.,.F.,(4,3,3,
3,3,3,3,4),(-136.039640490966,-135.67834267989,-134.680707807243,-133.683072934597,
-132.685438061951,-131.687803189305,-130.690168316658,-129.756455183786),
 .UNSPECIFIED.);
#6173=B_SPLINE_CURVE_WITH_KNOTS('',3,(#39439,#39440,#39441,#39442,#39443,
#39444,#39445,#39446,#39447,#39448,#39449,#39450,#39451,#39452,#39453,#39454,
#39455,#39456,#39457,#39458,#39459,#39460),.UNSPECIFIED.,.F.,.F.,(4,3,3,
3,3,3,3,4),(126.773751354504,127.69726369872,128.694898571366,129.692533444012,
130.690168316658,131.687803189305,132.685438061951,133.056936661683),
 .UNSPECIFIED.);
#6174=B_SPLINE_CURVE_WITH_KNOTS('',3,(#39465,#39466,#39467,#39468,#39469,
#39470,#39471,#39472,#39473,#39474,#39475,#39476,#39477,#39478,#39479,#39480,
#39481,#39482,#39483,#39484,#39485,#39486),.UNSPECIFIED.,.F.,.F.,(4,3,3,
3,3,3,3,4),(-142.322825798145,-141.664151915767,-140.666517043121,-139.668882170475,
-138.671247297828,-137.673612425182,-136.675977552536,-136.039640490966),
 .UNSPECIFIED.);
#6175=B_SPLINE_CURVE_WITH_KNOTS('',3,(#39487,#39488,#39489,#39490,#39491,
#39492,#39493,#39494,#39495,#39496,#39497,#39498,#39499,#39500,#39501,#39502,
#39503,#39504,#39505,#39506,#39507,#39508),.UNSPECIFIED.,.F.,.F.,(4,3,3,
3,3,3,3,4),(133.056936661683,133.683072934597,134.680707807244,135.67834267989,
136.675977552536,137.673612425182,138.671247297829,139.340121968863),
 .UNSPECIFIED.);
#6176=B_SPLINE_CURVE_WITH_KNOTS('',3,(#39513,#39514,#39515,#39516,#39517,
#39518,#39519,#39520,#39521,#39522,#39523,#39524,#39525,#39526,#39527,#39528,
#39529,#39530,#39531,#39532,#39533,#39534),.UNSPECIFIED.,.F.,.F.,(4,3,3,
3,3,3,3,4),(-148.606011105325,-147.649961151645,-146.652326278998,-145.654691406352,
-144.657056533706,-143.65942166106,-142.661786788413,-142.322825798145),
 .UNSPECIFIED.);
#6177=B_SPLINE_CURVE_WITH_KNOTS('',3,(#39535,#39536,#39537,#39538,#39539,
#39540,#39541,#39542,#39543,#39544,#39545,#39546,#39547,#39548,#39549,#39550,
#39551,#39552,#39553,#39554,#39555,#39556),.UNSPECIFIED.,.F.,.F.,(4,3,3,
3,3,3,3,4),(139.340121968863,139.668882170475,140.666517043121,141.664151915767,
142.661786788413,143.65942166106,144.657056533706,145.623307276042),
 .UNSPECIFIED.);
#6178=B_SPLINE_CURVE_WITH_KNOTS('',3,(#39561,#39562,#39563,#39564,#39565,
#39566,#39567,#39568,#39569,#39570,#39571,#39572,#39573,#39574,#39575,#39576,
#39577,#39578,#39579,#39580,#39581,#39582,#39583,#39584,#39585),
 .UNSPECIFIED.,.F.,.F.,(4,3,3,3,3,3,3,3,4),(-154.889196412504,-154.633405260168,
-153.635770387522,-152.638135514876,-151.64050064223,-150.642865769583,
-149.645230896937,-148.647596024291,-148.606011105325),.UNSPECIFIED.);
#6179=B_SPLINE_CURVE_WITH_KNOTS('',3,(#39586,#39587,#39588,#39589,#39590,
#39591,#39592,#39593,#39594,#39595,#39596,#39597,#39598,#39599,#39600,#39601,
#39602,#39603,#39604,#39605,#39606,#39607,#39608,#39609,#39610),
 .UNSPECIFIED.,.F.,.F.,(4,3,3,3,3,3,3,3,4),(145.623307276042,145.654691406352,
146.652326278998,147.649961151645,148.647596024291,149.645230896937,150.642865769583,
151.64050064223,151.906492583222),.UNSPECIFIED.);
#6180=B_SPLINE_CURVE_WITH_KNOTS('',3,(#39615,#39616,#39617,#39618,#39619,
#39620,#39621,#39622,#39623,#39624,#39625,#39626,#39627,#39628,#39629,#39630,
#39631,#39632,#39633,#39634,#39635,#39636),.UNSPECIFIED.,.F.,.F.,(4,3,3,
3,3,3,3,4),(-161.172381719684,-160.619214496046,-159.6215796234,-158.623944750753,
-157.626309878107,-156.628675005461,-155.631040132815,-154.889196412504),
 .UNSPECIFIED.);
#6181=B_SPLINE_CURVE_WITH_KNOTS('',3,(#39637,#39638,#39639,#39640,#39641,
#39642,#39643,#39644,#39645,#39646,#39647,#39648,#39649,#39650,#39651,#39652,
#39653,#39654,#39655,#39656,#39657,#39658),.UNSPECIFIED.,.F.,.F.,(4,3,3,
3,3,3,3,4),(151.906492583222,152.638135514876,153.635770387522,154.633405260168,
155.631040132815,156.628675005461,157.626309878107,158.189677890402),
 .UNSPECIFIED.);
#6182=B_SPLINE_CURVE_WITH_KNOTS('',3,(#39663,#39664,#39665,#39666,#39667,
#39668,#39669,#39670,#39671,#39672,#39673,#39674,#39675,#39676,#39677,#39678,
#39679,#39680,#39681,#39682,#39683,#39684),.UNSPECIFIED.,.F.,.F.,(4,3,3,
3,3,3,3,4),(-167.455567026863,-166.605023731923,-165.607388859277,-164.609753986631,
-163.612119113985,-162.614484241338,-161.616849368692,-161.172381719684),
 .UNSPECIFIED.);
#6183=B_SPLINE_CURVE_WITH_KNOTS('',3,(#39685,#39686,#39687,#39688,#39689,
#39690,#39691,#39692,#39693,#39694,#39695,#39696,#39697,#39698,#39699,#39700,
#39701,#39702,#39703,#39704,#39705,#39706),.UNSPECIFIED.,.F.,.F.,(4,3,3,
3,3,3,3,4),(158.189677890402,158.623944750753,159.6215796234,160.619214496046,
161.616849368692,162.614484241338,163.612119113985,164.472863197581),
 .UNSPECIFIED.);
#6184=B_SPLINE_CURVE_WITH_KNOTS('',3,(#39711,#39712,#39713,#39714,#39715,
#39716,#39717,#39718,#39719,#39720,#39721,#39722,#39723,#39724,#39725,#39726,
#39727,#39728,#39729,#39730,#39731,#39732,#39733,#39734,#39735),
 .UNSPECIFIED.,.F.,.F.,(4,3,3,3,3,3,3,3,4),(-173.738752334043,-173.588467840447,
-172.590832967801,-171.593198095155,-170.595563222508,-169.597928349862,
-168.600293477216,-167.60265860457,-167.455567026863),.UNSPECIFIED.);
#6185=B_SPLINE_CURVE_WITH_KNOTS('',3,(#39736,#39737,#39738,#39739,#39740,
#39741,#39742,#39743,#39744,#39745,#39746,#39747,#39748,#39749,#39750,#39751,
#39752,#39753,#39754,#39755,#39756,#39757,#39758,#39759,#39760),
 .UNSPECIFIED.,.F.,.F.,(4,3,3,3,3,3,3,3,4),(164.472863197581,164.609753986631,
165.607388859277,166.605023731923,167.60265860457,168.600293477216,169.597928349862,
170.595563222508,170.756048504761),.UNSPECIFIED.);
#6186=B_SPLINE_CURVE_WITH_KNOTS('',3,(#39765,#39766,#39767,#39768,#39769,
#39770,#39771,#39772,#39773,#39774,#39775,#39776,#39777,#39778,#39779,#39780,
#39781,#39782,#39783,#39784,#39785,#39786),.UNSPECIFIED.,.F.,.F.,(4,3,3,
3,3,3,3,4),(-180.021937641223,-179.574277076325,-178.576642203678,-177.579007331032,
-176.581372458386,-175.58373758574,-174.586102713093,-173.738752334043),
 .UNSPECIFIED.);
#6187=B_SPLINE_CURVE_WITH_KNOTS('',3,(#39787,#39788,#39789,#39790,#39791,
#39792,#39793,#39794,#39795,#39796,#39797,#39798,#39799,#39800,#39801,#39802,
#39803,#39804,#39805,#39806,#39807,#39808),.UNSPECIFIED.,.F.,.F.,(4,3,3,
3,3,3,3,4),(170.756048504761,171.593198095155,172.590832967801,173.588467840447,
174.586102713093,175.58373758574,176.581372458386,177.03923381194),
 .UNSPECIFIED.);
#6188=B_SPLINE_CURVE_WITH_KNOTS('',3,(#39813,#39814,#39815,#39816,#39817,
#39818,#39819,#39820,#39821,#39822,#39823,#39824,#39825,#39826,#39827,#39828,
#39829,#39830,#39831,#39832,#39833,#39834),.UNSPECIFIED.,.F.,.F.,(4,3,3,
3,3,3,3,4),(-186.305122948402,-185.560086312202,-184.562451439556,-183.56481656691,
-182.567181694263,-181.569546821617,-180.571911948971,-180.021937641223),
 .UNSPECIFIED.);
#6189=B_SPLINE_CURVE_WITH_KNOTS('',3,(#39835,#39836,#39837,#39838,#39839,
#39840,#39841,#39842,#39843,#39844,#39845,#39846,#39847,#39848,#39849,#39850,
#39851,#39852,#39853,#39854,#39855,#39856),.UNSPECIFIED.,.F.,.F.,(4,3,3,
3,3,3,3,4),(177.03923381194,177.579007331032,178.576642203678,179.574277076325,
180.571911948971,181.569546821617,182.567181694263,183.32241911912),
 .UNSPECIFIED.);
#6190=B_SPLINE_CURVE_WITH_KNOTS('',3,(#39861,#39862,#39863,#39864,#39865,
#39866,#39867,#39868,#39869,#39870,#39871,#39872,#39873,#39874,#39875,#39876,
#39877,#39878,#39879,#39880,#39881,#39882,#39883,#39884,#39885),
 .UNSPECIFIED.,.F.,.F.,(4,3,3,3,3,3,3,3,4),(-192.588308255582,-192.543530420726,
-191.545895548079,-190.548260675433,-189.550625802787,-188.552990930141,
-187.555356057495,-186.557721184848,-186.305122948402),.UNSPECIFIED.);
#6191=B_SPLINE_CURVE_WITH_KNOTS('',3,(#39886,#39887,#39888,#39889,#39890,
#39891,#39892,#39893,#39894,#39895,#39896,#39897,#39898,#39899,#39900,#39901,
#39902,#39903,#39904,#39905,#39906,#39907,#39908,#39909,#39910),
 .UNSPECIFIED.,.F.,.F.,(4,3,3,3,3,3,3,3,4),(183.32241911912,183.56481656691,
184.562451439556,185.560086312202,186.557721184848,187.555356057495,188.552990930141,
189.550625802787,189.605604426299),.UNSPECIFIED.);
#6192=B_SPLINE_CURVE_WITH_KNOTS('',3,(#39915,#39916,#39917,#39918,#39919,
#39920,#39921,#39922,#39923,#39924,#39925,#39926,#39927,#39928,#39929,#39930,
#39931,#39932,#39933,#39934,#39935,#39936),.UNSPECIFIED.,.F.,.F.,(4,3,3,
3,3,3,3,4),(-198.871493562761,-198.529339656603,-197.531704783957,-196.534069911311,
-195.536435038664,-194.538800166018,-193.541165293372,-192.588308255582),
 .UNSPECIFIED.);
#6193=B_SPLINE_CURVE_WITH_KNOTS('',3,(#39937,#39938,#39939,#39940,#39941,
#39942,#39943,#39944,#39945,#39946,#39947,#39948,#39949,#39950,#39951,#39952,
#39953,#39954,#39955,#39956,#39957,#39958),.UNSPECIFIED.,.F.,.F.,(4,3,3,
3,3,3,3,4),(189.605604426299,190.548260675433,191.54589554808,192.543530420726,
193.541165293372,194.538800166018,195.536435038665,195.888789733479),
 .UNSPECIFIED.);
#6194=B_SPLINE_CURVE_WITH_KNOTS('',3,(#39963,#39964,#39965,#39966,#39967,
#39968,#39969,#39970,#39971,#39972,#39973,#39974,#39975,#39976,#39977,#39978,
#39979,#39980,#39981,#39982,#39983,#39984),.UNSPECIFIED.,.F.,.F.,(4,3,3,
3,3,3,3,4),(-205.154678869941,-204.515148892481,-203.517514019834,-202.519879147188,
-201.522244274542,-200.524609401896,-199.526974529249,-198.871493562761),
 .UNSPECIFIED.);
#6195=B_SPLINE_CURVE_WITH_KNOTS('',3,(#39985,#39986,#39987,#39988,#39989,
#39990,#39991,#39992,#39993,#39994,#39995,#39996,#39997,#39998,#39999,#40000,
#40001,#40002,#40003,#40004,#40005,#40006),.UNSPECIFIED.,.F.,.F.,(4,3,3,
3,3,3,3,4),(195.888789733479,196.534069911311,197.531704783957,198.529339656603,
199.52697452925,200.524609401896,201.522244274542,202.171975040659),
 .UNSPECIFIED.);
#6196=B_SPLINE_CURVE_WITH_KNOTS('',3,(#40011,#40012,#40013,#40014,#40015,
#40016,#40017,#40018,#40019,#40020,#40021,#40022,#40023,#40024,#40025,#40026,
#40027,#40028,#40029,#40030,#40031,#40032),.UNSPECIFIED.,.F.,.F.,(4,3,3,
3,3,3,3,4),(-211.43786417712,-210.500958128358,-209.503323255712,-208.505688383066,
-207.50805351042,-206.510418637773,-205.512783765127,-205.154678869941),
 .UNSPECIFIED.);
#6197=B_SPLINE_CURVE_WITH_KNOTS('',3,(#40033,#40034,#40035,#40036,#40037,
#40038,#40039,#40040,#40041,#40042,#40043,#40044,#40045,#40046,#40047,#40048,
#40049,#40050,#40051,#40052,#40053,#40054),.UNSPECIFIED.,.F.,.F.,(4,3,3,
3,3,3,3,4),(202.171975040659,202.519879147188,203.517514019835,204.515148892481,
205.512783765127,206.510418637773,207.50805351042,208.455160347838),
 .UNSPECIFIED.);
#6198=B_SPLINE_CURVE_WITH_KNOTS('',3,(#40059,#40060,#40061,#40062,#40063,
#40064,#40065,#40066,#40067,#40068,#40069,#40070,#40071,#40072,#40073,#40074,
#40075,#40076,#40077,#40078,#40079,#40080,#40081,#40082,#40083),
 .UNSPECIFIED.,.F.,.F.,(4,3,3,3,3,3,3,3,4),(-217.7210494843,-217.484402236882,
-216.486767364236,-215.489132491589,-214.491497618943,-213.493862746297,
-212.496227873651,-211.498593001004,-211.43786417712),.UNSPECIFIED.);
#6199=B_SPLINE_CURVE_WITH_KNOTS('',3,(#40084,#40085,#40086,#40087,#40088,
#40089,#40090,#40091,#40092,#40093,#40094,#40095,#40096,#40097,#40098,#40099,
#40100,#40101,#40102,#40103,#40104,#40105,#40106,#40107,#40108),
 .UNSPECIFIED.,.F.,.F.,(4,3,3,3,3,3,3,3,4),(208.455160347838,208.505688383066,
209.503323255712,210.500958128358,211.498593001005,212.496227873651,213.493862746297,
214.491497618943,214.738345655018),.UNSPECIFIED.);
#6200=B_SPLINE_CURVE_WITH_KNOTS('',3,(#40113,#40114,#40115,#40116,#40117,
#40118,#40119,#40120,#40121,#40122,#40123,#40124,#40125,#40126,#40127,#40128,
#40129,#40130,#40131,#40132,#40133,#40134),.UNSPECIFIED.,.F.,.F.,(4,3,3,
3,3,3,3,4),(-224.00423479148,-223.470211472759,-222.472576600113,-221.474941727467,
-220.477306854821,-219.479671982174,-218.482037109528,-217.7210494843),
 .UNSPECIFIED.);
#6201=B_SPLINE_CURVE_WITH_KNOTS('',3,(#40135,#40136,#40137,#40138,#40139,
#40140,#40141,#40142,#40143,#40144,#40145,#40146,#40147,#40148,#40149,#40150,
#40151,#40152,#40153,#40154,#40155,#40156),.UNSPECIFIED.,.F.,.F.,(4,3,3,
3,3,3,3,4),(214.738345655018,215.48913249159,216.486767364236,217.484402236882,
218.482037109528,219.479671982175,220.477306854821,221.021530962197),
 .UNSPECIFIED.);
#6202=B_SPLINE_CURVE_WITH_KNOTS('',3,(#40161,#40162,#40163,#40164,#40165,
#40166,#40167,#40168,#40169,#40170,#40171,#40172,#40173,#40174,#40175,#40176,
#40177,#40178,#40179,#40180,#40181,#40182),.UNSPECIFIED.,.F.,.F.,(4,3,3,
3,3,3,3,4),(-230.287420098659,-229.456020708637,-228.458385835991,-227.460750963344,
-226.463116090698,-225.465481218052,-224.467846345406,-224.00423479148),
 .UNSPECIFIED.);
#6203=B_SPLINE_CURVE_WITH_KNOTS('',3,(#40183,#40184,#40185,#40186,#40187,
#40188,#40189,#40190,#40191,#40192,#40193,#40194,#40195,#40196,#40197,#40198,
#40199,#40200,#40201,#40202,#40203,#40204),.UNSPECIFIED.,.F.,.F.,(4,3,3,
3,3,3,3,4),(221.021530962197,221.474941727467,222.472576600113,223.47021147276,
224.467846345406,225.465481218052,226.463116090698,227.304716269377),
 .UNSPECIFIED.);
#6204=B_SPLINE_CURVE_WITH_KNOTS('',3,(#40209,#40210,#40211,#40212,#40213,
#40214,#40215,#40216,#40217,#40218,#40219,#40220,#40221,#40222,#40223,#40224,
#40225,#40226,#40227,#40228,#40229,#40230,#40231,#40232,#40233),
 .UNSPECIFIED.,.F.,.F.,(4,3,3,3,3,3,3,3,4),(-236.570605405839,-236.439464817161,
-235.441829944514,-234.444195071868,-233.446560199222,-232.448925326576,
-231.451290453929,-230.453655581283,-230.287420098659),.UNSPECIFIED.);
#6205=B_SPLINE_CURVE_WITH_KNOTS('',3,(#40234,#40235,#40236,#40237,#40238,
#40239,#40240,#40241,#40242,#40243,#40244,#40245,#40246,#40247,#40248,#40249,
#40250,#40251,#40252,#40253,#40254,#40255,#40256,#40257,#40258),
 .UNSPECIFIED.,.F.,.F.,(4,3,3,3,3,3,3,3,4),(227.304716269377,227.460750963345,
228.458385835991,229.456020708637,230.453655581283,231.451290453929,232.448925326576,
233.446560199222,233.587901576556),.UNSPECIFIED.);
#6206=B_SPLINE_CURVE_WITH_KNOTS('',3,(#40263,#40264,#40265,#40266,#40267,
#40268,#40269,#40270,#40271,#40272,#40273,#40274,#40275,#40276,#40277,#40278,
#40279,#40280,#40281,#40282,#40283,#40284),.UNSPECIFIED.,.F.,.F.,(4,3,3,
3,3,3,3,4),(-242.853790713018,-242.425274053038,-241.427639180392,-240.430004307746,
-239.432369435099,-238.434734562453,-237.437099689807,-236.570605405839),
 .UNSPECIFIED.);
#6207=B_SPLINE_CURVE_WITH_KNOTS('',3,(#40285,#40286,#40287,#40288,#40289,
#40290,#40291,#40292,#40293,#40294,#40295,#40296,#40297,#40298,#40299,#40300,
#40301,#40302,#40303,#40304,#40305,#40306),.UNSPECIFIED.,.F.,.F.,(4,3,3,
3,3,3,3,4),(233.587901576556,234.444195071868,235.441829944515,236.439464817161,
237.437099689807,238.434734562453,239.432369435099,239.871086883736),
 .UNSPECIFIED.);
#6208=B_SPLINE_CURVE_WITH_KNOTS('',3,(#40311,#40312,#40313,#40314,#40315,
#40316,#40317,#40318,#40319,#40320,#40321,#40322,#40323,#40324,#40325,#40326,
#40327,#40328,#40329,#40330,#40331,#40332),.UNSPECIFIED.,.F.,.F.,(4,3,3,
3,3,3,3,4),(-249.136976020198,-248.411083288916,-247.413448416269,-246.415813543623,
-245.418178670977,-244.420543798331,-243.422908925684,-242.853790713018),
 .UNSPECIFIED.);
#6209=B_SPLINE_CURVE_WITH_KNOTS('',3,(#40333,#40334,#40335,#40336,#40337,
#40338,#40339,#40340,#40341,#40342,#40343,#40344,#40345,#40346,#40347,#40348,
#40349,#40350,#40351,#40352,#40353,#40354),.UNSPECIFIED.,.F.,.F.,(4,3,3,
3,3,3,3,4),(239.871086883736,240.430004307746,241.427639180392,242.425274053038,
243.422908925684,244.420543798331,245.418178670977,246.154272190915),
 .UNSPECIFIED.);
#6210=B_SPLINE_CURVE_WITH_KNOTS('',3,(#40359,#40360,#40361,#40362,#40363,
#40364,#40365,#40366,#40367,#40368,#40369,#40370,#40371,#40372,#40373,#40374,
#40375,#40376,#40377,#40378,#40379,#40380,#40381,#40382,#40383),
 .UNSPECIFIED.,.F.,.F.,(4,3,3,3,3,3,3,3,4),(-255.420161327377,-255.394527397439,
-254.396892524793,-253.399257652147,-252.401622779501,-251.403987906854,
-250.406353034208,-249.408718161562,-249.136976020198),.UNSPECIFIED.);
#6211=B_SPLINE_CURVE_WITH_KNOTS('',3,(#40384,#40385,#40386,#40387,#40388,
#40389,#40390,#40391,#40392,#40393,#40394,#40395,#40396,#40397,#40398,#40399,
#40400,#40401,#40402,#40403,#40404,#40405,#40406,#40407,#40408),
 .UNSPECIFIED.,.F.,.F.,(4,3,3,3,3,3,3,3,4),(246.154272190915,246.415813543623,
247.41344841627,248.411083288916,249.408718161562,250.406353034208,251.403987906854,
252.401622779501,252.437457498095),.UNSPECIFIED.);
#6212=B_SPLINE_CURVE_WITH_KNOTS('',3,(#40413,#40414,#40415,#40416,#40417,
#40418,#40419,#40420,#40421,#40422,#40423,#40424,#40425,#40426,#40427,#40428,
#40429,#40430,#40431,#40432,#40433,#40434),.UNSPECIFIED.,.F.,.F.,(4,3,3,
3,3,3,3,4),(-261.703346634557,-261.380336633317,-260.382701760671,-259.385066888024,
-258.387432015378,-257.389797142732,-256.392162270086,-255.420161327377),
 .UNSPECIFIED.);
#6213=B_SPLINE_CURVE_WITH_KNOTS('',3,(#40435,#40436,#40437,#40438,#40439,
#40440,#40441,#40442,#40443,#40444,#40445,#40446,#40447,#40448,#40449,#40450,
#40451,#40452,#40453,#40454,#40455,#40456),.UNSPECIFIED.,.F.,.F.,(4,3,3,
3,3,3,3,4),(252.437457498095,253.399257652147,254.396892524793,255.394527397439,
256.392162270086,257.389797142732,258.387432015378,258.720642805275),
 .UNSPECIFIED.);
#6214=B_SPLINE_CURVE_WITH_KNOTS('',3,(#40461,#40462,#40463,#40464,#40465,
#40466,#40467,#40468,#40469,#40470,#40471,#40472,#40473,#40474,#40475,#40476,
#40477,#40478,#40479,#40480,#40481,#40482),.UNSPECIFIED.,.F.,.F.,(4,3,3,
3,3,3,3,4),(-267.986531941737,-267.366145869194,-266.368510996548,-265.370876123902,
-264.373241251256,-263.375606378609,-262.377971505963,-261.703346634557),
 .UNSPECIFIED.);
#6215=B_SPLINE_CURVE_WITH_KNOTS('',3,(#40483,#40484,#40485,#40486,#40487,
#40488,#40489,#40490,#40491,#40492,#40493,#40494,#40495,#40496,#40497,#40498,
#40499,#40500,#40501,#40502,#40503,#40504),.UNSPECIFIED.,.F.,.F.,(4,3,3,
3,3,3,3,4),(258.720642805275,259.385066888024,260.382701760671,261.380336633317,
262.377971505963,263.375606378609,264.373241251256,265.003828112454),
 .UNSPECIFIED.);
#6216=B_SPLINE_CURVE_WITH_KNOTS('',3,(#40509,#40510,#40511,#40512,#40513,
#40514,#40515,#40516,#40517,#40518,#40519,#40520,#40521,#40522,#40523,#40524,
#40525,#40526,#40527,#40528,#40529,#40530),.UNSPECIFIED.,.F.,.F.,(4,3,3,
3,3,3,3,4),(-274.269717248916,-273.351955105072,-272.354320232426,-271.356685359779,
-270.359050487133,-269.361415614487,-268.363780741841,-267.986531941737),
 .UNSPECIFIED.);
#6217=B_SPLINE_CURVE_WITH_KNOTS('',3,(#40531,#40532,#40533,#40534,#40535,
#40536,#40537,#40538,#40539,#40540,#40541,#40542,#40543,#40544,#40545,#40546,
#40547,#40548,#40549,#40550,#40551,#40552),.UNSPECIFIED.,.F.,.F.,(4,3,3,
3,3,3,3,4),(265.003828112454,265.370876123902,266.368510996548,267.366145869194,
268.363780741841,269.361415614487,270.359050487133,271.287013419634),
 .UNSPECIFIED.);
#6218=B_SPLINE_CURVE_WITH_KNOTS('',3,(#40558,#40559,#40560,#40561),
 .UNSPECIFIED.,.F.,.F.,(4,4),(285.884931476671,285.89887235325),
 .UNSPECIFIED.);
#6219=B_SPLINE_CURVE_WITH_KNOTS('',3,(#40567,#40568,#40569,#40570,#40571,
#40572,#40573,#40574,#40575,#40576),.UNSPECIFIED.,.F.,.F.,(4,1,1,1,1,1,
1,4),(279.601746169491,279.978994969596,280.976629842242,281.974264714888,
282.971899587534,283.969534460181,284.967169332827,285.884931476671),
 .UNSPECIFIED.);
#6220=B_SPLINE_CURVE_WITH_KNOTS('',3,(#40579,#40580,#40581,#40582,#40583,
#40584,#40585,#40586,#40587),.UNSPECIFIED.,.F.,.F.,(4,1,1,1,1,1,4),(279.601746169492,
279.671418109638,280.669052982284,281.66668785493,282.664322727577,283.661957600223,
284.659592472869),.UNSPECIFIED.);
#6221=B_SPLINE_CURVE_WITH_KNOTS('',3,(#40592,#40593,#40594,#40595,#40596,
#40597,#40598,#40599,#40600,#40601),.UNSPECIFIED.,.F.,.F.,(4,1,1,1,1,1,
1,4),(273.318560862312,273.993185733718,274.990820606364,275.988455479011,
276.986090351657,277.983725224303,278.981360096949,279.601746169491),
 .UNSPECIFIED.);
#6222=B_SPLINE_CURVE_WITH_KNOTS('',3,(#40602,#40603,#40604,#40605,#40606,
#40607,#40608,#40609,#40610,#40611),.UNSPECIFIED.,.F.,.F.,(4,1,1,1,1,1,
1,4),(273.318560862312,273.68560887376,274.683243746407,275.680878619053,
276.678513491699,277.676148364345,278.673783236992,279.601746169492),
 .UNSPECIFIED.);
#6223=B_SPLINE_CURVE_WITH_KNOTS('',3,(#40616,#40617,#40618,#40619,#40620,
#40621,#40622,#40623,#40624,#40625),.UNSPECIFIED.,.F.,.F.,(4,1,1,1,1,1,
1,4),(267.035375555132,268.007376497841,269.005011370487,270.002646243133,
271.000281115779,271.997915988426,272.995550861072,273.318560862312),
 .UNSPECIFIED.);
#6224=B_SPLINE_CURVE_WITH_KNOTS('',3,(#40626,#40627,#40628,#40629,#40630,
#40631,#40632,#40633,#40634,#40635),.UNSPECIFIED.,.F.,.F.,(4,1,1,1,1,1,
1,4),(267.035375555132,267.699799637883,268.697434510529,269.695069383175,
270.692704255822,271.690339128468,272.687974001114,273.318560862312),
 .UNSPECIFIED.);
#6225=B_SPLINE_CURVE_WITH_KNOTS('',3,(#40640,#40641,#40642,#40643,#40644,
#40645,#40646,#40647,#40648,#40649,#40650),.UNSPECIFIED.,.F.,.F.,(4,1,1,
1,1,1,1,1,4),(260.752190247953,261.023932389317,262.021567261963,263.019202134609,
264.016837007256,265.014471879902,266.012106752548,267.009741625194,267.035375555132),
 .UNSPECIFIED.);
#6226=B_SPLINE_CURVE_WITH_KNOTS('',3,(#40651,#40652,#40653,#40654,#40655,
#40656,#40657,#40658,#40659,#40660),.UNSPECIFIED.,.F.,.F.,(4,1,1,1,1,1,
1,4),(260.752190247953,261.713990402005,262.711625274652,263.709260147298,
264.706895019944,265.70452989259,266.702164765237,267.035375555132),
 .UNSPECIFIED.);
#6227=B_SPLINE_CURVE_WITH_KNOTS('',3,(#40665,#40666,#40667,#40668,#40669,
#40670,#40671,#40672,#40673,#40674),.UNSPECIFIED.,.F.,.F.,(4,1,1,1,1,1,
1,4),(254.469004940773,255.038123153439,256.035758026086,257.033392898732,
258.031027771378,259.028662644024,260.026297516671,260.752190247953),
 .UNSPECIFIED.);
#6228=B_SPLINE_CURVE_WITH_KNOTS('',3,(#40675,#40676,#40677,#40678,#40679,
#40680,#40681,#40682,#40683,#40684,#40685),.UNSPECIFIED.,.F.,.F.,(4,1,1,
1,1,1,1,1,4),(254.469004940773,254.730546293482,255.728181166128,256.725816038774,
257.72345091142,258.721085784067,259.718720656713,260.716355529359,260.752190247953),
 .UNSPECIFIED.);
#6229=B_SPLINE_CURVE_WITH_KNOTS('',3,(#40690,#40691,#40692,#40693,#40694,
#40695,#40696,#40697,#40698,#40699),.UNSPECIFIED.,.F.,.F.,(4,1,1,1,1,1,
1,4),(248.185819633594,249.052313917562,250.049948790208,251.047583662854,
252.045218535501,253.042853408147,254.040488280793,254.469004940773),
 .UNSPECIFIED.);
#6230=B_SPLINE_CURVE_WITH_KNOTS('',3,(#40700,#40701,#40702,#40703,#40704,
#40705,#40706,#40707,#40708,#40709),.UNSPECIFIED.,.F.,.F.,(4,1,1,1,1,1,
1,4),(248.185819633594,248.744737057604,249.74237193025,250.740006802897,
251.737641675543,252.735276548189,253.732911420835,254.469004940773),
 .UNSPECIFIED.);
#6231=B_SPLINE_CURVE_WITH_KNOTS('',3,(#40714,#40715,#40716,#40717,#40718,
#40719,#40720,#40721,#40722,#40723,#40724),.UNSPECIFIED.,.F.,.F.,(4,1,1,
1,1,1,1,1,4),(241.902634326414,242.068869809038,243.066504681685,244.064139554331,
245.061774426977,246.059409299623,247.05704417227,248.054679044916,248.185819633594),
 .UNSPECIFIED.);
#6232=B_SPLINE_CURVE_WITH_KNOTS('',3,(#40725,#40726,#40727,#40728,#40729,
#40730,#40731,#40732,#40733,#40734),.UNSPECIFIED.,.F.,.F.,(4,1,1,1,1,1,
1,4),(241.902634326414,242.758927821727,243.756562694373,244.754197567019,
245.751832439665,246.749467312312,247.747102184958,248.185819633594),
 .UNSPECIFIED.);
#6233=B_SPLINE_CURVE_WITH_KNOTS('',3,(#40739,#40740,#40741,#40742,#40743,
#40744,#40745,#40746,#40747,#40748),.UNSPECIFIED.,.F.,.F.,(4,1,1,1,1,1,
1,4),(235.619449019234,236.083060573161,237.080695445807,238.078330318453,
239.0759651911,240.073600063746,241.071234936392,241.902634326414),
 .UNSPECIFIED.);
#6234=B_SPLINE_CURVE_WITH_KNOTS('',3,(#40749,#40750,#40751,#40752,#40753,
#40754,#40755,#40756,#40757,#40758,#40759),.UNSPECIFIED.,.F.,.F.,(4,1,1,
1,1,1,1,1,4),(235.619449019235,235.775483713203,236.773118585849,237.770753458495,
238.768388331142,239.766023203788,240.763658076434,241.76129294908,241.902634326414),
 .UNSPECIFIED.);
#6235=B_SPLINE_CURVE_WITH_KNOTS('',3,(#40764,#40765,#40766,#40767,#40768,
#40769,#40770,#40771,#40772,#40773),.UNSPECIFIED.,.F.,.F.,(4,1,1,1,1,1,
1,4),(229.336263712055,230.097251337283,231.09488620993,232.092521082576,
233.090155955222,234.087790827868,235.085425700515,235.619449019234),
 .UNSPECIFIED.);
#6236=B_SPLINE_CURVE_WITH_KNOTS('',3,(#40774,#40775,#40776,#40777,#40778,
#40779,#40780,#40781,#40782,#40783),.UNSPECIFIED.,.F.,.F.,(4,1,1,1,1,1,
1,4),(229.336263712055,229.789674477325,230.787309349972,231.784944222618,
232.782579095264,233.78021396791,234.777848840557,235.619449019235),
 .UNSPECIFIED.);
#6237=B_SPLINE_CURVE_WITH_KNOTS('',3,(#40788,#40789,#40790,#40791,#40792,
#40793,#40794,#40795,#40796,#40797,#40798),.UNSPECIFIED.,.F.,.F.,(4,1,1,
1,1,1,1,1,4),(223.053078404875,223.11380722876,224.111442101406,225.109076974052,
226.106711846698,227.104346719345,228.101981591991,229.099616464637,229.336263712055),
 .UNSPECIFIED.);
#6238=B_SPLINE_CURVE_WITH_KNOTS('',3,(#40799,#40800,#40801,#40802,#40803,
#40804,#40805,#40806,#40807,#40808),.UNSPECIFIED.,.F.,.F.,(4,1,1,1,1,1,
1,4),(223.053078404876,223.803865241448,224.801500114094,225.79913498674,
226.796769859387,227.794404732033,228.792039604679,229.336263712055),
 .UNSPECIFIED.);
#6239=B_SPLINE_CURVE_WITH_KNOTS('',3,(#40813,#40814,#40815,#40816,#40817,
#40818,#40819,#40820,#40821,#40822),.UNSPECIFIED.,.F.,.F.,(4,1,1,1,1,1,
1,4),(216.769893097696,217.127997992882,218.125632865528,219.123267738175,
220.120902610821,221.118537483467,222.116172356113,223.053078404875),
 .UNSPECIFIED.);
#6240=B_SPLINE_CURVE_WITH_KNOTS('',3,(#40823,#40824,#40825,#40826,#40827,
#40828,#40829,#40830,#40831,#40832,#40833),.UNSPECIFIED.,.F.,.F.,(4,1,1,
1,1,1,1,1,4),(216.769893097696,216.820421132924,217.81805600557,218.815690878217,
219.813325750863,220.810960623509,221.808595496155,222.806230368802,223.053078404876),
 .UNSPECIFIED.);
#6241=B_SPLINE_CURVE_WITH_KNOTS('',3,(#40838,#40839,#40840,#40841,#40842,
#40843,#40844,#40845,#40846,#40847),.UNSPECIFIED.,.F.,.F.,(4,1,1,1,1,1,
1,4),(210.486707790516,211.142188757005,212.139823629651,213.137458502297,
214.135093374943,215.13272824759,216.130363120236,216.769893097696),
 .UNSPECIFIED.);
#6242=B_SPLINE_CURVE_WITH_KNOTS('',3,(#40848,#40849,#40850,#40851,#40852,
#40853,#40854,#40855,#40856,#40857),.UNSPECIFIED.,.F.,.F.,(4,1,1,1,1,1,
1,4),(210.486707790516,210.834611897047,211.832246769693,212.829881642339,
213.827516514985,214.825151387632,215.822786260278,216.769893097696),
 .UNSPECIFIED.);
#6243=B_SPLINE_CURVE_WITH_KNOTS('',3,(#40862,#40863,#40864,#40865,#40866,
#40867,#40868,#40869,#40870,#40871),.UNSPECIFIED.,.F.,.F.,(4,1,1,1,1,1,
1,4),(204.203522483337,205.156379521127,206.154014393773,207.15164926642,
208.149284139066,209.146919011712,210.144553884358,210.486707790516),
 .UNSPECIFIED.);
#6244=B_SPLINE_CURVE_WITH_KNOTS('',3,(#40872,#40873,#40874,#40875,#40876,
#40877,#40878,#40879,#40880,#40881),.UNSPECIFIED.,.F.,.F.,(4,1,1,1,1,1,
1,4),(204.203522483337,204.848802661169,205.846437533815,206.844072406462,
207.841707279108,208.839342151754,209.8369770244,210.486707790516),
 .UNSPECIFIED.);
#6245=B_SPLINE_CURVE_WITH_KNOTS('',3,(#40886,#40887,#40888,#40889,#40890,
#40891,#40892,#40893,#40894,#40895,#40896),.UNSPECIFIED.,.F.,.F.,(4,1,1,
1,1,1,1,1,4),(197.920337176157,198.172935412603,199.17057028525,200.168205157896,
201.165840030542,202.163474903188,203.161109775835,204.158744648481,204.203522483337),
 .UNSPECIFIED.);
#6246=B_SPLINE_CURVE_WITH_KNOTS('',3,(#40897,#40898,#40899,#40900,#40901,
#40902,#40903,#40904,#40905,#40906),.UNSPECIFIED.,.F.,.F.,(4,1,1,1,1,1,
1,4),(197.920337176157,198.862993425292,199.860628297938,200.858263170584,
201.85589804323,202.853532915877,203.851167788523,204.203522483337),
 .UNSPECIFIED.);
#6247=B_SPLINE_CURVE_WITH_KNOTS('',3,(#40911,#40912,#40913,#40914,#40915,
#40916,#40917,#40918,#40919,#40920),.UNSPECIFIED.,.F.,.F.,(4,1,1,1,1,1,
1,4),(191.637151868978,192.187126176726,193.184761049372,194.182395922018,
195.180030794665,196.177665667311,197.175300539957,197.920337176157),
 .UNSPECIFIED.);
#6248=B_SPLINE_CURVE_WITH_KNOTS('',3,(#40921,#40922,#40923,#40924,#40925,
#40926,#40927,#40928,#40929,#40930,#40931),.UNSPECIFIED.,.F.,.F.,(4,1,1,
1,1,1,1,1,4),(191.637151868978,191.879549316768,192.877184189414,193.87481906206,
194.872453934707,195.870088807353,196.867723679999,197.865358552645,197.920337176157),
 .UNSPECIFIED.);
#6249=B_SPLINE_CURVE_WITH_KNOTS('',3,(#40936,#40937,#40938,#40939,#40940,
#40941,#40942,#40943,#40944,#40945),.UNSPECIFIED.,.F.,.F.,(4,1,1,1,1,1,
1,4),(185.353966561798,186.201316940848,187.198951813495,188.196586686141,
189.194221558787,190.191856431433,191.18949130408,191.637151868978),
 .UNSPECIFIED.);
#6250=B_SPLINE_CURVE_WITH_KNOTS('',3,(#40946,#40947,#40948,#40949,#40950,
#40951,#40952,#40953,#40954,#40955),.UNSPECIFIED.,.F.,.F.,(4,1,1,1,1,1,
1,4),(185.353966561798,185.89374008089,186.891374953537,187.889009826183,
188.886644698829,189.884279571475,190.881914444122,191.637151868978),
 .UNSPECIFIED.);
#6251=B_SPLINE_CURVE_WITH_KNOTS('',3,(#40960,#40961,#40962,#40963,#40964,
#40965,#40966,#40967,#40968,#40969,#40970),.UNSPECIFIED.,.F.,.F.,(4,1,1,
1,1,1,1,1,4),(179.070781254618,179.217872832325,180.215507704971,181.213142577617,
182.210777450263,183.20841232291,184.206047195556,185.203682068202,185.353966561798),
 .UNSPECIFIED.);
#6252=B_SPLINE_CURVE_WITH_KNOTS('',3,(#40971,#40972,#40973,#40974,#40975,
#40976,#40977,#40978,#40979,#40980),.UNSPECIFIED.,.F.,.F.,(4,1,1,1,1,1,
1,4),(179.070781254619,179.907930845013,180.905565717659,181.903200590305,
182.900835462952,183.898470335598,184.896105208244,185.353966561798),
 .UNSPECIFIED.);
#6253=B_SPLINE_CURVE_WITH_KNOTS('',3,(#40985,#40986,#40987,#40988,#40989,
#40990,#40991,#40992,#40993,#40994),.UNSPECIFIED.,.F.,.F.,(4,1,1,1,1,1,
1,4),(172.787595947439,173.232063596447,174.229698469093,175.22733334174,
176.224968214386,177.222603087032,178.220237959678,179.070781254618),
 .UNSPECIFIED.);
#6254=B_SPLINE_CURVE_WITH_KNOTS('',3,(#40995,#40996,#40997,#40998,#40999,
#41000,#41001,#41002,#41003,#41004,#41005),.UNSPECIFIED.,.F.,.F.,(4,1,1,
1,1,1,1,1,4),(172.787595947439,172.924486736489,173.922121609136,174.919756481782,
175.917391354428,176.915026227074,177.912661099721,178.910295972367,179.070781254619),
 .UNSPECIFIED.);
#6255=B_SPLINE_CURVE_WITH_KNOTS('',3,(#41010,#41011,#41012,#41013,#41014,
#41015,#41016,#41017,#41018,#41019),.UNSPECIFIED.,.F.,.F.,(4,1,1,1,1,1,
1,4),(166.504410640259,167.24625436057,168.243889233216,169.241524105862,
170.239158978508,171.236793851155,172.234428723801,172.787595947439),
 .UNSPECIFIED.);
#6256=B_SPLINE_CURVE_WITH_KNOTS('',3,(#41020,#41021,#41022,#41023,#41024,
#41025,#41026,#41027,#41028,#41029),.UNSPECIFIED.,.F.,.F.,(4,1,1,1,1,1,
1,4),(166.504410640259,166.938677500612,167.936312373258,168.933947245904,
169.931582118551,170.929216991197,171.926851863843,172.787595947439),
 .UNSPECIFIED.);
#6257=B_SPLINE_CURVE_WITH_KNOTS('',3,(#41034,#41035,#41036,#41037,#41038,
#41039,#41040,#41041,#41042,#41043,#41044),.UNSPECIFIED.,.F.,.F.,(4,1,1,
1,1,1,1,1,4),(160.22122533308,160.262810252046,161.260445124692,162.258079997338,
163.255714869985,164.253349742631,165.250984615277,166.248619487923,166.504410640259),
 .UNSPECIFIED.);
#6258=B_SPLINE_CURVE_WITH_KNOTS('',3,(#41045,#41046,#41047,#41048,#41049,
#41050,#41051,#41052,#41053,#41054),.UNSPECIFIED.,.F.,.F.,(4,1,1,1,1,1,
1,4),(160.22122533308,160.952868264734,161.950503137381,162.948138010027,
163.945772882673,164.943407755319,165.941042627966,166.504410640259),
 .UNSPECIFIED.);
#6259=B_SPLINE_CURVE_WITH_KNOTS('',3,(#41059,#41060,#41061,#41062,#41063,
#41064,#41065,#41066,#41067,#41068),.UNSPECIFIED.,.F.,.F.,(4,1,1,1,1,1,
1,4),(153.9380400259,154.277001016168,155.274635888815,156.272270761461,
157.269905634107,158.267540506754,159.2651753794,160.22122533308),
 .UNSPECIFIED.);
#6260=B_SPLINE_CURVE_WITH_KNOTS('',3,(#41069,#41070,#41071,#41072,#41073,
#41074,#41075,#41076,#41077,#41078,#41079),.UNSPECIFIED.,.F.,.F.,(4,1,1,
1,1,1,1,1,4),(153.9380400259,153.969424156211,154.967059028857,155.964693901503,
156.962328774149,157.959963646796,158.957598519442,159.955233392088,160.22122533308),
 .UNSPECIFIED.);
#6261=B_SPLINE_CURVE_WITH_KNOTS('',3,(#41084,#41085,#41086,#41087,#41088,
#41089,#41090,#41091,#41092,#41093),.UNSPECIFIED.,.F.,.F.,(4,1,1,1,1,1,
1,4),(147.654854718721,148.291191780291,149.288826652937,150.286461525584,
151.28409639823,152.281731270876,153.279366143522,153.9380400259),
 .UNSPECIFIED.);
#6262=B_SPLINE_CURVE_WITH_KNOTS('',3,(#41094,#41095,#41096,#41097,#41098,
#41099,#41100,#41101,#41102,#41103),.UNSPECIFIED.,.F.,.F.,(4,1,1,1,1,1,
1,4),(147.654854718721,147.983614920333,148.981249792979,149.978884665626,
150.976519538272,151.974154410918,152.971789283564,153.9380400259),
 .UNSPECIFIED.);
#6263=B_SPLINE_CURVE_WITH_KNOTS('',3,(#41108,#41109,#41110,#41111,#41112,
#41113,#41114,#41115,#41116,#41117),.UNSPECIFIED.,.F.,.F.,(4,1,1,1,1,1,
1,4),(141.371669411541,142.305382544414,143.30301741706,144.300652289706,
145.298287162352,146.295922034999,147.293556907645,147.654854718721),
 .UNSPECIFIED.);
#6264=B_SPLINE_CURVE_WITH_KNOTS('',3,(#41118,#41119,#41120,#41121,#41122,
#41123,#41124,#41125,#41126,#41127),.UNSPECIFIED.,.F.,.F.,(4,1,1,1,1,1,
1,4),(141.371669411541,141.997805684456,142.995440557102,143.993075429748,
144.990710302394,145.988345175041,146.985980047687,147.654854718721),
 .UNSPECIFIED.);
#6265=B_SPLINE_CURVE_WITH_KNOTS('',3,(#41132,#41133,#41134,#41135,#41136,
#41137,#41138,#41139,#41140,#41141,#41142),.UNSPECIFIED.,.F.,.F.,(4,1,1,
1,1,1,1,1,4),(135.088484104361,135.32193843589,136.319573308536,137.317208181182,
138.314843053829,139.312477926475,140.310112799121,141.307747671767,141.371669411541),
 .UNSPECIFIED.);
#6266=B_SPLINE_CURVE_WITH_KNOTS('',3,(#41143,#41144,#41145,#41146,#41147,
#41148,#41149,#41150,#41151,#41152),.UNSPECIFIED.,.F.,.F.,(4,1,1,1,1,1,
1,4),(135.088484104362,136.011996448578,137.009631321224,138.007266193871,
139.004901066517,140.002535939163,141.000170811809,141.371669411541),
 .UNSPECIFIED.);
#6267=B_SPLINE_CURVE_WITH_KNOTS('',3,(#41157,#41158,#41159,#41160,#41161,
#41162,#41163,#41164,#41165,#41166),.UNSPECIFIED.,.F.,.F.,(4,1,1,1,1,1,
1,4),(128.805298797182,129.336129200012,130.333764072659,131.331398945305,
132.329033817951,133.326668690597,134.324303563244,135.088484104361),
 .UNSPECIFIED.);
#6268=B_SPLINE_CURVE_WITH_KNOTS('',3,(#41167,#41168,#41169,#41170,#41171,
#41172,#41173,#41174,#41175,#41176,#41177),.UNSPECIFIED.,.F.,.F.,(4,1,1,
1,1,1,1,1,4),(128.805298797182,129.028552340054,130.026187212701,131.023822085347,
132.021456957993,133.019091830639,134.016726703286,135.014361575932,135.088484104362),
 .UNSPECIFIED.);
#6269=B_SPLINE_CURVE_WITH_KNOTS('',3,(#41182,#41183,#41184,#41185,#41186,
#41187,#41188,#41189,#41190,#41191),.UNSPECIFIED.,.F.,.F.,(4,1,1,1,1,1,
1,4),(122.522113490002,123.350319964135,124.347954836781,125.345589709427,
126.343224582074,127.34085945472,128.338494327366,128.805298797182),
 .UNSPECIFIED.);
#6270=B_SPLINE_CURVE_WITH_KNOTS('',3,(#41192,#41193,#41194,#41195,#41196,
#41197,#41198,#41199,#41200,#41201),.UNSPECIFIED.,.F.,.F.,(4,1,1,1,1,1,
1,4),(122.522113490002,123.042743104177,124.040377976823,125.038012849469,
126.035647722116,127.033282594762,128.030917467408,128.805298797182),
 .UNSPECIFIED.);
#6271=B_SPLINE_CURVE_WITH_KNOTS('',3,(#41206,#41207,#41208,#41209,#41210,
#41211,#41212,#41213,#41214,#41215,#41216),.UNSPECIFIED.,.F.,.F.,(4,1,1,
1,1,1,1,1,4),(116.238928182823,116.366875855611,117.364510728257,118.362145600904,
119.35978047355,120.357415346196,121.355050218842,122.352685091489,122.522113490002),
 .UNSPECIFIED.);
#6272=B_SPLINE_CURVE_WITH_KNOTS('',3,(#41217,#41218,#41219,#41220,#41221,
#41222,#41223,#41224,#41225,#41226),.UNSPECIFIED.,.F.,.F.,(4,1,1,1,1,1,
1,4),(116.238928182823,117.056933868299,118.054568740946,119.052203613592,
120.049838486238,121.047473358884,122.045108231531,122.522113490002),
 .UNSPECIFIED.);
#6273=B_SPLINE_CURVE_WITH_KNOTS('',3,(#41231,#41232,#41233,#41234,#41235,
#41236,#41237,#41238,#41239,#41240),.UNSPECIFIED.,.F.,.F.,(4,1,1,1,1,1,
1,4),(109.955742875643,110.381066619734,111.37870149238,112.376336365026,
113.373971237672,114.371606110319,115.369240982965,116.238928182823),
 .UNSPECIFIED.);
#6274=B_SPLINE_CURVE_WITH_KNOTS('',3,(#41241,#41242,#41243,#41244,#41245,
#41246,#41247,#41248,#41249,#41250,#41251),.UNSPECIFIED.,.F.,.F.,(4,1,1,
1,1,1,1,1,4),(109.955742875643,110.073489759776,111.071124632422,112.068759505068,
113.066394377714,114.064029250361,115.061664123007,116.059298995653,116.238928182823),
 .UNSPECIFIED.);
#6275=B_SPLINE_CURVE_WITH_KNOTS('',3,(#41256,#41257,#41258,#41259,#41260,
#41261,#41262,#41263,#41264,#41265),.UNSPECIFIED.,.F.,.F.,(4,1,1,1,1,1,
1,4),(103.672557568464,104.395257383856,105.392892256502,106.390527129149,
107.388162001795,108.385796874441,109.383431747087,109.955742875643),
 .UNSPECIFIED.);
#6276=B_SPLINE_CURVE_WITH_KNOTS('',3,(#41266,#41267,#41268,#41269,#41270,
#41271,#41272,#41273,#41274,#41275),.UNSPECIFIED.,.F.,.F.,(4,1,1,1,1,1,
1,4),(103.672557568464,104.087680523898,105.085315396544,106.082950269191,
107.080585141837,108.078220014483,109.075854887129,109.955742875643),
 .UNSPECIFIED.);
#6277=B_SPLINE_CURVE_WITH_KNOTS('',3,(#41280,#41281,#41282,#41283,#41284,
#41285,#41286,#41287,#41288,#41289,#41290),.UNSPECIFIED.,.F.,.F.,(4,1,1,
1,1,1,1,1,4),(97.389372261284,97.4118132753324,98.4094481479786,99.4070830206249,
100.404717893271,101.402352765917,102.399987638564,103.39762251121,103.672557568464),
 .UNSPECIFIED.);
#6278=B_SPLINE_CURVE_WITH_KNOTS('',3,(#41291,#41292,#41293,#41294,#41295,
#41296,#41297,#41298,#41299,#41300),.UNSPECIFIED.,.F.,.F.,(4,1,1,1,1,1,
1,4),(97.3893722612841,98.1018712880207,99.0995061606669,100.097141033313,
101.094775905959,102.092410778606,103.090045651252,103.672557568464),
 .UNSPECIFIED.);
#6279=B_SPLINE_CURVE_WITH_KNOTS('',3,(#41305,#41306,#41307,#41308,#41309,
#41310,#41311,#41312,#41313,#41314),.UNSPECIFIED.,.F.,.F.,(4,1,1,1,1,1,
1,4),(91.1061869541044,91.4260040394549,92.4236389121012,93.4212737847474,
94.4189086573937,95.4165435300399,96.4141784026861,97.389372261284),
 .UNSPECIFIED.);
#6280=B_SPLINE_CURVE_WITH_KNOTS('',3,(#41315,#41316,#41317,#41318,#41319,
#41320,#41321,#41322,#41323,#41324,#41325),.UNSPECIFIED.,.F.,.F.,(4,1,1,
1,1,1,1,1,4),(91.1061869541045,91.1184271794969,92.1160620521432,93.1136969247894,
94.1113317974357,95.1089666700819,96.1066015427282,97.1042364153744,97.3893722612841),
 .UNSPECIFIED.);
#6281=B_SPLINE_CURVE_WITH_KNOTS('',3,(#41330,#41331,#41332,#41333,#41334,
#41335,#41336,#41337,#41338,#41339),.UNSPECIFIED.,.F.,.F.,(4,1,1,1,1,1,
1,4),(84.8230016469248,85.4401948035774,86.4378296762237,87.4354645488699,
88.4330994215162,89.4307342941624,90.4283691668087,91.1061869541044),
 .UNSPECIFIED.);
#6282=B_SPLINE_CURVE_WITH_KNOTS('',3,(#41340,#41341,#41342,#41343,#41344,
#41345,#41346,#41347,#41348,#41349),.UNSPECIFIED.,.F.,.F.,(4,1,1,1,1,1,
1,4),(84.8230016469249,85.1326179436194,86.1302528162657,87.1278876889119,
88.1255225615582,89.1231574342044,90.1207923068507,91.1061869541045),
 .UNSPECIFIED.);
#6283=B_SPLINE_CURVE_WITH_KNOTS('',3,(#41354,#41355,#41356,#41357,#41358,
#41359,#41360,#41361,#41362,#41363),.UNSPECIFIED.,.F.,.F.,(4,1,1,1,1,1,
1,4),(78.5398163397452,79.4543855676999,80.4520204403462,81.4496553129924,
82.4472901856387,83.4449250582849,84.4425599309312,84.8230016469248),
 .UNSPECIFIED.);
#6284=B_SPLINE_CURVE_WITH_KNOTS('',3,(#41364,#41365,#41366,#41367,#41368,
#41369,#41370,#41371,#41372,#41373),.UNSPECIFIED.,.F.,.F.,(4,1,1,1,1,1,
1,4),(78.5398163397453,79.146808707742,80.1444435803882,81.1420784530345,
82.1397133256807,83.1373481983269,84.1349830709732,84.8230016469249),
 .UNSPECIFIED.);
#6285=B_SPLINE_CURVE_WITH_KNOTS('',3,(#41378,#41379,#41380,#41381,#41382,
#41383,#41384,#41385,#41386,#41387,#41388),.UNSPECIFIED.,.F.,.F.,(4,1,1,
1,1,1,1,1,4),(72.2566310325656,72.4709414591762,73.4685763318225,74.4662112044687,
75.463846077115,76.4614809497612,77.4591158224074,78.4567506950537,78.5398163397452),
 .UNSPECIFIED.);
#6286=B_SPLINE_CURVE_WITH_KNOTS('',3,(#41389,#41390,#41391,#41392,#41393,
#41394,#41395,#41396,#41397,#41398),.UNSPECIFIED.,.F.,.F.,(4,1,1,1,1,1,
1,4),(72.2566310325657,73.1609994718645,74.1586343445107,75.156269217157,
76.1539040898032,77.1515389624495,78.1491738350957,78.5398163397453),
 .UNSPECIFIED.);
#6287=B_SPLINE_CURVE_WITH_KNOTS('',3,(#41403,#41404,#41405,#41406,#41407,
#41408,#41409,#41410,#41411,#41412),.UNSPECIFIED.,.F.,.F.,(4,1,1,1,1,1,
1,4),(65.973445725386,66.4851322232987,67.482767095945,68.4804019685912,
69.4780368412375,70.4756717138837,71.47330658653,72.2566310325656),
 .UNSPECIFIED.);
#6288=B_SPLINE_CURVE_WITH_KNOTS('',3,(#41413,#41414,#41415,#41416,#41417,
#41418,#41419,#41420,#41421,#41422,#41423),.UNSPECIFIED.,.F.,.F.,(4,1,1,
1,1,1,1,1,4),(65.9734457253861,66.1775553633407,67.175190235987,68.1728251086332,
69.1704599812795,70.1680948539257,71.165729726572,72.1633645992182,72.2566310325657),
 .UNSPECIFIED.);
#6289=B_SPLINE_CURVE_WITH_KNOTS('',3,(#41428,#41429,#41430,#41431,#41432,
#41433,#41434,#41435,#41436,#41437),.UNSPECIFIED.,.F.,.F.,(4,1,1,1,1,1,
1,4),(59.6902604182064,60.4993229874212,61.4969578600675,62.4945927327137,
63.49222760536,64.4898624780062,65.4874973506525,65.973445725386),
 .UNSPECIFIED.);
#6290=B_SPLINE_CURVE_WITH_KNOTS('',3,(#41438,#41439,#41440,#41441,#41442,
#41443,#41444,#41445,#41446,#41447),.UNSPECIFIED.,.F.,.F.,(4,1,1,1,1,1,
1,4),(59.6902604182065,60.1917461274632,61.1893810001095,62.1870158727557,
63.184650745402,64.1822856180482,65.1799204906945,65.9734457253861),
 .UNSPECIFIED.);
#6291=B_SPLINE_CURVE_WITH_KNOTS('',3,(#41452,#41453,#41454,#41455,#41456,
#41457,#41458,#41459,#41460,#41461,#41462),.UNSPECIFIED.,.F.,.F.,(4,1,1,
1,1,1,1,1,4),(53.4070751110268,53.5158788788975,54.5135137515438,55.51114862419,
56.5087834968363,57.5064183694825,58.5040532421287,59.501688114775,59.6902604182064),
 .UNSPECIFIED.);
#6292=B_SPLINE_CURVE_WITH_KNOTS('',3,(#41463,#41464,#41465,#41466,#41467,
#41468,#41469,#41470,#41471,#41472),.UNSPECIFIED.,.F.,.F.,(4,1,1,1,1,1,
1,4),(53.4070751110269,54.2059368915858,55.203571764232,56.2012066368783,
57.1988415095245,58.1964763821708,59.194111254817,59.6902604182065),
 .UNSPECIFIED.);
#6293=B_SPLINE_CURVE_WITH_KNOTS('',3,(#41477,#41478,#41479,#41480,#41481,
#41482,#41483,#41484,#41485,#41486),.UNSPECIFIED.,.F.,.F.,(4,1,1,1,1,1,
1,4),(47.1238898038472,47.53006964302,48.5277045156663,49.5253393883125,
50.5229742609588,51.520609133605,52.5182440062513,53.4070751110268),
 .UNSPECIFIED.);
#6294=B_SPLINE_CURVE_WITH_KNOTS('',3,(#41487,#41488,#41489,#41490,#41491,
#41492,#41493,#41494,#41495,#41496,#41497),.UNSPECIFIED.,.F.,.F.,(4,1,1,
1,1,1,1,1,4),(47.1238898038473,47.222492783062,48.2201276557083,49.2177625283545,
50.2153974010008,51.213032273647,52.2106671462933,53.2083020189395,53.4070751110269),
 .UNSPECIFIED.);
#6295=B_SPLINE_CURVE_WITH_KNOTS('',3,(#41502,#41503,#41504,#41505,#41506,
#41507,#41508,#41509,#41510,#41511),.UNSPECIFIED.,.F.,.F.,(4,1,1,1,1,1,
1,4),(40.8407044966676,41.5442604071425,42.5418952797888,43.539530152435,
44.5371650250813,45.5347998977275,46.5324347703738,47.1238898038472),
 .UNSPECIFIED.);
#6296=B_SPLINE_CURVE_WITH_KNOTS('',3,(#41512,#41513,#41514,#41515,#41516,
#41517,#41518,#41519,#41520,#41521),.UNSPECIFIED.,.F.,.F.,(4,1,1,1,1,1,
1,4),(40.8407044966677,41.2366835471845,42.2343184198308,43.231953292477,
44.2295881651233,45.2272230377695,46.2248579104158,47.1238898038473),
 .UNSPECIFIED.);
#6297=B_SPLINE_CURVE_WITH_KNOTS('',3,(#41526,#41527,#41528,#41529,#41530,
#41531,#41532,#41533,#41534,#41535,#41536),.UNSPECIFIED.,.F.,.F.,(4,1,1,
1,1,1,1,1,4),(34.557519189488,34.5608162986188,35.5584511712651,36.5560860439113,
37.5537209165576,38.5513557892038,39.54899066185,40.5466255344963,40.8407044966676),
 .UNSPECIFIED.);
#6298=B_SPLINE_CURVE_WITH_KNOTS('',3,(#41537,#41538,#41539,#41540,#41541,
#41542,#41543,#41544,#41545,#41546),.UNSPECIFIED.,.F.,.F.,(4,1,1,1,1,1,
1,4),(34.5575191894882,35.2508743113071,36.2485091839533,37.2461440565995,
38.2437789292458,39.241413801892,40.2390486745383,40.8407044966677),
 .UNSPECIFIED.);
#6299=B_SPLINE_CURVE_WITH_KNOTS('',3,(#41551,#41552,#41553,#41554,#41555,
#41556,#41557,#41558,#41559,#41560),.UNSPECIFIED.,.F.,.F.,(4,1,1,1,1,1,
1,4),(28.2743338823084,28.5750070627413,29.5726419353876,30.5702768080338,
31.5679116806801,32.5655465533263,33.5631814259726,34.557519189488),
 .UNSPECIFIED.);
#6300=B_SPLINE_CURVE_WITH_KNOTS('',3,(#41561,#41562,#41563,#41564,#41565,
#41566,#41567,#41568,#41569,#41570),.UNSPECIFIED.,.F.,.F.,(4,1,1,1,1,1,
1,4),(28.2743338823086,29.2650650754296,30.2626999480758,31.2603348207221,
32.2579696933683,33.2556045660146,34.2532394386608,34.5575191894882),
 .UNSPECIFIED.);
#6301=B_SPLINE_CURVE_WITH_KNOTS('',3,(#41575,#41576,#41577,#41578,#41579,
#41580,#41581,#41582,#41583,#41584),.UNSPECIFIED.,.F.,.F.,(4,1,1,1,1,1,
1,4),(21.9911485751289,22.5891978268638,23.5868326995101,24.5844675721563,
25.5821024448026,26.5797373174488,27.5773721900951,28.2743338823084),
 .UNSPECIFIED.);
#6302=B_SPLINE_CURVE_WITH_KNOTS('',3,(#41585,#41586,#41587,#41588,#41589,
#41590,#41591,#41592,#41593,#41594,#41595),.UNSPECIFIED.,.F.,.F.,(4,1,1,
1,1,1,1,1,4),(21.991148575129,22.2816209669058,23.2792558395521,24.2768907121983,
25.2745255848446,26.2721604574908,27.2697953301371,28.2674302027833,28.2743338823086),
 .UNSPECIFIED.);
#6303=B_SPLINE_CURVE_WITH_KNOTS('',3,(#41600,#41601,#41602,#41603,#41604,
#41605,#41606,#41607,#41608,#41609),.UNSPECIFIED.,.F.,.F.,(4,1,1,1,1,1,
1,4),(15.7079632679493,16.6033885909864,17.6010234636326,18.5986583362789,
19.5962932089251,20.5939280815713,21.5915629542176,21.9911485751289),
 .UNSPECIFIED.);
#6304=B_SPLINE_CURVE_WITH_KNOTS('',3,(#41610,#41611,#41612,#41613,#41614,
#41615,#41616,#41617,#41618,#41619),.UNSPECIFIED.,.F.,.F.,(4,1,1,1,1,1,
1,4),(15.7079632679494,16.2958117310283,17.2934466036746,18.2910814763208,
19.2887163489671,20.2863512216133,21.2839860942596,21.991148575129),
 .UNSPECIFIED.);
#6305=B_SPLINE_CURVE_WITH_KNOTS('',3,(#42741,#42742,#42743,#42744,#42745,
#42746,#42747,#42748,#42749,#42750,#42751,#42752,#42753,#42754,#42755,#42756,
#42757,#42758,#42759,#42760,#42761,#42762,#42763,#42764,#42765,#42766,#42767,
#42768,#42769,#42770,#42771,#42772,#42773,#42774,#42775,#42776,#42777,#42778,
#42779,#42780,#42781,#42782,#42783,#42784,#42785,#42786,#42787,#42788,#42789,
#42790,#42791,#42792,#42793,#42794,#42795,#42796,#42797,#42798,#42799,#42800,
#42801,#42802,#42803,#42804,#42805,#42806,#42807,#42808,#42809,#42810,#42811,
#42812,#42813,#42814,#42815,#42816,#42817,#42818,#42819,#42820,#42821,#42822,
#42823,#42824,#42825,#42826,#42827,#42828,#42829,#42830,#42831,#42832,#42833,
#42834,#42835,#42836,#42837),.UNSPECIFIED.,.F.,.F.,(4,3,3,3,3,3,3,3,3,3,
3,3,3,3,3,3,3,3,3,3,3,3,3,3,3,3,3,3,3,3,3,3,4),(-0.741270768406308,-0.715387510784636,
-0.678846032931345,-0.657738243517773,-0.643316797175534,-0.635862900512505,
-0.599020213237717,-0.566782861872277,-0.552679020649897,-0.544234280993646,
-0.537662343230828,-0.502261333851186,-0.467119578216044,-0.433015993298668,
-0.41004234555255,-0.398746749984718,-0.393744789683524,-0.360135524847538,
-0.341121402314197,-0.306853456049999,-0.272440609283236,-0.261693001887453,
-0.257007819058798,-0.223577420294793,-0.190116876212526,-0.157068650315129,
-0.137435069025738,-0.130957629949228,-0.124458872839733,-0.0922450955809254,
-0.0604778109814689,-0.0296903572576096,0.),.UNSPECIFIED.);
#6306=B_SPLINE_CURVE_WITH_KNOTS('',3,(#42838,#42839,#42840,#42841,#42842,
#42843,#42844,#42845,#42846,#42847,#42848,#42849,#42850),.UNSPECIFIED.,
 .F.,.F.,(4,3,3,3,4),(271.287013419634,271.356685359779,272.354320232426,
273.351955105072,274.283658125495),.UNSPECIFIED.);
#6307=B_SPLINE_CURVE_WITH_KNOTS('',3,(#42852,#42853,#42854,#42855,#42856,
#42857,#42858,#42859,#42860,#42861,#42862,#42863,#42864,#42865,#42866,#42867,
#42868,#42869,#42870,#42871,#42872,#42873,#42874,#42875,#42876,#42877,#42878,
#42879,#42880,#42881,#42882,#42883,#42884,#42885,#42886,#42887,#42888,#42889,
#42890,#42891,#42892,#42893,#42894,#42895,#42896,#42897,#42898,#42899,#42900,
#42901,#42902,#42903,#42904,#42905,#42906,#42907,#42908,#42909,#42910,#42911,
#42912,#42913,#42914,#42915,#42916,#42917,#42918,#42919,#42920,#42921,#42922,
#42923,#42924,#42925,#42926,#42927,#42928,#42929,#42930,#42931,#42932,#42933,
#42934,#42935,#42936,#42937,#42938,#42939,#42940,#42941,#42942,#42943,#42944,
#42945,#42946,#42947,#42948,#42949,#42950,#42951),.UNSPECIFIED.,.F.,.F.,
(4,3,3,3,3,3,3,3,3,3,3,3,3,3,3,3,3,3,3,3,3,3,3,3,3,3,3,3,3,3,3,3,3,4),(-0.744397949170561,
-0.722857348546835,-0.691759636347062,-0.672173659622073,-0.659729697581051,
-0.653647223896304,-0.621623974301131,-0.591218978606893,-0.57779191421541,
-0.572099067158539,-0.566376890083838,-0.532985059609366,-0.499081457463265,
-0.465285106585306,-0.443559832125787,-0.437180479628824,-0.432790863135699,
-0.397876458807638,-0.378384008747229,-0.344662910041584,-0.31030331663291,
-0.299192426024121,-0.292592230277462,-0.2581831131989,-0.222669619455726,
-0.186825819848632,-0.163472592367553,-0.155670996352624,-0.150810522246808,
-0.145703618645708,-0.108961989561893,-0.0721598384238253,-0.0360557370617284,
0.),.UNSPECIFIED.);
#6308=B_SPLINE_CURVE_WITH_KNOTS('',3,(#42952,#42953,#42954,#42955,#42956,
#42957,#42958,#42959,#42960),.UNSPECIFIED.,.F.,.F.,(4,1,1,1,1,1,4),(10.3759343473742,
11.3076373677971,12.3052722404433,13.3029071130896,14.3005419857358,15.2981768583821,
15.7079632679494),.UNSPECIFIED.);
#6309=B_SPLINE_CURVE_WITH_KNOTS('',3,(#42966,#42967,#42968,#42969,#42970,
#42971,#42972,#42973,#42974,#42975,#42976,#42977,#42978,#42979,#42980,#42981,
#42982,#42983,#42984,#42985,#42986,#42987,#42988,#42989,#42990,#42991,#42992,
#42993,#42994,#42995,#42996,#42997,#42998,#42999,#43000,#43001,#43002,#43003,
#43004,#43005,#43006,#43007,#43008,#43009,#43010,#43011,#43012,#43013,#43014,
#43015,#43016,#43017,#43018,#43019,#43020,#43021,#43022,#43023,#43024,#43025,
#43026,#43027,#43028,#43029,#43030,#43031,#43032,#43033,#43034,#43035,#43036,
#43037,#43038,#43039,#43040,#43041,#43042,#43043,#43044,#43045,#43046,#43047,
#43048,#43049,#43050,#43051,#43052,#43053,#43054,#43055,#43056,#43057,#43058,
#43059,#43060,#43061,#43062),.UNSPECIFIED.,.F.,.F.,(4,3,3,3,3,3,3,3,3,3,
3,3,3,3,3,3,3,3,3,3,3,3,3,3,3,3,3,3,3,3,3,3,4),(-0.741270768406415,-0.715387510784742,
-0.678846032311912,-0.657738242937057,-0.643316795555802,-0.635862898961111,
-0.599020211880251,-0.566782860684498,-0.552679019536357,-0.544234276107367,
-0.537662341481398,-0.502261331512692,-0.46711957209537,-0.433015977083203,
-0.41004233339096,-0.398746728953922,-0.39374478606441,-0.360135513608645,
-0.341121402314231,-0.306853450668917,-0.272440605048863,-0.261692995236242,
-0.257007812571432,-0.223577410634224,-0.190116869812972,-0.157068653419064,
-0.137435071741681,-0.13095764083796,-0.124458872072335,-0.0922451026976537,
-0.0604778299681871,-0.029690391740758,0.),.UNSPECIFIED.);
#6310=B_SPLINE_CURVE_WITH_KNOTS('',3,(#43065,#43066,#43067,#43068,#43069,
#43070,#43071,#43072),.UNSPECIFIED.,.F.,.F.,(4,1,1,1,1,4),(11.6152142277551,
12.6128491004014,13.6104839730476,14.6081188456939,15.6057537183401,15.7079632679493),
 .UNSPECIFIED.);
#6311=B_SPLINE_CURVE_WITH_KNOTS('',3,(#44194,#44195,#44196,#44197,#44198,
#44199,#44200,#44201,#44202,#44203,#44204,#44205,#44206,#44207,#44208,#44209,
#44210,#44211,#44212,#44213,#44214,#44215,#44216,#44217,#44218,#44219,#44220,
#44221,#44222,#44223,#44224,#44225,#44226,#44227,#44228,#44229,#44230,#44231,
#44232,#44233,#44234,#44235,#44236,#44237,#44238,#44239,#44240,#44241,#44242,
#44243,#44244,#44245,#44246,#44247,#44248,#44249,#44250,#44251,#44252,#44253,
#44254,#44255,#44256,#44257,#44258,#44259,#44260,#44261,#44262,#44263,#44264,
#44265,#44266,#44267,#44268,#44269,#44270,#44271,#44272,#44273,#44274,#44275,
#44276,#44277,#44278,#44279,#44280,#44281,#44282,#44283,#44284,#44285,#44286,
#44287,#44288,#44289,#44290,#44291,#44292,#44293),.UNSPECIFIED.,.F.,.F.,
(4,3,3,3,3,3,3,3,3,3,3,3,3,3,3,3,3,3,3,3,3,3,3,3,3,3,3,3,3,3,3,3,3,4),(-0.744397949170713,
-0.722857348547031,-0.691759626910421,-0.672173650775227,-0.659729685964857,
-0.653647221772012,-0.621623964078995,-0.591218969662536,-0.577791899653599,
-0.57209901896209,-0.566376879451804,-0.532985044276137,-0.499081441064884,
-0.465285090294045,-0.443559819907365,-0.437180447783716,-0.432790799375827,
-0.39787639550394,-0.378384008747325,-0.344662906100098,-0.310303308027255,
-0.299192413474635,-0.29259223086673,-0.25818311008637,-0.222669611795312,
-0.186825810288309,-0.163472584002271,-0.155670981000362,-0.150810518391116,
-0.145703618285079,-0.108961986661821,-0.072159837380098,-0.0360557472806876,
0.),.UNSPECIFIED.);
#6312=B_SPLINE_CURVE_WITH_KNOTS('',3,(#44294,#44295,#44296,#44297,#44298,
#44299,#44300,#44301,#44302,#44303),.UNSPECIFIED.,.F.,.F.,(4,3,3,4),(-276.344859723011,
-275.347224850364,-274.349589977718,-274.269717248916),.UNSPECIFIED.);
#7663=VERTEX_POINT('',#38394);
#7664=VERTEX_POINT('',#38395);
#7665=VERTEX_POINT('',#38397);
#7666=VERTEX_POINT('',#38408);
#7667=VERTEX_POINT('',#38418);
#7668=VERTEX_POINT('',#38419);
#7669=VERTEX_POINT('',#38466);
#7670=VERTEX_POINT('',#38467);
#7671=VERTEX_POINT('',#38514);
#7672=VERTEX_POINT('',#38515);
#7673=VERTEX_POINT('',#38565);
#7674=VERTEX_POINT('',#38566);
#7675=VERTEX_POINT('',#38616);
#7676=VERTEX_POINT('',#38617);
#7677=VERTEX_POINT('',#38664);
#7678=VERTEX_POINT('',#38665);
#7679=VERTEX_POINT('',#38712);
#7680=VERTEX_POINT('',#38713);
#7681=VERTEX_POINT('',#38766);
#7682=VERTEX_POINT('',#38767);
#7683=VERTEX_POINT('',#38814);
#7684=VERTEX_POINT('',#38815);
#7685=VERTEX_POINT('',#38862);
#7686=VERTEX_POINT('',#38863);
#7687=VERTEX_POINT('',#38916);
#7688=VERTEX_POINT('',#38917);
#7689=VERTEX_POINT('',#38964);
#7690=VERTEX_POINT('',#38965);
#7691=VERTEX_POINT('',#39012);
#7692=VERTEX_POINT('',#39013);
#7693=VERTEX_POINT('',#39060);
#7694=VERTEX_POINT('',#39061);
#7695=VERTEX_POINT('',#39114);
#7696=VERTEX_POINT('',#39115);
#7697=VERTEX_POINT('',#39162);
#7698=VERTEX_POINT('',#39163);
#7699=VERTEX_POINT('',#39210);
#7700=VERTEX_POINT('',#39211);
#7701=VERTEX_POINT('',#39264);
#7702=VERTEX_POINT('',#39265);
#7703=VERTEX_POINT('',#39312);
#7704=VERTEX_POINT('',#39313);
#7705=VERTEX_POINT('',#39360);
#7706=VERTEX_POINT('',#39361);
#7707=VERTEX_POINT('',#39414);
#7708=VERTEX_POINT('',#39415);
#7709=VERTEX_POINT('',#39462);
#7710=VERTEX_POINT('',#39463);
#7711=VERTEX_POINT('',#39510);
#7712=VERTEX_POINT('',#39511);
#7713=VERTEX_POINT('',#39558);
#7714=VERTEX_POINT('',#39559);
#7715=VERTEX_POINT('',#39612);
#7716=VERTEX_POINT('',#39613);
#7717=VERTEX_POINT('',#39660);
#7718=VERTEX_POINT('',#39661);
#7719=VERTEX_POINT('',#39708);
#7720=VERTEX_POINT('',#39709);
#7721=VERTEX_POINT('',#39762);
#7722=VERTEX_POINT('',#39763);
#7723=VERTEX_POINT('',#39810);
#7724=VERTEX_POINT('',#39811);
#7725=VERTEX_POINT('',#39858);
#7726=VERTEX_POINT('',#39859);
#7727=VERTEX_POINT('',#39912);
#7728=VERTEX_POINT('',#39913);
#7729=VERTEX_POINT('',#39960);
#7730=VERTEX_POINT('',#39961);
#7731=VERTEX_POINT('',#40008);
#7732=VERTEX_POINT('',#40009);
#7733=VERTEX_POINT('',#40056);
#7734=VERTEX_POINT('',#40057);
#7735=VERTEX_POINT('',#40110);
#7736=VERTEX_POINT('',#40111);
#7737=VERTEX_POINT('',#40158);
#7738=VERTEX_POINT('',#40159);
#7739=VERTEX_POINT('',#40206);
#7740=VERTEX_POINT('',#40207);
#7741=VERTEX_POINT('',#40260);
#7742=VERTEX_POINT('',#40261);
#7743=VERTEX_POINT('',#40308);
#7744=VERTEX_POINT('',#40309);
#7745=VERTEX_POINT('',#40356);
#7746=VERTEX_POINT('',#40357);
#7747=VERTEX_POINT('',#40410);
#7748=VERTEX_POINT('',#40411);
#7749=VERTEX_POINT('',#40458);
#7750=VERTEX_POINT('',#40459);
#7751=VERTEX_POINT('',#40506);
#7752=VERTEX_POINT('',#40507);
#7753=VERTEX_POINT('',#40554);
#7754=VERTEX_POINT('',#40555);
#7755=VERTEX_POINT('',#40557);
#7756=VERTEX_POINT('',#40564);
#7757=VERTEX_POINT('',#40565);
#7758=VERTEX_POINT('',#40577);
#7759=VERTEX_POINT('',#40589);
#7760=VERTEX_POINT('',#40590);
#7761=VERTEX_POINT('',#40613);
#7762=VERTEX_POINT('',#40614);
#7763=VERTEX_POINT('',#40637);
#7764=VERTEX_POINT('',#40638);
#7765=VERTEX_POINT('',#40662);
#7766=VERTEX_POINT('',#40663);
#7767=VERTEX_POINT('',#40687);
#7768=VERTEX_POINT('',#40688);
#7769=VERTEX_POINT('',#40711);
#7770=VERTEX_POINT('',#40712);
#7771=VERTEX_POINT('',#40736);
#7772=VERTEX_POINT('',#40737);
#7773=VERTEX_POINT('',#40761);
#7774=VERTEX_POINT('',#40762);
#7775=VERTEX_POINT('',#40785);
#7776=VERTEX_POINT('',#40786);
#7777=VERTEX_POINT('',#40810);
#7778=VERTEX_POINT('',#40811);
#7779=VERTEX_POINT('',#40835);
#7780=VERTEX_POINT('',#40836);
#7781=VERTEX_POINT('',#40859);
#7782=VERTEX_POINT('',#40860);
#7783=VERTEX_POINT('',#40883);
#7784=VERTEX_POINT('',#40884);
#7785=VERTEX_POINT('',#40908);
#7786=VERTEX_POINT('',#40909);
#7787=VERTEX_POINT('',#40933);
#7788=VERTEX_POINT('',#40934);
#7789=VERTEX_POINT('',#40957);
#7790=VERTEX_POINT('',#40958);
#7791=VERTEX_POINT('',#40982);
#7792=VERTEX_POINT('',#40983);
#7793=VERTEX_POINT('',#41007);
#7794=VERTEX_POINT('',#41008);
#7795=VERTEX_POINT('',#41031);
#7796=VERTEX_POINT('',#41032);
#7797=VERTEX_POINT('',#41056);
#7798=VERTEX_POINT('',#41057);
#7799=VERTEX_POINT('',#41081);
#7800=VERTEX_POINT('',#41082);
#7801=VERTEX_POINT('',#41105);
#7802=VERTEX_POINT('',#41106);
#7803=VERTEX_POINT('',#41129);
#7804=VERTEX_POINT('',#41130);
#7805=VERTEX_POINT('',#41154);
#7806=VERTEX_POINT('',#41155);
#7807=VERTEX_POINT('',#41179);
#7808=VERTEX_POINT('',#41180);
#7809=VERTEX_POINT('',#41203);
#7810=VERTEX_POINT('',#41204);
#7811=VERTEX_POINT('',#41228);
#7812=VERTEX_POINT('',#41229);
#7813=VERTEX_POINT('',#41253);
#7814=VERTEX_POINT('',#41254);
#7815=VERTEX_POINT('',#41277);
#7816=VERTEX_POINT('',#41278);
#7817=VERTEX_POINT('',#41302);
#7818=VERTEX_POINT('',#41303);
#7819=VERTEX_POINT('',#41327);
#7820=VERTEX_POINT('',#41328);
#7821=VERTEX_POINT('',#41351);
#7822=VERTEX_POINT('',#41352);
#7823=VERTEX_POINT('',#41375);
#7824=VERTEX_POINT('',#41376);
#7825=VERTEX_POINT('',#41400);
#7826=VERTEX_POINT('',#41401);
#7827=VERTEX_POINT('',#41425);
#7828=VERTEX_POINT('',#41426);
#7829=VERTEX_POINT('',#41449);
#7830=VERTEX_POINT('',#41450);
#7831=VERTEX_POINT('',#41474);
#7832=VERTEX_POINT('',#41475);
#7833=VERTEX_POINT('',#41499);
#7834=VERTEX_POINT('',#41500);
#7835=VERTEX_POINT('',#41523);
#7836=VERTEX_POINT('',#41524);
#7837=VERTEX_POINT('',#41548);
#7838=VERTEX_POINT('',#41549);
#7839=VERTEX_POINT('',#41572);
#7840=VERTEX_POINT('',#41573);
#7841=VERTEX_POINT('',#41597);
#7842=VERTEX_POINT('',#41598);
#7843=VERTEX_POINT('',#42740);
#7844=VERTEX_POINT('',#42851);
#7845=VERTEX_POINT('',#42962);
#7846=VERTEX_POINT('',#42965);
#7847=VERTEX_POINT('',#44193);
#7848=VERTEX_POINT('',#44305);
#7849=VERTEX_POINT('',#44306);
#7850=VERTEX_POINT('',#44310);
#7851=VERTEX_POINT('',#44314);
#7852=VERTEX_POINT('',#44318);
#7853=VERTEX_POINT('',#44322);
#7854=VERTEX_POINT('',#44326);
#7855=VERTEX_POINT('',#44329);
#7856=VERTEX_POINT('',#44337);
#7857=VERTEX_POINT('',#44339);
#7858=VERTEX_POINT('',#44343);
#7859=VERTEX_POINT('',#44347);
#7860=VERTEX_POINT('',#44351);
#7861=VERTEX_POINT('',#44353);
#7862=VERTEX_POINT('',#44364);
#9813=EDGE_CURVE('',#7663,#7664,#4540,.T.);
#9814=EDGE_CURVE('',#7663,#7665,#6130,.T.);
#9815=EDGE_CURVE('',#7665,#7666,#1196,.T.);
#9816=EDGE_CURVE('',#7666,#7664,#6131,.T.);
#9817=EDGE_CURVE('',#7667,#7668,#4541,.T.);
#9818=EDGE_CURVE('',#7667,#7663,#6132,.T.);
#9819=EDGE_CURVE('',#7664,#7668,#6133,.T.);
#9820=EDGE_CURVE('',#7669,#7670,#4542,.T.);
#9821=EDGE_CURVE('',#7669,#7667,#6134,.T.);
#9822=EDGE_CURVE('',#7668,#7670,#6135,.T.);
#9823=EDGE_CURVE('',#7671,#7672,#4543,.T.);
#9824=EDGE_CURVE('',#7671,#7669,#6136,.T.);
#9825=EDGE_CURVE('',#7670,#7672,#6137,.T.);
#9826=EDGE_CURVE('',#7673,#7674,#4544,.T.);
#9827=EDGE_CURVE('',#7673,#7671,#6138,.T.);
#9828=EDGE_CURVE('',#7672,#7674,#6139,.T.);
#9829=EDGE_CURVE('',#7675,#7676,#4545,.T.);
#9830=EDGE_CURVE('',#7675,#7673,#6140,.T.);
#9831=EDGE_CURVE('',#7674,#7676,#6141,.T.);
#9832=EDGE_CURVE('',#7677,#7678,#4546,.T.);
#9833=EDGE_CURVE('',#7677,#7675,#6142,.T.);
#9834=EDGE_CURVE('',#7676,#7678,#6143,.T.);
#9835=EDGE_CURVE('',#7679,#7680,#4547,.T.);
#9836=EDGE_CURVE('',#7679,#7677,#6144,.T.);
#9837=EDGE_CURVE('',#7678,#7680,#6145,.T.);
#9838=EDGE_CURVE('',#7681,#7682,#4548,.T.);
#9839=EDGE_CURVE('',#7681,#7679,#6146,.T.);
#9840=EDGE_CURVE('',#7680,#7682,#6147,.T.);
#9841=EDGE_CURVE('',#7683,#7684,#4549,.T.);
#9842=EDGE_CURVE('',#7683,#7681,#6148,.T.);
#9843=EDGE_CURVE('',#7682,#7684,#6149,.T.);
#9844=EDGE_CURVE('',#7685,#7686,#4550,.T.);
#9845=EDGE_CURVE('',#7685,#7683,#6150,.T.);
#9846=EDGE_CURVE('',#7684,#7686,#6151,.T.);
#9847=EDGE_CURVE('',#7687,#7688,#4551,.T.);
#9848=EDGE_CURVE('',#7687,#7685,#6152,.T.);
#9849=EDGE_CURVE('',#7686,#7688,#6153,.T.);
#9850=EDGE_CURVE('',#7689,#7690,#4552,.T.);
#9851=EDGE_CURVE('',#7689,#7687,#6154,.T.);
#9852=EDGE_CURVE('',#7688,#7690,#6155,.T.);
#9853=EDGE_CURVE('',#7691,#7692,#4553,.T.);
#9854=EDGE_CURVE('',#7691,#7689,#6156,.T.);
#9855=EDGE_CURVE('',#7690,#7692,#6157,.T.);
#9856=EDGE_CURVE('',#7693,#7694,#4554,.T.);
#9857=EDGE_CURVE('',#7693,#7691,#6158,.T.);
#9858=EDGE_CURVE('',#7692,#7694,#6159,.T.);
#9859=EDGE_CURVE('',#7695,#7696,#4555,.T.);
#9860=EDGE_CURVE('',#7695,#7693,#6160,.T.);
#9861=EDGE_CURVE('',#7694,#7696,#6161,.T.);
#9862=EDGE_CURVE('',#7697,#7698,#4556,.T.);
#9863=EDGE_CURVE('',#7697,#7695,#6162,.T.);
#9864=EDGE_CURVE('',#7696,#7698,#6163,.T.);
#9865=EDGE_CURVE('',#7699,#7700,#4557,.T.);
#9866=EDGE_CURVE('',#7699,#7697,#6164,.T.);
#9867=EDGE_CURVE('',#7698,#7700,#6165,.T.);
#9868=EDGE_CURVE('',#7701,#7702,#4558,.T.);
#9869=EDGE_CURVE('',#7701,#7699,#6166,.T.);
#9870=EDGE_CURVE('',#7700,#7702,#6167,.T.);
#9871=EDGE_CURVE('',#7703,#7704,#4559,.T.);
#9872=EDGE_CURVE('',#7703,#7701,#6168,.T.);
#9873=EDGE_CURVE('',#7702,#7704,#6169,.T.);
#9874=EDGE_CURVE('',#7705,#7706,#4560,.T.);
#9875=EDGE_CURVE('',#7705,#7703,#6170,.T.);
#9876=EDGE_CURVE('',#7704,#7706,#6171,.T.);
#9877=EDGE_CURVE('',#7707,#7708,#4561,.T.);
#9878=EDGE_CURVE('',#7707,#7705,#6172,.T.);
#9879=EDGE_CURVE('',#7706,#7708,#6173,.T.);
#9880=EDGE_CURVE('',#7709,#7710,#4562,.T.);
#9881=EDGE_CURVE('',#7709,#7707,#6174,.T.);
#9882=EDGE_CURVE('',#7708,#7710,#6175,.T.);
#9883=EDGE_CURVE('',#7711,#7712,#4563,.T.);
#9884=EDGE_CURVE('',#7711,#7709,#6176,.T.);
#9885=EDGE_CURVE('',#7710,#7712,#6177,.T.);
#9886=EDGE_CURVE('',#7713,#7714,#4564,.T.);
#9887=EDGE_CURVE('',#7713,#7711,#6178,.T.);
#9888=EDGE_CURVE('',#7712,#7714,#6179,.T.);
#9889=EDGE_CURVE('',#7715,#7716,#4565,.T.);
#9890=EDGE_CURVE('',#7715,#7713,#6180,.T.);
#9891=EDGE_CURVE('',#7714,#7716,#6181,.T.);
#9892=EDGE_CURVE('',#7717,#7718,#4566,.T.);
#9893=EDGE_CURVE('',#7717,#7715,#6182,.T.);
#9894=EDGE_CURVE('',#7716,#7718,#6183,.T.);
#9895=EDGE_CURVE('',#7719,#7720,#4567,.T.);
#9896=EDGE_CURVE('',#7719,#7717,#6184,.T.);
#9897=EDGE_CURVE('',#7718,#7720,#6185,.T.);
#9898=EDGE_CURVE('',#7721,#7722,#4568,.T.);
#9899=EDGE_CURVE('',#7721,#7719,#6186,.T.);
#9900=EDGE_CURVE('',#7720,#7722,#6187,.T.);
#9901=EDGE_CURVE('',#7723,#7724,#4569,.T.);
#9902=EDGE_CURVE('',#7723,#7721,#6188,.T.);
#9903=EDGE_CURVE('',#7722,#7724,#6189,.T.);
#9904=EDGE_CURVE('',#7725,#7726,#4570,.T.);
#9905=EDGE_CURVE('',#7725,#7723,#6190,.T.);
#9906=EDGE_CURVE('',#7724,#7726,#6191,.T.);
#9907=EDGE_CURVE('',#7727,#7728,#4571,.T.);
#9908=EDGE_CURVE('',#7727,#7725,#6192,.T.);
#9909=EDGE_CURVE('',#7726,#7728,#6193,.T.);
#9910=EDGE_CURVE('',#7729,#7730,#4572,.T.);
#9911=EDGE_CURVE('',#7729,#7727,#6194,.T.);
#9912=EDGE_CURVE('',#7728,#7730,#6195,.T.);
#9913=EDGE_CURVE('',#7731,#7732,#4573,.T.);
#9914=EDGE_CURVE('',#7731,#7729,#6196,.T.);
#9915=EDGE_CURVE('',#7730,#7732,#6197,.T.);
#9916=EDGE_CURVE('',#7733,#7734,#4574,.T.);
#9917=EDGE_CURVE('',#7733,#7731,#6198,.T.);
#9918=EDGE_CURVE('',#7732,#7734,#6199,.T.);
#9919=EDGE_CURVE('',#7735,#7736,#4575,.T.);
#9920=EDGE_CURVE('',#7735,#7733,#6200,.T.);
#9921=EDGE_CURVE('',#7734,#7736,#6201,.T.);
#9922=EDGE_CURVE('',#7737,#7738,#4576,.T.);
#9923=EDGE_CURVE('',#7737,#7735,#6202,.T.);
#9924=EDGE_CURVE('',#7736,#7738,#6203,.T.);
#9925=EDGE_CURVE('',#7739,#7740,#4577,.T.);
#9926=EDGE_CURVE('',#7739,#7737,#6204,.T.);
#9927=EDGE_CURVE('',#7738,#7740,#6205,.T.);
#9928=EDGE_CURVE('',#7741,#7742,#4578,.T.);
#9929=EDGE_CURVE('',#7741,#7739,#6206,.T.);
#9930=EDGE_CURVE('',#7740,#7742,#6207,.T.);
#9931=EDGE_CURVE('',#7743,#7744,#4579,.T.);
#9932=EDGE_CURVE('',#7743,#7741,#6208,.T.);
#9933=EDGE_CURVE('',#7742,#7744,#6209,.T.);
#9934=EDGE_CURVE('',#7745,#7746,#4580,.T.);
#9935=EDGE_CURVE('',#7745,#7743,#6210,.T.);
#9936=EDGE_CURVE('',#7744,#7746,#6211,.T.);
#9937=EDGE_CURVE('',#7747,#7748,#4581,.T.);
#9938=EDGE_CURVE('',#7747,#7745,#6212,.T.);
#9939=EDGE_CURVE('',#7746,#7748,#6213,.T.);
#9940=EDGE_CURVE('',#7749,#7750,#4582,.T.);
#9941=EDGE_CURVE('',#7749,#7747,#6214,.T.);
#9942=EDGE_CURVE('',#7748,#7750,#6215,.T.);
#9943=EDGE_CURVE('',#7751,#7752,#4583,.T.);
#9944=EDGE_CURVE('',#7751,#7749,#6216,.T.);
#9945=EDGE_CURVE('',#7750,#7752,#6217,.T.);
#9946=EDGE_CURVE('',#7753,#7754,#4584,.T.);
#9947=EDGE_CURVE('',#7753,#7755,#6218,.T.);
#9948=EDGE_CURVE('',#7754,#7755,#1197,.T.);
#9949=EDGE_CURVE('',#7756,#7757,#4585,.T.);
#9950=EDGE_CURVE('',#7756,#7753,#6219,.T.);
#9951=EDGE_CURVE('',#7758,#7754,#1198,.T.);
#9952=EDGE_CURVE('',#7757,#7758,#6220,.T.);
#9953=EDGE_CURVE('',#7759,#7760,#4586,.T.);
#9954=EDGE_CURVE('',#7759,#7756,#6221,.T.);
#9955=EDGE_CURVE('',#7760,#7757,#6222,.T.);
#9956=EDGE_CURVE('',#7761,#7762,#4587,.T.);
#9957=EDGE_CURVE('',#7761,#7759,#6223,.T.);
#9958=EDGE_CURVE('',#7762,#7760,#6224,.T.);
#9959=EDGE_CURVE('',#7763,#7764,#4588,.T.);
#9960=EDGE_CURVE('',#7763,#7761,#6225,.T.);
#9961=EDGE_CURVE('',#7764,#7762,#6226,.T.);
#9962=EDGE_CURVE('',#7765,#7766,#4589,.T.);
#9963=EDGE_CURVE('',#7765,#7763,#6227,.T.);
#9964=EDGE_CURVE('',#7766,#7764,#6228,.T.);
#9965=EDGE_CURVE('',#7767,#7768,#4590,.T.);
#9966=EDGE_CURVE('',#7767,#7765,#6229,.T.);
#9967=EDGE_CURVE('',#7768,#7766,#6230,.T.);
#9968=EDGE_CURVE('',#7769,#7770,#4591,.T.);
#9969=EDGE_CURVE('',#7769,#7767,#6231,.T.);
#9970=EDGE_CURVE('',#7770,#7768,#6232,.T.);
#9971=EDGE_CURVE('',#7771,#7772,#4592,.T.);
#9972=EDGE_CURVE('',#7771,#7769,#6233,.T.);
#9973=EDGE_CURVE('',#7772,#7770,#6234,.T.);
#9974=EDGE_CURVE('',#7773,#7774,#4593,.T.);
#9975=EDGE_CURVE('',#7773,#7771,#6235,.T.);
#9976=EDGE_CURVE('',#7774,#7772,#6236,.T.);
#9977=EDGE_CURVE('',#7775,#7776,#4594,.T.);
#9978=EDGE_CURVE('',#7775,#7773,#6237,.T.);
#9979=EDGE_CURVE('',#7776,#7774,#6238,.T.);
#9980=EDGE_CURVE('',#7777,#7778,#4595,.T.);
#9981=EDGE_CURVE('',#7777,#7775,#6239,.T.);
#9982=EDGE_CURVE('',#7778,#7776,#6240,.T.);
#9983=EDGE_CURVE('',#7779,#7780,#4596,.T.);
#9984=EDGE_CURVE('',#7779,#7777,#6241,.T.);
#9985=EDGE_CURVE('',#7780,#7778,#6242,.T.);
#9986=EDGE_CURVE('',#7781,#7782,#4597,.T.);
#9987=EDGE_CURVE('',#7781,#7779,#6243,.T.);
#9988=EDGE_CURVE('',#7782,#7780,#6244,.T.);
#9989=EDGE_CURVE('',#7783,#7784,#4598,.T.);
#9990=EDGE_CURVE('',#7783,#7781,#6245,.T.);
#9991=EDGE_CURVE('',#7784,#7782,#6246,.T.);
#9992=EDGE_CURVE('',#7785,#7786,#4599,.T.);
#9993=EDGE_CURVE('',#7785,#7783,#6247,.T.);
#9994=EDGE_CURVE('',#7786,#7784,#6248,.T.);
#9995=EDGE_CURVE('',#7787,#7788,#4600,.T.);
#9996=EDGE_CURVE('',#7787,#7785,#6249,.T.);
#9997=EDGE_CURVE('',#7788,#7786,#6250,.T.);
#9998=EDGE_CURVE('',#7789,#7790,#4601,.T.);
#9999=EDGE_CURVE('',#7789,#7787,#6251,.T.);
#10000=EDGE_CURVE('',#7790,#7788,#6252,.T.);
#10001=EDGE_CURVE('',#7791,#7792,#4602,.T.);
#10002=EDGE_CURVE('',#7791,#7789,#6253,.T.);
#10003=EDGE_CURVE('',#7792,#7790,#6254,.T.);
#10004=EDGE_CURVE('',#7793,#7794,#4603,.T.);
#10005=EDGE_CURVE('',#7793,#7791,#6255,.T.);
#10006=EDGE_CURVE('',#7794,#7792,#6256,.T.);
#10007=EDGE_CURVE('',#7795,#7796,#4604,.T.);
#10008=EDGE_CURVE('',#7795,#7793,#6257,.T.);
#10009=EDGE_CURVE('',#7796,#7794,#6258,.T.);
#10010=EDGE_CURVE('',#7797,#7798,#4605,.T.);
#10011=EDGE_CURVE('',#7797,#7795,#6259,.T.);
#10012=EDGE_CURVE('',#7798,#7796,#6260,.T.);
#10013=EDGE_CURVE('',#7799,#7800,#4606,.T.);
#10014=EDGE_CURVE('',#7799,#7797,#6261,.T.);
#10015=EDGE_CURVE('',#7800,#7798,#6262,.T.);
#10016=EDGE_CURVE('',#7801,#7802,#4607,.T.);
#10017=EDGE_CURVE('',#7801,#7799,#6263,.T.);
#10018=EDGE_CURVE('',#7802,#7800,#6264,.T.);
#10019=EDGE_CURVE('',#7803,#7804,#4608,.T.);
#10020=EDGE_CURVE('',#7803,#7801,#6265,.T.);
#10021=EDGE_CURVE('',#7804,#7802,#6266,.T.);
#10022=EDGE_CURVE('',#7805,#7806,#4609,.T.);
#10023=EDGE_CURVE('',#7805,#7803,#6267,.T.);
#10024=EDGE_CURVE('',#7806,#7804,#6268,.T.);
#10025=EDGE_CURVE('',#7807,#7808,#4610,.T.);
#10026=EDGE_CURVE('',#7807,#7805,#6269,.T.);
#10027=EDGE_CURVE('',#7808,#7806,#6270,.T.);
#10028=EDGE_CURVE('',#7809,#7810,#4611,.T.);
#10029=EDGE_CURVE('',#7809,#7807,#6271,.T.);
#10030=EDGE_CURVE('',#7810,#7808,#6272,.T.);
#10031=EDGE_CURVE('',#7811,#7812,#4612,.T.);
#10032=EDGE_CURVE('',#7811,#7809,#6273,.T.);
#10033=EDGE_CURVE('',#7812,#7810,#6274,.T.);
#10034=EDGE_CURVE('',#7813,#7814,#4613,.T.);
#10035=EDGE_CURVE('',#7813,#7811,#6275,.T.);
#10036=EDGE_CURVE('',#7814,#7812,#6276,.T.);
#10037=EDGE_CURVE('',#7815,#7816,#4614,.T.);
#10038=EDGE_CURVE('',#7815,#7813,#6277,.T.);
#10039=EDGE_CURVE('',#7816,#7814,#6278,.T.);
#10040=EDGE_CURVE('',#7817,#7818,#4615,.T.);
#10041=EDGE_CURVE('',#7817,#7815,#6279,.T.);
#10042=EDGE_CURVE('',#7818,#7816,#6280,.T.);
#10043=EDGE_CURVE('',#7819,#7820,#4616,.T.);
#10044=EDGE_CURVE('',#7819,#7817,#6281,.T.);
#10045=EDGE_CURVE('',#7820,#7818,#6282,.T.);
#10046=EDGE_CURVE('',#7821,#7822,#4617,.T.);
#10047=EDGE_CURVE('',#7821,#7819,#6283,.T.);
#10048=EDGE_CURVE('',#7822,#7820,#6284,.T.);
#10049=EDGE_CURVE('',#7823,#7824,#4618,.T.);
#10050=EDGE_CURVE('',#7823,#7821,#6285,.T.);
#10051=EDGE_CURVE('',#7824,#7822,#6286,.T.);
#10052=EDGE_CURVE('',#7825,#7826,#4619,.T.);
#10053=EDGE_CURVE('',#7825,#7823,#6287,.T.);
#10054=EDGE_CURVE('',#7826,#7824,#6288,.T.);
#10055=EDGE_CURVE('',#7827,#7828,#4620,.T.);
#10056=EDGE_CURVE('',#7827,#7825,#6289,.T.);
#10057=EDGE_CURVE('',#7828,#7826,#6290,.T.);
#10058=EDGE_CURVE('',#7829,#7830,#4621,.T.);
#10059=EDGE_CURVE('',#7829,#7827,#6291,.T.);
#10060=EDGE_CURVE('',#7830,#7828,#6292,.T.);
#10061=EDGE_CURVE('',#7831,#7832,#4622,.T.);
#10062=EDGE_CURVE('',#7831,#7829,#6293,.T.);
#10063=EDGE_CURVE('',#7832,#7830,#6294,.T.);
#10064=EDGE_CURVE('',#7833,#7834,#4623,.T.);
#10065=EDGE_CURVE('',#7833,#7831,#6295,.T.);
#10066=EDGE_CURVE('',#7834,#7832,#6296,.T.);
#10067=EDGE_CURVE('',#7835,#7836,#4624,.T.);
#10068=EDGE_CURVE('',#7835,#7833,#6297,.T.);
#10069=EDGE_CURVE('',#7836,#7834,#6298,.T.);
#10070=EDGE_CURVE('',#7837,#7838,#4625,.T.);
#10071=EDGE_CURVE('',#7837,#7835,#6299,.T.);
#10072=EDGE_CURVE('',#7838,#7836,#6300,.T.);
#10073=EDGE_CURVE('',#7839,#7840,#4626,.T.);
#10074=EDGE_CURVE('',#7839,#7837,#6301,.T.);
#10075=EDGE_CURVE('',#7840,#7838,#6302,.T.);
#10076=EDGE_CURVE('',#7841,#7842,#4627,.T.);
#10077=EDGE_CURVE('',#7841,#7839,#6303,.T.);
#10078=EDGE_CURVE('',#7842,#7840,#6304,.T.);
#10079=EDGE_CURVE('',#7843,#7758,#6305,.T.);
#10080=EDGE_CURVE('',#7752,#7843,#6306,.T.);
#10081=EDGE_CURVE('',#7844,#7666,#6307,.T.);
#10082=EDGE_CURVE('',#7844,#7842,#6308,.T.);
#10083=EDGE_CURVE('',#7666,#7845,#1199,.T.);
#10084=EDGE_CURVE('',#7845,#7665,#1200,.T.);
#10085=EDGE_CURVE('',#7665,#7846,#6309,.T.);
#10086=EDGE_CURVE('',#7846,#7844,#1201,.T.);
#10087=EDGE_CURVE('',#7846,#7841,#6310,.T.);
#10088=EDGE_CURVE('',#7755,#7847,#6311,.T.);
#10089=EDGE_CURVE('',#7847,#7751,#6312,.T.);
#10090=EDGE_CURVE('',#7848,#7849,#1778,.T.);
#10091=EDGE_CURVE('',#7850,#7848,#1779,.T.);
#10092=EDGE_CURVE('',#7851,#7850,#1780,.T.);
#10093=EDGE_CURVE('',#7852,#7851,#1781,.T.);
#10094=EDGE_CURVE('',#7853,#7852,#1782,.T.);
#10095=EDGE_CURVE('',#7853,#7854,#4628,.T.);
#10096=EDGE_CURVE('',#7854,#7854,#1202,.T.);
#10097=EDGE_CURVE('',#7855,#7853,#1783,.T.);
#10098=EDGE_CURVE('',#7849,#7855,#1784,.T.);
#10099=EDGE_CURVE('',#7856,#7851,#4629,.T.);
#10100=EDGE_CURVE('',#7856,#7857,#4630,.T.);
#10101=EDGE_CURVE('',#7857,#7852,#4631,.T.);
#10102=EDGE_CURVE('',#7858,#7850,#4632,.T.);
#10103=EDGE_CURVE('',#7858,#7856,#4633,.T.);
#10104=EDGE_CURVE('',#7859,#7848,#4634,.T.);
#10105=EDGE_CURVE('',#7859,#7858,#4635,.T.);
#10106=EDGE_CURVE('',#7860,#7859,#4636,.T.);
#10107=EDGE_CURVE('',#7861,#7860,#4637,.T.);
#10108=EDGE_CURVE('',#7857,#7861,#4638,.T.);
#10109=EDGE_CURVE('',#7847,#7843,#1203,.F.);
#10110=EDGE_CURVE('',#7860,#7849,#4639,.T.);
#10111=EDGE_CURVE('',#7861,#7855,#4640,.T.);
#10112=EDGE_CURVE('',#7862,#7862,#1204,.T.);
#10113=EDGE_CURVE('',#7845,#7862,#4641,.T.);
#13812=ORIENTED_EDGE('',*,*,#9813,.F.);
#13813=ORIENTED_EDGE('',*,*,#9814,.T.);
#13814=ORIENTED_EDGE('',*,*,#9815,.T.);
#13815=ORIENTED_EDGE('',*,*,#9816,.T.);
#13816=ORIENTED_EDGE('',*,*,#9817,.F.);
#13817=ORIENTED_EDGE('',*,*,#9818,.T.);
#13818=ORIENTED_EDGE('',*,*,#9813,.T.);
#13819=ORIENTED_EDGE('',*,*,#9819,.T.);
#13820=ORIENTED_EDGE('',*,*,#9820,.F.);
#13821=ORIENTED_EDGE('',*,*,#9821,.T.);
#13822=ORIENTED_EDGE('',*,*,#9817,.T.);
#13823=ORIENTED_EDGE('',*,*,#9822,.T.);
#13824=ORIENTED_EDGE('',*,*,#9823,.F.);
#13825=ORIENTED_EDGE('',*,*,#9824,.T.);
#13826=ORIENTED_EDGE('',*,*,#9820,.T.);
#13827=ORIENTED_EDGE('',*,*,#9825,.T.);
#13828=ORIENTED_EDGE('',*,*,#9826,.F.);
#13829=ORIENTED_EDGE('',*,*,#9827,.T.);
#13830=ORIENTED_EDGE('',*,*,#9823,.T.);
#13831=ORIENTED_EDGE('',*,*,#9828,.T.);
#13832=ORIENTED_EDGE('',*,*,#9829,.F.);
#13833=ORIENTED_EDGE('',*,*,#9830,.T.);
#13834=ORIENTED_EDGE('',*,*,#9826,.T.);
#13835=ORIENTED_EDGE('',*,*,#9831,.T.);
#13836=ORIENTED_EDGE('',*,*,#9832,.F.);
#13837=ORIENTED_EDGE('',*,*,#9833,.T.);
#13838=ORIENTED_EDGE('',*,*,#9829,.T.);
#13839=ORIENTED_EDGE('',*,*,#9834,.T.);
#13840=ORIENTED_EDGE('',*,*,#9835,.F.);
#13841=ORIENTED_EDGE('',*,*,#9836,.T.);
#13842=ORIENTED_EDGE('',*,*,#9832,.T.);
#13843=ORIENTED_EDGE('',*,*,#9837,.T.);
#13844=ORIENTED_EDGE('',*,*,#9838,.F.);
#13845=ORIENTED_EDGE('',*,*,#9839,.T.);
#13846=ORIENTED_EDGE('',*,*,#9835,.T.);
#13847=ORIENTED_EDGE('',*,*,#9840,.T.);
#13848=ORIENTED_EDGE('',*,*,#9841,.F.);
#13849=ORIENTED_EDGE('',*,*,#9842,.T.);
#13850=ORIENTED_EDGE('',*,*,#9838,.T.);
#13851=ORIENTED_EDGE('',*,*,#9843,.T.);
#13852=ORIENTED_EDGE('',*,*,#9844,.F.);
#13853=ORIENTED_EDGE('',*,*,#9845,.T.);
#13854=ORIENTED_EDGE('',*,*,#9841,.T.);
#13855=ORIENTED_EDGE('',*,*,#9846,.T.);
#13856=ORIENTED_EDGE('',*,*,#9847,.F.);
#13857=ORIENTED_EDGE('',*,*,#9848,.T.);
#13858=ORIENTED_EDGE('',*,*,#9844,.T.);
#13859=ORIENTED_EDGE('',*,*,#9849,.T.);
#13860=ORIENTED_EDGE('',*,*,#9850,.F.);
#13861=ORIENTED_EDGE('',*,*,#9851,.T.);
#13862=ORIENTED_EDGE('',*,*,#9847,.T.);
#13863=ORIENTED_EDGE('',*,*,#9852,.T.);
#13864=ORIENTED_EDGE('',*,*,#9853,.F.);
#13865=ORIENTED_EDGE('',*,*,#9854,.T.);
#13866=ORIENTED_EDGE('',*,*,#9850,.T.);
#13867=ORIENTED_EDGE('',*,*,#9855,.T.);
#13868=ORIENTED_EDGE('',*,*,#9856,.F.);
#13869=ORIENTED_EDGE('',*,*,#9857,.T.);
#13870=ORIENTED_EDGE('',*,*,#9853,.T.);
#13871=ORIENTED_EDGE('',*,*,#9858,.T.);
#13872=ORIENTED_EDGE('',*,*,#9859,.F.);
#13873=ORIENTED_EDGE('',*,*,#9860,.T.);
#13874=ORIENTED_EDGE('',*,*,#9856,.T.);
#13875=ORIENTED_EDGE('',*,*,#9861,.T.);
#13876=ORIENTED_EDGE('',*,*,#9862,.F.);
#13877=ORIENTED_EDGE('',*,*,#9863,.T.);
#13878=ORIENTED_EDGE('',*,*,#9859,.T.);
#13879=ORIENTED_EDGE('',*,*,#9864,.T.);
#13880=ORIENTED_EDGE('',*,*,#9865,.F.);
#13881=ORIENTED_EDGE('',*,*,#9866,.T.);
#13882=ORIENTED_EDGE('',*,*,#9862,.T.);
#13883=ORIENTED_EDGE('',*,*,#9867,.T.);
#13884=ORIENTED_EDGE('',*,*,#9868,.F.);
#13885=ORIENTED_EDGE('',*,*,#9869,.T.);
#13886=ORIENTED_EDGE('',*,*,#9865,.T.);
#13887=ORIENTED_EDGE('',*,*,#9870,.T.);
#13888=ORIENTED_EDGE('',*,*,#9871,.F.);
#13889=ORIENTED_EDGE('',*,*,#9872,.T.);
#13890=ORIENTED_EDGE('',*,*,#9868,.T.);
#13891=ORIENTED_EDGE('',*,*,#9873,.T.);
#13892=ORIENTED_EDGE('',*,*,#9874,.F.);
#13893=ORIENTED_EDGE('',*,*,#9875,.T.);
#13894=ORIENTED_EDGE('',*,*,#9871,.T.);
#13895=ORIENTED_EDGE('',*,*,#9876,.T.);
#13896=ORIENTED_EDGE('',*,*,#9877,.F.);
#13897=ORIENTED_EDGE('',*,*,#9878,.T.);
#13898=ORIENTED_EDGE('',*,*,#9874,.T.);
#13899=ORIENTED_EDGE('',*,*,#9879,.T.);
#13900=ORIENTED_EDGE('',*,*,#9880,.F.);
#13901=ORIENTED_EDGE('',*,*,#9881,.T.);
#13902=ORIENTED_EDGE('',*,*,#9877,.T.);
#13903=ORIENTED_EDGE('',*,*,#9882,.T.);
#13904=ORIENTED_EDGE('',*,*,#9883,.F.);
#13905=ORIENTED_EDGE('',*,*,#9884,.T.);
#13906=ORIENTED_EDGE('',*,*,#9880,.T.);
#13907=ORIENTED_EDGE('',*,*,#9885,.T.);
#13908=ORIENTED_EDGE('',*,*,#9886,.F.);
#13909=ORIENTED_EDGE('',*,*,#9887,.T.);
#13910=ORIENTED_EDGE('',*,*,#9883,.T.);
#13911=ORIENTED_EDGE('',*,*,#9888,.T.);
#13912=ORIENTED_EDGE('',*,*,#9889,.F.);
#13913=ORIENTED_EDGE('',*,*,#9890,.T.);
#13914=ORIENTED_EDGE('',*,*,#9886,.T.);
#13915=ORIENTED_EDGE('',*,*,#9891,.T.);
#13916=ORIENTED_EDGE('',*,*,#9892,.F.);
#13917=ORIENTED_EDGE('',*,*,#9893,.T.);
#13918=ORIENTED_EDGE('',*,*,#9889,.T.);
#13919=ORIENTED_EDGE('',*,*,#9894,.T.);
#13920=ORIENTED_EDGE('',*,*,#9895,.F.);
#13921=ORIENTED_EDGE('',*,*,#9896,.T.);
#13922=ORIENTED_EDGE('',*,*,#9892,.T.);
#13923=ORIENTED_EDGE('',*,*,#9897,.T.);
#13924=ORIENTED_EDGE('',*,*,#9898,.F.);
#13925=ORIENTED_EDGE('',*,*,#9899,.T.);
#13926=ORIENTED_EDGE('',*,*,#9895,.T.);
#13927=ORIENTED_EDGE('',*,*,#9900,.T.);
#13928=ORIENTED_EDGE('',*,*,#9901,.F.);
#13929=ORIENTED_EDGE('',*,*,#9902,.T.);
#13930=ORIENTED_EDGE('',*,*,#9898,.T.);
#13931=ORIENTED_EDGE('',*,*,#9903,.T.);
#13932=ORIENTED_EDGE('',*,*,#9904,.F.);
#13933=ORIENTED_EDGE('',*,*,#9905,.T.);
#13934=ORIENTED_EDGE('',*,*,#9901,.T.);
#13935=ORIENTED_EDGE('',*,*,#9906,.T.);
#13936=ORIENTED_EDGE('',*,*,#9907,.F.);
#13937=ORIENTED_EDGE('',*,*,#9908,.T.);
#13938=ORIENTED_EDGE('',*,*,#9904,.T.);
#13939=ORIENTED_EDGE('',*,*,#9909,.T.);
#13940=ORIENTED_EDGE('',*,*,#9910,.F.);
#13941=ORIENTED_EDGE('',*,*,#9911,.T.);
#13942=ORIENTED_EDGE('',*,*,#9907,.T.);
#13943=ORIENTED_EDGE('',*,*,#9912,.T.);
#13944=ORIENTED_EDGE('',*,*,#9913,.F.);
#13945=ORIENTED_EDGE('',*,*,#9914,.T.);
#13946=ORIENTED_EDGE('',*,*,#9910,.T.);
#13947=ORIENTED_EDGE('',*,*,#9915,.T.);
#13948=ORIENTED_EDGE('',*,*,#9916,.F.);
#13949=ORIENTED_EDGE('',*,*,#9917,.T.);
#13950=ORIENTED_EDGE('',*,*,#9913,.T.);
#13951=ORIENTED_EDGE('',*,*,#9918,.T.);
#13952=ORIENTED_EDGE('',*,*,#9919,.F.);
#13953=ORIENTED_EDGE('',*,*,#9920,.T.);
#13954=ORIENTED_EDGE('',*,*,#9916,.T.);
#13955=ORIENTED_EDGE('',*,*,#9921,.T.);
#13956=ORIENTED_EDGE('',*,*,#9922,.F.);
#13957=ORIENTED_EDGE('',*,*,#9923,.T.);
#13958=ORIENTED_EDGE('',*,*,#9919,.T.);
#13959=ORIENTED_EDGE('',*,*,#9924,.T.);
#13960=ORIENTED_EDGE('',*,*,#9925,.F.);
#13961=ORIENTED_EDGE('',*,*,#9926,.T.);
#13962=ORIENTED_EDGE('',*,*,#9922,.T.);
#13963=ORIENTED_EDGE('',*,*,#9927,.T.);
#13964=ORIENTED_EDGE('',*,*,#9928,.F.);
#13965=ORIENTED_EDGE('',*,*,#9929,.T.);
#13966=ORIENTED_EDGE('',*,*,#9925,.T.);
#13967=ORIENTED_EDGE('',*,*,#9930,.T.);
#13968=ORIENTED_EDGE('',*,*,#9931,.F.);
#13969=ORIENTED_EDGE('',*,*,#9932,.T.);
#13970=ORIENTED_EDGE('',*,*,#9928,.T.);
#13971=ORIENTED_EDGE('',*,*,#9933,.T.);
#13972=ORIENTED_EDGE('',*,*,#9934,.F.);
#13973=ORIENTED_EDGE('',*,*,#9935,.T.);
#13974=ORIENTED_EDGE('',*,*,#9931,.T.);
#13975=ORIENTED_EDGE('',*,*,#9936,.T.);
#13976=ORIENTED_EDGE('',*,*,#9937,.F.);
#13977=ORIENTED_EDGE('',*,*,#9938,.T.);
#13978=ORIENTED_EDGE('',*,*,#9934,.T.);
#13979=ORIENTED_EDGE('',*,*,#9939,.T.);
#13980=ORIENTED_EDGE('',*,*,#9940,.F.);
#13981=ORIENTED_EDGE('',*,*,#9941,.T.);
#13982=ORIENTED_EDGE('',*,*,#9937,.T.);
#13983=ORIENTED_EDGE('',*,*,#9942,.T.);
#13984=ORIENTED_EDGE('',*,*,#9943,.F.);
#13985=ORIENTED_EDGE('',*,*,#9944,.T.);
#13986=ORIENTED_EDGE('',*,*,#9940,.T.);
#13987=ORIENTED_EDGE('',*,*,#9945,.T.);
#13988=ORIENTED_EDGE('',*,*,#9946,.F.);
#13989=ORIENTED_EDGE('',*,*,#9947,.T.);
#13990=ORIENTED_EDGE('',*,*,#9948,.F.);
#13991=ORIENTED_EDGE('',*,*,#9949,.F.);
#13992=ORIENTED_EDGE('',*,*,#9950,.T.);
#13993=ORIENTED_EDGE('',*,*,#9946,.T.);
#13994=ORIENTED_EDGE('',*,*,#9951,.F.);
#13995=ORIENTED_EDGE('',*,*,#9952,.F.);
#13996=ORIENTED_EDGE('',*,*,#9953,.F.);
#13997=ORIENTED_EDGE('',*,*,#9954,.T.);
#13998=ORIENTED_EDGE('',*,*,#9949,.T.);
#13999=ORIENTED_EDGE('',*,*,#9955,.F.);
#14000=ORIENTED_EDGE('',*,*,#9956,.F.);
#14001=ORIENTED_EDGE('',*,*,#9957,.T.);
#14002=ORIENTED_EDGE('',*,*,#9953,.T.);
#14003=ORIENTED_EDGE('',*,*,#9958,.F.);
#14004=ORIENTED_EDGE('',*,*,#9959,.F.);
#14005=ORIENTED_EDGE('',*,*,#9960,.T.);
#14006=ORIENTED_EDGE('',*,*,#9956,.T.);
#14007=ORIENTED_EDGE('',*,*,#9961,.F.);
#14008=ORIENTED_EDGE('',*,*,#9962,.F.);
#14009=ORIENTED_EDGE('',*,*,#9963,.T.);
#14010=ORIENTED_EDGE('',*,*,#9959,.T.);
#14011=ORIENTED_EDGE('',*,*,#9964,.F.);
#14012=ORIENTED_EDGE('',*,*,#9965,.F.);
#14013=ORIENTED_EDGE('',*,*,#9966,.T.);
#14014=ORIENTED_EDGE('',*,*,#9962,.T.);
#14015=ORIENTED_EDGE('',*,*,#9967,.F.);
#14016=ORIENTED_EDGE('',*,*,#9968,.F.);
#14017=ORIENTED_EDGE('',*,*,#9969,.T.);
#14018=ORIENTED_EDGE('',*,*,#9965,.T.);
#14019=ORIENTED_EDGE('',*,*,#9970,.F.);
#14020=ORIENTED_EDGE('',*,*,#9971,.F.);
#14021=ORIENTED_EDGE('',*,*,#9972,.T.);
#14022=ORIENTED_EDGE('',*,*,#9968,.T.);
#14023=ORIENTED_EDGE('',*,*,#9973,.F.);
#14024=ORIENTED_EDGE('',*,*,#9974,.F.);
#14025=ORIENTED_EDGE('',*,*,#9975,.T.);
#14026=ORIENTED_EDGE('',*,*,#9971,.T.);
#14027=ORIENTED_EDGE('',*,*,#9976,.F.);
#14028=ORIENTED_EDGE('',*,*,#9977,.F.);
#14029=ORIENTED_EDGE('',*,*,#9978,.T.);
#14030=ORIENTED_EDGE('',*,*,#9974,.T.);
#14031=ORIENTED_EDGE('',*,*,#9979,.F.);
#14032=ORIENTED_EDGE('',*,*,#9980,.F.);
#14033=ORIENTED_EDGE('',*,*,#9981,.T.);
#14034=ORIENTED_EDGE('',*,*,#9977,.T.);
#14035=ORIENTED_EDGE('',*,*,#9982,.F.);
#14036=ORIENTED_EDGE('',*,*,#9983,.F.);
#14037=ORIENTED_EDGE('',*,*,#9984,.T.);
#14038=ORIENTED_EDGE('',*,*,#9980,.T.);
#14039=ORIENTED_EDGE('',*,*,#9985,.F.);
#14040=ORIENTED_EDGE('',*,*,#9986,.F.);
#14041=ORIENTED_EDGE('',*,*,#9987,.T.);
#14042=ORIENTED_EDGE('',*,*,#9983,.T.);
#14043=ORIENTED_EDGE('',*,*,#9988,.F.);
#14044=ORIENTED_EDGE('',*,*,#9989,.F.);
#14045=ORIENTED_EDGE('',*,*,#9990,.T.);
#14046=ORIENTED_EDGE('',*,*,#9986,.T.);
#14047=ORIENTED_EDGE('',*,*,#9991,.F.);
#14048=ORIENTED_EDGE('',*,*,#9992,.F.);
#14049=ORIENTED_EDGE('',*,*,#9993,.T.);
#14050=ORIENTED_EDGE('',*,*,#9989,.T.);
#14051=ORIENTED_EDGE('',*,*,#9994,.F.);
#14052=ORIENTED_EDGE('',*,*,#9995,.F.);
#14053=ORIENTED_EDGE('',*,*,#9996,.T.);
#14054=ORIENTED_EDGE('',*,*,#9992,.T.);
#14055=ORIENTED_EDGE('',*,*,#9997,.F.);
#14056=ORIENTED_EDGE('',*,*,#9998,.F.);
#14057=ORIENTED_EDGE('',*,*,#9999,.T.);
#14058=ORIENTED_EDGE('',*,*,#9995,.T.);
#14059=ORIENTED_EDGE('',*,*,#10000,.F.);
#14060=ORIENTED_EDGE('',*,*,#10001,.F.);
#14061=ORIENTED_EDGE('',*,*,#10002,.T.);
#14062=ORIENTED_EDGE('',*,*,#9998,.T.);
#14063=ORIENTED_EDGE('',*,*,#10003,.F.);
#14064=ORIENTED_EDGE('',*,*,#10004,.F.);
#14065=ORIENTED_EDGE('',*,*,#10005,.T.);
#14066=ORIENTED_EDGE('',*,*,#10001,.T.);
#14067=ORIENTED_EDGE('',*,*,#10006,.F.);
#14068=ORIENTED_EDGE('',*,*,#10007,.F.);
#14069=ORIENTED_EDGE('',*,*,#10008,.T.);
#14070=ORIENTED_EDGE('',*,*,#10004,.T.);
#14071=ORIENTED_EDGE('',*,*,#10009,.F.);
#14072=ORIENTED_EDGE('',*,*,#10010,.F.);
#14073=ORIENTED_EDGE('',*,*,#10011,.T.);
#14074=ORIENTED_EDGE('',*,*,#10007,.T.);
#14075=ORIENTED_EDGE('',*,*,#10012,.F.);
#14076=ORIENTED_EDGE('',*,*,#10013,.F.);
#14077=ORIENTED_EDGE('',*,*,#10014,.T.);
#14078=ORIENTED_EDGE('',*,*,#10010,.T.);
#14079=ORIENTED_EDGE('',*,*,#10015,.F.);
#14080=ORIENTED_EDGE('',*,*,#10016,.F.);
#14081=ORIENTED_EDGE('',*,*,#10017,.T.);
#14082=ORIENTED_EDGE('',*,*,#10013,.T.);
#14083=ORIENTED_EDGE('',*,*,#10018,.F.);
#14084=ORIENTED_EDGE('',*,*,#10019,.F.);
#14085=ORIENTED_EDGE('',*,*,#10020,.T.);
#14086=ORIENTED_EDGE('',*,*,#10016,.T.);
#14087=ORIENTED_EDGE('',*,*,#10021,.F.);
#14088=ORIENTED_EDGE('',*,*,#10022,.F.);
#14089=ORIENTED_EDGE('',*,*,#10023,.T.);
#14090=ORIENTED_EDGE('',*,*,#10019,.T.);
#14091=ORIENTED_EDGE('',*,*,#10024,.F.);
#14092=ORIENTED_EDGE('',*,*,#10025,.F.);
#14093=ORIENTED_EDGE('',*,*,#10026,.T.);
#14094=ORIENTED_EDGE('',*,*,#10022,.T.);
#14095=ORIENTED_EDGE('',*,*,#10027,.F.);
#14096=ORIENTED_EDGE('',*,*,#10028,.F.);
#14097=ORIENTED_EDGE('',*,*,#10029,.T.);
#14098=ORIENTED_EDGE('',*,*,#10025,.T.);
#14099=ORIENTED_EDGE('',*,*,#10030,.F.);
#14100=ORIENTED_EDGE('',*,*,#10031,.F.);
#14101=ORIENTED_EDGE('',*,*,#10032,.T.);
#14102=ORIENTED_EDGE('',*,*,#10028,.T.);
#14103=ORIENTED_EDGE('',*,*,#10033,.F.);
#14104=ORIENTED_EDGE('',*,*,#10034,.F.);
#14105=ORIENTED_EDGE('',*,*,#10035,.T.);
#14106=ORIENTED_EDGE('',*,*,#10031,.T.);
#14107=ORIENTED_EDGE('',*,*,#10036,.F.);
#14108=ORIENTED_EDGE('',*,*,#10037,.F.);
#14109=ORIENTED_EDGE('',*,*,#10038,.T.);
#14110=ORIENTED_EDGE('',*,*,#10034,.T.);
#14111=ORIENTED_EDGE('',*,*,#10039,.F.);
#14112=ORIENTED_EDGE('',*,*,#10040,.F.);
#14113=ORIENTED_EDGE('',*,*,#10041,.T.);
#14114=ORIENTED_EDGE('',*,*,#10037,.T.);
#14115=ORIENTED_EDGE('',*,*,#10042,.F.);
#14116=ORIENTED_EDGE('',*,*,#10043,.F.);
#14117=ORIENTED_EDGE('',*,*,#10044,.T.);
#14118=ORIENTED_EDGE('',*,*,#10040,.T.);
#14119=ORIENTED_EDGE('',*,*,#10045,.F.);
#14120=ORIENTED_EDGE('',*,*,#10046,.F.);
#14121=ORIENTED_EDGE('',*,*,#10047,.T.);
#14122=ORIENTED_EDGE('',*,*,#10043,.T.);
#14123=ORIENTED_EDGE('',*,*,#10048,.F.);
#14124=ORIENTED_EDGE('',*,*,#10049,.F.);
#14125=ORIENTED_EDGE('',*,*,#10050,.T.);
#14126=ORIENTED_EDGE('',*,*,#10046,.T.);
#14127=ORIENTED_EDGE('',*,*,#10051,.F.);
#14128=ORIENTED_EDGE('',*,*,#10052,.F.);
#14129=ORIENTED_EDGE('',*,*,#10053,.T.);
#14130=ORIENTED_EDGE('',*,*,#10049,.T.);
#14131=ORIENTED_EDGE('',*,*,#10054,.F.);
#14132=ORIENTED_EDGE('',*,*,#10055,.F.);
#14133=ORIENTED_EDGE('',*,*,#10056,.T.);
#14134=ORIENTED_EDGE('',*,*,#10052,.T.);
#14135=ORIENTED_EDGE('',*,*,#10057,.F.);
#14136=ORIENTED_EDGE('',*,*,#10058,.F.);
#14137=ORIENTED_EDGE('',*,*,#10059,.T.);
#14138=ORIENTED_EDGE('',*,*,#10055,.T.);
#14139=ORIENTED_EDGE('',*,*,#10060,.F.);
#14140=ORIENTED_EDGE('',*,*,#10061,.F.);
#14141=ORIENTED_EDGE('',*,*,#10062,.T.);
#14142=ORIENTED_EDGE('',*,*,#10058,.T.);
#14143=ORIENTED_EDGE('',*,*,#10063,.F.);
#14144=ORIENTED_EDGE('',*,*,#10064,.F.);
#14145=ORIENTED_EDGE('',*,*,#10065,.T.);
#14146=ORIENTED_EDGE('',*,*,#10061,.T.);
#14147=ORIENTED_EDGE('',*,*,#10066,.F.);
#14148=ORIENTED_EDGE('',*,*,#10067,.F.);
#14149=ORIENTED_EDGE('',*,*,#10068,.T.);
#14150=ORIENTED_EDGE('',*,*,#10064,.T.);
#14151=ORIENTED_EDGE('',*,*,#10069,.F.);
#14152=ORIENTED_EDGE('',*,*,#10070,.F.);
#14153=ORIENTED_EDGE('',*,*,#10071,.T.);
#14154=ORIENTED_EDGE('',*,*,#10067,.T.);
#14155=ORIENTED_EDGE('',*,*,#10072,.F.);
#14156=ORIENTED_EDGE('',*,*,#10073,.F.);
#14157=ORIENTED_EDGE('',*,*,#10074,.T.);
#14158=ORIENTED_EDGE('',*,*,#10070,.T.);
#14159=ORIENTED_EDGE('',*,*,#10075,.F.);
#14160=ORIENTED_EDGE('',*,*,#10076,.F.);
#14161=ORIENTED_EDGE('',*,*,#10077,.T.);
#14162=ORIENTED_EDGE('',*,*,#10073,.T.);
#14163=ORIENTED_EDGE('',*,*,#10078,.F.);
#14164=ORIENTED_EDGE('',*,*,#10079,.F.);
#14165=ORIENTED_EDGE('',*,*,#10080,.F.);
#14166=ORIENTED_EDGE('',*,*,#9945,.F.);
#14167=ORIENTED_EDGE('',*,*,#9942,.F.);
#14168=ORIENTED_EDGE('',*,*,#9939,.F.);
#14169=ORIENTED_EDGE('',*,*,#9936,.F.);
#14170=ORIENTED_EDGE('',*,*,#9933,.F.);
#14171=ORIENTED_EDGE('',*,*,#9930,.F.);
#14172=ORIENTED_EDGE('',*,*,#9927,.F.);
#14173=ORIENTED_EDGE('',*,*,#9924,.F.);
#14174=ORIENTED_EDGE('',*,*,#9921,.F.);
#14175=ORIENTED_EDGE('',*,*,#9918,.F.);
#14176=ORIENTED_EDGE('',*,*,#9915,.F.);
#14177=ORIENTED_EDGE('',*,*,#9912,.F.);
#14178=ORIENTED_EDGE('',*,*,#9909,.F.);
#14179=ORIENTED_EDGE('',*,*,#9906,.F.);
#14180=ORIENTED_EDGE('',*,*,#9903,.F.);
#14181=ORIENTED_EDGE('',*,*,#9900,.F.);
#14182=ORIENTED_EDGE('',*,*,#9897,.F.);
#14183=ORIENTED_EDGE('',*,*,#9894,.F.);
#14184=ORIENTED_EDGE('',*,*,#9891,.F.);
#14185=ORIENTED_EDGE('',*,*,#9888,.F.);
#14186=ORIENTED_EDGE('',*,*,#9885,.F.);
#14187=ORIENTED_EDGE('',*,*,#9882,.F.);
#14188=ORIENTED_EDGE('',*,*,#9879,.F.);
#14189=ORIENTED_EDGE('',*,*,#9876,.F.);
#14190=ORIENTED_EDGE('',*,*,#9873,.F.);
#14191=ORIENTED_EDGE('',*,*,#9870,.F.);
#14192=ORIENTED_EDGE('',*,*,#9867,.F.);
#14193=ORIENTED_EDGE('',*,*,#9864,.F.);
#14194=ORIENTED_EDGE('',*,*,#9861,.F.);
#14195=ORIENTED_EDGE('',*,*,#9858,.F.);
#14196=ORIENTED_EDGE('',*,*,#9855,.F.);
#14197=ORIENTED_EDGE('',*,*,#9852,.F.);
#14198=ORIENTED_EDGE('',*,*,#9849,.F.);
#14199=ORIENTED_EDGE('',*,*,#9846,.F.);
#14200=ORIENTED_EDGE('',*,*,#9843,.F.);
#14201=ORIENTED_EDGE('',*,*,#9840,.F.);
#14202=ORIENTED_EDGE('',*,*,#9837,.F.);
#14203=ORIENTED_EDGE('',*,*,#9834,.F.);
#14204=ORIENTED_EDGE('',*,*,#9831,.F.);
#14205=ORIENTED_EDGE('',*,*,#9828,.F.);
#14206=ORIENTED_EDGE('',*,*,#9825,.F.);
#14207=ORIENTED_EDGE('',*,*,#9822,.F.);
#14208=ORIENTED_EDGE('',*,*,#9819,.F.);
#14209=ORIENTED_EDGE('',*,*,#9816,.F.);
#14210=ORIENTED_EDGE('',*,*,#10081,.F.);
#14211=ORIENTED_EDGE('',*,*,#10082,.T.);
#14212=ORIENTED_EDGE('',*,*,#10078,.T.);
#14213=ORIENTED_EDGE('',*,*,#10075,.T.);
#14214=ORIENTED_EDGE('',*,*,#10072,.T.);
#14215=ORIENTED_EDGE('',*,*,#10069,.T.);
#14216=ORIENTED_EDGE('',*,*,#10066,.T.);
#14217=ORIENTED_EDGE('',*,*,#10063,.T.);
#14218=ORIENTED_EDGE('',*,*,#10060,.T.);
#14219=ORIENTED_EDGE('',*,*,#10057,.T.);
#14220=ORIENTED_EDGE('',*,*,#10054,.T.);
#14221=ORIENTED_EDGE('',*,*,#10051,.T.);
#14222=ORIENTED_EDGE('',*,*,#10048,.T.);
#14223=ORIENTED_EDGE('',*,*,#10045,.T.);
#14224=ORIENTED_EDGE('',*,*,#10042,.T.);
#14225=ORIENTED_EDGE('',*,*,#10039,.T.);
#14226=ORIENTED_EDGE('',*,*,#10036,.T.);
#14227=ORIENTED_EDGE('',*,*,#10033,.T.);
#14228=ORIENTED_EDGE('',*,*,#10030,.T.);
#14229=ORIENTED_EDGE('',*,*,#10027,.T.);
#14230=ORIENTED_EDGE('',*,*,#10024,.T.);
#14231=ORIENTED_EDGE('',*,*,#10021,.T.);
#14232=ORIENTED_EDGE('',*,*,#10018,.T.);
#14233=ORIENTED_EDGE('',*,*,#10015,.T.);
#14234=ORIENTED_EDGE('',*,*,#10012,.T.);
#14235=ORIENTED_EDGE('',*,*,#10009,.T.);
#14236=ORIENTED_EDGE('',*,*,#10006,.T.);
#14237=ORIENTED_EDGE('',*,*,#10003,.T.);
#14238=ORIENTED_EDGE('',*,*,#10000,.T.);
#14239=ORIENTED_EDGE('',*,*,#9997,.T.);
#14240=ORIENTED_EDGE('',*,*,#9994,.T.);
#14241=ORIENTED_EDGE('',*,*,#9991,.T.);
#14242=ORIENTED_EDGE('',*,*,#9988,.T.);
#14243=ORIENTED_EDGE('',*,*,#9985,.T.);
#14244=ORIENTED_EDGE('',*,*,#9982,.T.);
#14245=ORIENTED_EDGE('',*,*,#9979,.T.);
#14246=ORIENTED_EDGE('',*,*,#9976,.T.);
#14247=ORIENTED_EDGE('',*,*,#9973,.T.);
#14248=ORIENTED_EDGE('',*,*,#9970,.T.);
#14249=ORIENTED_EDGE('',*,*,#9967,.T.);
#14250=ORIENTED_EDGE('',*,*,#9964,.T.);
#14251=ORIENTED_EDGE('',*,*,#9961,.T.);
#14252=ORIENTED_EDGE('',*,*,#9958,.T.);
#14253=ORIENTED_EDGE('',*,*,#9955,.T.);
#14254=ORIENTED_EDGE('',*,*,#9952,.T.);
#14255=ORIENTED_EDGE('',*,*,#10083,.T.);
#14256=ORIENTED_EDGE('',*,*,#10084,.T.);
#14257=ORIENTED_EDGE('',*,*,#10085,.T.);
#14258=ORIENTED_EDGE('',*,*,#10086,.T.);
#14259=ORIENTED_EDGE('',*,*,#10081,.T.);
#14260=ORIENTED_EDGE('',*,*,#10076,.T.);
#14261=ORIENTED_EDGE('',*,*,#10082,.F.);
#14262=ORIENTED_EDGE('',*,*,#10086,.F.);
#14263=ORIENTED_EDGE('',*,*,#10087,.T.);
#14264=ORIENTED_EDGE('',*,*,#10088,.F.);
#14265=ORIENTED_EDGE('',*,*,#9947,.F.);
#14266=ORIENTED_EDGE('',*,*,#9950,.F.);
#14267=ORIENTED_EDGE('',*,*,#9954,.F.);
#14268=ORIENTED_EDGE('',*,*,#9957,.F.);
#14269=ORIENTED_EDGE('',*,*,#9960,.F.);
#14270=ORIENTED_EDGE('',*,*,#9963,.F.);
#14271=ORIENTED_EDGE('',*,*,#9966,.F.);
#14272=ORIENTED_EDGE('',*,*,#9969,.F.);
#14273=ORIENTED_EDGE('',*,*,#9972,.F.);
#14274=ORIENTED_EDGE('',*,*,#9975,.F.);
#14275=ORIENTED_EDGE('',*,*,#9978,.F.);
#14276=ORIENTED_EDGE('',*,*,#9981,.F.);
#14277=ORIENTED_EDGE('',*,*,#9984,.F.);
#14278=ORIENTED_EDGE('',*,*,#9987,.F.);
#14279=ORIENTED_EDGE('',*,*,#9990,.F.);
#14280=ORIENTED_EDGE('',*,*,#9993,.F.);
#14281=ORIENTED_EDGE('',*,*,#9996,.F.);
#14282=ORIENTED_EDGE('',*,*,#9999,.F.);
#14283=ORIENTED_EDGE('',*,*,#10002,.F.);
#14284=ORIENTED_EDGE('',*,*,#10005,.F.);
#14285=ORIENTED_EDGE('',*,*,#10008,.F.);
#14286=ORIENTED_EDGE('',*,*,#10011,.F.);
#14287=ORIENTED_EDGE('',*,*,#10014,.F.);
#14288=ORIENTED_EDGE('',*,*,#10017,.F.);
#14289=ORIENTED_EDGE('',*,*,#10020,.F.);
#14290=ORIENTED_EDGE('',*,*,#10023,.F.);
#14291=ORIENTED_EDGE('',*,*,#10026,.F.);
#14292=ORIENTED_EDGE('',*,*,#10029,.F.);
#14293=ORIENTED_EDGE('',*,*,#10032,.F.);
#14294=ORIENTED_EDGE('',*,*,#10035,.F.);
#14295=ORIENTED_EDGE('',*,*,#10038,.F.);
#14296=ORIENTED_EDGE('',*,*,#10041,.F.);
#14297=ORIENTED_EDGE('',*,*,#10044,.F.);
#14298=ORIENTED_EDGE('',*,*,#10047,.F.);
#14299=ORIENTED_EDGE('',*,*,#10050,.F.);
#14300=ORIENTED_EDGE('',*,*,#10053,.F.);
#14301=ORIENTED_EDGE('',*,*,#10056,.F.);
#14302=ORIENTED_EDGE('',*,*,#10059,.F.);
#14303=ORIENTED_EDGE('',*,*,#10062,.F.);
#14304=ORIENTED_EDGE('',*,*,#10065,.F.);
#14305=ORIENTED_EDGE('',*,*,#10068,.F.);
#14306=ORIENTED_EDGE('',*,*,#10071,.F.);
#14307=ORIENTED_EDGE('',*,*,#10074,.F.);
#14308=ORIENTED_EDGE('',*,*,#10077,.F.);
#14309=ORIENTED_EDGE('',*,*,#10087,.F.);
#14310=ORIENTED_EDGE('',*,*,#10085,.F.);
#14311=ORIENTED_EDGE('',*,*,#9814,.F.);
#14312=ORIENTED_EDGE('',*,*,#9818,.F.);
#14313=ORIENTED_EDGE('',*,*,#9821,.F.);
#14314=ORIENTED_EDGE('',*,*,#9824,.F.);
#14315=ORIENTED_EDGE('',*,*,#9827,.F.);
#14316=ORIENTED_EDGE('',*,*,#9830,.F.);
#14317=ORIENTED_EDGE('',*,*,#9833,.F.);
#14318=ORIENTED_EDGE('',*,*,#9836,.F.);
#14319=ORIENTED_EDGE('',*,*,#9839,.F.);
#14320=ORIENTED_EDGE('',*,*,#9842,.F.);
#14321=ORIENTED_EDGE('',*,*,#9845,.F.);
#14322=ORIENTED_EDGE('',*,*,#9848,.F.);
#14323=ORIENTED_EDGE('',*,*,#9851,.F.);
#14324=ORIENTED_EDGE('',*,*,#9854,.F.);
#14325=ORIENTED_EDGE('',*,*,#9857,.F.);
#14326=ORIENTED_EDGE('',*,*,#9860,.F.);
#14327=ORIENTED_EDGE('',*,*,#9863,.F.);
#14328=ORIENTED_EDGE('',*,*,#9866,.F.);
#14329=ORIENTED_EDGE('',*,*,#9869,.F.);
#14330=ORIENTED_EDGE('',*,*,#9872,.F.);
#14331=ORIENTED_EDGE('',*,*,#9875,.F.);
#14332=ORIENTED_EDGE('',*,*,#9878,.F.);
#14333=ORIENTED_EDGE('',*,*,#9881,.F.);
#14334=ORIENTED_EDGE('',*,*,#9884,.F.);
#14335=ORIENTED_EDGE('',*,*,#9887,.F.);
#14336=ORIENTED_EDGE('',*,*,#9890,.F.);
#14337=ORIENTED_EDGE('',*,*,#9893,.F.);
#14338=ORIENTED_EDGE('',*,*,#9896,.F.);
#14339=ORIENTED_EDGE('',*,*,#9899,.F.);
#14340=ORIENTED_EDGE('',*,*,#9902,.F.);
#14341=ORIENTED_EDGE('',*,*,#9905,.F.);
#14342=ORIENTED_EDGE('',*,*,#9908,.F.);
#14343=ORIENTED_EDGE('',*,*,#9911,.F.);
#14344=ORIENTED_EDGE('',*,*,#9914,.F.);
#14345=ORIENTED_EDGE('',*,*,#9917,.F.);
#14346=ORIENTED_EDGE('',*,*,#9920,.F.);
#14347=ORIENTED_EDGE('',*,*,#9923,.F.);
#14348=ORIENTED_EDGE('',*,*,#9926,.F.);
#14349=ORIENTED_EDGE('',*,*,#9929,.F.);
#14350=ORIENTED_EDGE('',*,*,#9932,.F.);
#14351=ORIENTED_EDGE('',*,*,#9935,.F.);
#14352=ORIENTED_EDGE('',*,*,#9938,.F.);
#14353=ORIENTED_EDGE('',*,*,#9941,.F.);
#14354=ORIENTED_EDGE('',*,*,#9944,.F.);
#14355=ORIENTED_EDGE('',*,*,#10089,.F.);
#14356=ORIENTED_EDGE('',*,*,#10090,.F.);
#14357=ORIENTED_EDGE('',*,*,#10091,.F.);
#14358=ORIENTED_EDGE('',*,*,#10092,.F.);
#14359=ORIENTED_EDGE('',*,*,#10093,.F.);
#14360=ORIENTED_EDGE('',*,*,#10094,.F.);
#14361=ORIENTED_EDGE('',*,*,#10095,.T.);
#14362=ORIENTED_EDGE('',*,*,#10096,.F.);
#14363=ORIENTED_EDGE('',*,*,#10095,.F.);
#14364=ORIENTED_EDGE('',*,*,#10097,.F.);
#14365=ORIENTED_EDGE('',*,*,#10098,.F.);
#14366=ORIENTED_EDGE('',*,*,#10093,.T.);
#14367=ORIENTED_EDGE('',*,*,#10099,.F.);
#14368=ORIENTED_EDGE('',*,*,#10100,.T.);
#14369=ORIENTED_EDGE('',*,*,#10101,.T.);
#14370=ORIENTED_EDGE('',*,*,#10092,.T.);
#14371=ORIENTED_EDGE('',*,*,#10102,.F.);
#14372=ORIENTED_EDGE('',*,*,#10103,.T.);
#14373=ORIENTED_EDGE('',*,*,#10099,.T.);
#14374=ORIENTED_EDGE('',*,*,#10091,.T.);
#14375=ORIENTED_EDGE('',*,*,#10104,.F.);
#14376=ORIENTED_EDGE('',*,*,#10105,.T.);
#14377=ORIENTED_EDGE('',*,*,#10102,.T.);
#14378=ORIENTED_EDGE('',*,*,#10105,.F.);
#14379=ORIENTED_EDGE('',*,*,#10106,.F.);
#14380=ORIENTED_EDGE('',*,*,#10107,.F.);
#14381=ORIENTED_EDGE('',*,*,#10108,.F.);
#14382=ORIENTED_EDGE('',*,*,#10100,.F.);
#14383=ORIENTED_EDGE('',*,*,#10103,.F.);
#14384=ORIENTED_EDGE('',*,*,#10109,.T.);
#14385=ORIENTED_EDGE('',*,*,#10079,.T.);
#14386=ORIENTED_EDGE('',*,*,#9951,.T.);
#14387=ORIENTED_EDGE('',*,*,#9948,.T.);
#14388=ORIENTED_EDGE('',*,*,#10088,.T.);
#14389=ORIENTED_EDGE('',*,*,#10090,.T.);
#14390=ORIENTED_EDGE('',*,*,#10110,.F.);
#14391=ORIENTED_EDGE('',*,*,#10106,.T.);
#14392=ORIENTED_EDGE('',*,*,#10104,.T.);
#14393=ORIENTED_EDGE('',*,*,#10098,.T.);
#14394=ORIENTED_EDGE('',*,*,#10111,.F.);
#14395=ORIENTED_EDGE('',*,*,#10107,.T.);
#14396=ORIENTED_EDGE('',*,*,#10110,.T.);
#14397=ORIENTED_EDGE('',*,*,#10097,.T.);
#14398=ORIENTED_EDGE('',*,*,#10094,.T.);
#14399=ORIENTED_EDGE('',*,*,#10101,.F.);
#14400=ORIENTED_EDGE('',*,*,#10108,.T.);
#14401=ORIENTED_EDGE('',*,*,#10111,.T.);
#14402=ORIENTED_EDGE('',*,*,#10096,.T.);
#14403=ORIENTED_EDGE('',*,*,#10112,.F.);
#14404=ORIENTED_EDGE('',*,*,#10083,.F.);
#14405=ORIENTED_EDGE('',*,*,#9815,.F.);
#14406=ORIENTED_EDGE('',*,*,#10084,.F.);
#14407=ORIENTED_EDGE('',*,*,#10113,.T.);
#14408=ORIENTED_EDGE('',*,*,#10112,.T.);
#14409=ORIENTED_EDGE('',*,*,#10113,.F.);
#14410=ORIENTED_EDGE('',*,*,#9943,.T.);
#14411=ORIENTED_EDGE('',*,*,#10080,.T.);
#14412=ORIENTED_EDGE('',*,*,#10109,.F.);
#14413=ORIENTED_EDGE('',*,*,#10089,.T.);
#15936=PLANE('',#18467);
#15937=PLANE('',#18474);
#15938=PLANE('',#18475);
#15939=PLANE('',#18476);
#15940=PLANE('',#18477);
#15941=PLANE('',#18479);
#15942=PLANE('',#18480);
#15943=PLANE('',#18481);
#15944=PLANE('',#18482);
#15945=PLANE('',#18483);
#16616=ADVANCED_FACE('',(#2445),#1492,.T.);
#16617=ADVANCED_FACE('',(#2446),#1493,.T.);
#16618=ADVANCED_FACE('',(#2447),#1494,.T.);
#16619=ADVANCED_FACE('',(#2448),#1495,.T.);
#16620=ADVANCED_FACE('',(#2449),#1496,.T.);
#16621=ADVANCED_FACE('',(#2450),#1497,.T.);
#16622=ADVANCED_FACE('',(#2451),#1498,.T.);
#16623=ADVANCED_FACE('',(#2452),#1499,.T.);
#16624=ADVANCED_FACE('',(#2453),#1500,.T.);
#16625=ADVANCED_FACE('',(#2454),#1501,.T.);
#16626=ADVANCED_FACE('',(#2455),#1502,.T.);
#16627=ADVANCED_FACE('',(#2456),#1503,.T.);
#16628=ADVANCED_FACE('',(#2457),#1504,.T.);
#16629=ADVANCED_FACE('',(#2458),#1505,.T.);
#16630=ADVANCED_FACE('',(#2459),#1506,.T.);
#16631=ADVANCED_FACE('',(#2460),#1507,.T.);
#16632=ADVANCED_FACE('',(#2461),#1508,.T.);
#16633=ADVANCED_FACE('',(#2462),#1509,.T.);
#16634=ADVANCED_FACE('',(#2463),#1510,.T.);
#16635=ADVANCED_FACE('',(#2464),#1511,.T.);
#16636=ADVANCED_FACE('',(#2465),#1512,.T.);
#16637=ADVANCED_FACE('',(#2466),#1513,.T.);
#16638=ADVANCED_FACE('',(#2467),#1514,.T.);
#16639=ADVANCED_FACE('',(#2468),#1515,.T.);
#16640=ADVANCED_FACE('',(#2469),#1516,.T.);
#16641=ADVANCED_FACE('',(#2470),#1517,.T.);
#16642=ADVANCED_FACE('',(#2471),#1518,.T.);
#16643=ADVANCED_FACE('',(#2472),#1519,.T.);
#16644=ADVANCED_FACE('',(#2473),#1520,.T.);
#16645=ADVANCED_FACE('',(#2474),#1521,.T.);
#16646=ADVANCED_FACE('',(#2475),#1522,.T.);
#16647=ADVANCED_FACE('',(#2476),#1523,.T.);
#16648=ADVANCED_FACE('',(#2477),#1524,.T.);
#16649=ADVANCED_FACE('',(#2478),#1525,.T.);
#16650=ADVANCED_FACE('',(#2479),#1526,.T.);
#16651=ADVANCED_FACE('',(#2480),#1527,.T.);
#16652=ADVANCED_FACE('',(#2481),#1528,.T.);
#16653=ADVANCED_FACE('',(#2482),#1529,.T.);
#16654=ADVANCED_FACE('',(#2483),#1530,.T.);
#16655=ADVANCED_FACE('',(#2484),#1531,.T.);
#16656=ADVANCED_FACE('',(#2485),#1532,.T.);
#16657=ADVANCED_FACE('',(#2486),#1533,.T.);
#16658=ADVANCED_FACE('',(#2487),#1534,.T.);
#16659=ADVANCED_FACE('',(#2488),#1535,.T.);
#16660=ADVANCED_FACE('',(#2489),#1536,.T.);
#16661=ADVANCED_FACE('',(#2490),#1537,.T.);
#16662=ADVANCED_FACE('',(#2491),#1538,.T.);
#16663=ADVANCED_FACE('',(#2492),#1539,.T.);
#16664=ADVANCED_FACE('',(#2493),#1540,.T.);
#16665=ADVANCED_FACE('',(#2494),#1541,.T.);
#16666=ADVANCED_FACE('',(#2495),#1542,.T.);
#16667=ADVANCED_FACE('',(#2496),#1543,.T.);
#16668=ADVANCED_FACE('',(#2497),#1544,.T.);
#16669=ADVANCED_FACE('',(#2498),#1545,.T.);
#16670=ADVANCED_FACE('',(#2499),#1546,.T.);
#16671=ADVANCED_FACE('',(#2500),#1547,.T.);
#16672=ADVANCED_FACE('',(#2501),#1548,.T.);
#16673=ADVANCED_FACE('',(#2502),#1549,.T.);
#16674=ADVANCED_FACE('',(#2503),#1550,.T.);
#16675=ADVANCED_FACE('',(#2504),#1551,.T.);
#16676=ADVANCED_FACE('',(#2505),#1552,.T.);
#16677=ADVANCED_FACE('',(#2506),#1553,.T.);
#16678=ADVANCED_FACE('',(#2507),#1554,.T.);
#16679=ADVANCED_FACE('',(#2508),#1555,.T.);
#16680=ADVANCED_FACE('',(#2509),#1556,.T.);
#16681=ADVANCED_FACE('',(#2510),#1557,.T.);
#16682=ADVANCED_FACE('',(#2511),#1558,.T.);
#16683=ADVANCED_FACE('',(#2512),#1559,.T.);
#16684=ADVANCED_FACE('',(#2513),#1560,.T.);
#16685=ADVANCED_FACE('',(#2514),#1561,.T.);
#16686=ADVANCED_FACE('',(#2515),#1562,.T.);
#16687=ADVANCED_FACE('',(#2516),#1563,.T.);
#16688=ADVANCED_FACE('',(#2517),#1564,.T.);
#16689=ADVANCED_FACE('',(#2518),#1565,.T.);
#16690=ADVANCED_FACE('',(#2519),#1566,.T.);
#16691=ADVANCED_FACE('',(#2520),#1567,.T.);
#16692=ADVANCED_FACE('',(#2521),#1568,.T.);
#16693=ADVANCED_FACE('',(#2522),#1569,.T.);
#16694=ADVANCED_FACE('',(#2523),#1570,.T.);
#16695=ADVANCED_FACE('',(#2524),#1571,.T.);
#16696=ADVANCED_FACE('',(#2525),#1572,.T.);
#16697=ADVANCED_FACE('',(#2526),#1573,.T.);
#16698=ADVANCED_FACE('',(#2527),#1574,.T.);
#16699=ADVANCED_FACE('',(#2528),#1575,.T.);
#16700=ADVANCED_FACE('',(#2529),#1576,.T.);
#16701=ADVANCED_FACE('',(#2530),#1577,.T.);
#16702=ADVANCED_FACE('',(#2531),#1578,.T.);
#16703=ADVANCED_FACE('',(#2532),#1579,.T.);
#16704=ADVANCED_FACE('',(#2533),#357,.F.);
#16705=ADVANCED_FACE('',(#2534),#15936,.T.);
#16706=ADVANCED_FACE('',(#2535),#1580,.T.);
#16707=ADVANCED_FACE('',(#2536),#358,.F.);
#16708=ADVANCED_FACE('',(#2537),#648,.T.);
#16709=ADVANCED_FACE('',(#2538),#15937,.T.);
#16710=ADVANCED_FACE('',(#2539),#15938,.T.);
#16711=ADVANCED_FACE('',(#2540),#15939,.T.);
#16712=ADVANCED_FACE('',(#2541,#560),#15940,.F.);
#16713=ADVANCED_FACE('',(#2542),#15941,.T.);
#16714=ADVANCED_FACE('',(#2543),#15942,.T.);
#16715=ADVANCED_FACE('',(#2544),#15943,.T.);
#16716=ADVANCED_FACE('',(#2545),#15944,.T.);
#16717=ADVANCED_FACE('',(#2546),#15945,.T.);
#16718=ADVANCED_FACE('',(#2547),#649,.T.);
#16719=ADVANCED_FACE('',(#2548),#1581,.T.);
#16966=CLOSED_SHELL('',(#16616,#16617,#16618,#16619,#16620,#16621,#16622,
#16623,#16624,#16625,#16626,#16627,#16628,#16629,#16630,#16631,#16632,#16633,
#16634,#16635,#16636,#16637,#16638,#16639,#16640,#16641,#16642,#16643,#16644,
#16645,#16646,#16647,#16648,#16649,#16650,#16651,#16652,#16653,#16654,#16655,
#16656,#16657,#16658,#16659,#16660,#16661,#16662,#16663,#16664,#16665,#16666,
#16667,#16668,#16669,#16670,#16671,#16672,#16673,#16674,#16675,#16676,#16677,
#16678,#16679,#16680,#16681,#16682,#16683,#16684,#16685,#16686,#16687,#16688,
#16689,#16690,#16691,#16692,#16693,#16694,#16695,#16696,#16697,#16698,#16699,
#16700,#16701,#16702,#16703,#16704,#16705,#16706,#16707,#16708,#16709,#16710,
#16711,#16712,#16713,#16714,#16715,#16716,#16717,#16718,#16719));
#18375=AXIS2_PLACEMENT_3D('',#38392,#21798,#21799);
#18376=AXIS2_PLACEMENT_3D('',#38393,#21800,#21801);
#18377=AXIS2_PLACEMENT_3D('',#38409,#21803,#21804);
#18378=AXIS2_PLACEMENT_3D('',#38417,#21805,#21806);
#18379=AXIS2_PLACEMENT_3D('',#38465,#21808,#21809);
#18380=AXIS2_PLACEMENT_3D('',#38513,#21811,#21812);
#18381=AXIS2_PLACEMENT_3D('',#38564,#21814,#21815);
#18382=AXIS2_PLACEMENT_3D('',#38615,#21817,#21818);
#18383=AXIS2_PLACEMENT_3D('',#38663,#21820,#21821);
#18384=AXIS2_PLACEMENT_3D('',#38711,#21823,#21824);
#18385=AXIS2_PLACEMENT_3D('',#38765,#21826,#21827);
#18386=AXIS2_PLACEMENT_3D('',#38813,#21829,#21830);
#18387=AXIS2_PLACEMENT_3D('',#38861,#21832,#21833);
#18388=AXIS2_PLACEMENT_3D('',#38915,#21835,#21836);
#18389=AXIS2_PLACEMENT_3D('',#38963,#21838,#21839);
#18390=AXIS2_PLACEMENT_3D('',#39011,#21841,#21842);
#18391=AXIS2_PLACEMENT_3D('',#39059,#21844,#21845);
#18392=AXIS2_PLACEMENT_3D('',#39113,#21847,#21848);
#18393=AXIS2_PLACEMENT_3D('',#39161,#21850,#21851);
#18394=AXIS2_PLACEMENT_3D('',#39209,#21853,#21854);
#18395=AXIS2_PLACEMENT_3D('',#39263,#21856,#21857);
#18396=AXIS2_PLACEMENT_3D('',#39311,#21859,#21860);
#18397=AXIS2_PLACEMENT_3D('',#39359,#21862,#21863);
#18398=AXIS2_PLACEMENT_3D('',#39413,#21865,#21866);
#18399=AXIS2_PLACEMENT_3D('',#39461,#21868,#21869);
#18400=AXIS2_PLACEMENT_3D('',#39509,#21871,#21872);
#18401=AXIS2_PLACEMENT_3D('',#39557,#21874,#21875);
#18402=AXIS2_PLACEMENT_3D('',#39611,#21877,#21878);
#18403=AXIS2_PLACEMENT_3D('',#39659,#21880,#21881);
#18404=AXIS2_PLACEMENT_3D('',#39707,#21883,#21884);
#18405=AXIS2_PLACEMENT_3D('',#39761,#21886,#21887);
#18406=AXIS2_PLACEMENT_3D('',#39809,#21889,#21890);
#18407=AXIS2_PLACEMENT_3D('',#39857,#21892,#21893);
#18408=AXIS2_PLACEMENT_3D('',#39911,#21895,#21896);
#18409=AXIS2_PLACEMENT_3D('',#39959,#21898,#21899);
#18410=AXIS2_PLACEMENT_3D('',#40007,#21901,#21902);
#18411=AXIS2_PLACEMENT_3D('',#40055,#21904,#21905);
#18412=AXIS2_PLACEMENT_3D('',#40109,#21907,#21908);
#18413=AXIS2_PLACEMENT_3D('',#40157,#21910,#21911);
#18414=AXIS2_PLACEMENT_3D('',#40205,#21913,#21914);
#18415=AXIS2_PLACEMENT_3D('',#40259,#21916,#21917);
#18416=AXIS2_PLACEMENT_3D('',#40307,#21919,#21920);
#18417=AXIS2_PLACEMENT_3D('',#40355,#21922,#21923);
#18418=AXIS2_PLACEMENT_3D('',#40409,#21925,#21926);
#18419=AXIS2_PLACEMENT_3D('',#40457,#21928,#21929);
#18420=AXIS2_PLACEMENT_3D('',#40505,#21931,#21932);
#18421=AXIS2_PLACEMENT_3D('',#40553,#21934,#21935);
#18422=AXIS2_PLACEMENT_3D('',#40562,#21937,#21938);
#18423=AXIS2_PLACEMENT_3D('',#40563,#21939,#21940);
#18424=AXIS2_PLACEMENT_3D('',#40578,#21942,#21943);
#18425=AXIS2_PLACEMENT_3D('',#40588,#21944,#21945);
#18426=AXIS2_PLACEMENT_3D('',#40612,#21947,#21948);
#18427=AXIS2_PLACEMENT_3D('',#40636,#21950,#21951);
#18428=AXIS2_PLACEMENT_3D('',#40661,#21953,#21954);
#18429=AXIS2_PLACEMENT_3D('',#40686,#21956,#21957);
#18430=AXIS2_PLACEMENT_3D('',#40710,#21959,#21960);
#18431=AXIS2_PLACEMENT_3D('',#40735,#21962,#21963);
#18432=AXIS2_PLACEMENT_3D('',#40760,#21965,#21966);
#18433=AXIS2_PLACEMENT_3D('',#40784,#21968,#21969);
#18434=AXIS2_PLACEMENT_3D('',#40809,#21971,#21972);
#18435=AXIS2_PLACEMENT_3D('',#40834,#21974,#21975);
#18436=AXIS2_PLACEMENT_3D('',#40858,#21977,#21978);
#18437=AXIS2_PLACEMENT_3D('',#40882,#21980,#21981);
#18438=AXIS2_PLACEMENT_3D('',#40907,#21983,#21984);
#18439=AXIS2_PLACEMENT_3D('',#40932,#21986,#21987);
#18440=AXIS2_PLACEMENT_3D('',#40956,#21989,#21990);
#18441=AXIS2_PLACEMENT_3D('',#40981,#21992,#21993);
#18442=AXIS2_PLACEMENT_3D('',#41006,#21995,#21996);
#18443=AXIS2_PLACEMENT_3D('',#41030,#21998,#21999);
#18444=AXIS2_PLACEMENT_3D('',#41055,#22001,#22002);
#18445=AXIS2_PLACEMENT_3D('',#41080,#22004,#22005);
#18446=AXIS2_PLACEMENT_3D('',#41104,#22007,#22008);
#18447=AXIS2_PLACEMENT_3D('',#41128,#22010,#22011);
#18448=AXIS2_PLACEMENT_3D('',#41153,#22013,#22014);
#18449=AXIS2_PLACEMENT_3D('',#41178,#22016,#22017);
#18450=AXIS2_PLACEMENT_3D('',#41202,#22019,#22020);
#18451=AXIS2_PLACEMENT_3D('',#41227,#22022,#22023);
#18452=AXIS2_PLACEMENT_3D('',#41252,#22025,#22026);
#18453=AXIS2_PLACEMENT_3D('',#41276,#22028,#22029);
#18454=AXIS2_PLACEMENT_3D('',#41301,#22031,#22032);
#18455=AXIS2_PLACEMENT_3D('',#41326,#22034,#22035);
#18456=AXIS2_PLACEMENT_3D('',#41350,#22037,#22038);
#18457=AXIS2_PLACEMENT_3D('',#41374,#22040,#22041);
#18458=AXIS2_PLACEMENT_3D('',#41399,#22043,#22044);
#18459=AXIS2_PLACEMENT_3D('',#41424,#22046,#22047);
#18460=AXIS2_PLACEMENT_3D('',#41448,#22049,#22050);
#18461=AXIS2_PLACEMENT_3D('',#41473,#22052,#22053);
#18462=AXIS2_PLACEMENT_3D('',#41498,#22055,#22056);
#18463=AXIS2_PLACEMENT_3D('',#41522,#22058,#22059);
#18464=AXIS2_PLACEMENT_3D('',#41547,#22061,#22062);
#18465=AXIS2_PLACEMENT_3D('',#41571,#22064,#22065);
#18466=AXIS2_PLACEMENT_3D('',#41596,#22067,#22068);
#18467=AXIS2_PLACEMENT_3D('',#42961,#22070,#22071);
#18468=AXIS2_PLACEMENT_3D('',#42963,#22072,#22073);
#18469=AXIS2_PLACEMENT_3D('',#42964,#22074,#22075);
#18470=AXIS2_PLACEMENT_3D('',#43063,#22076,#22077);
#18471=AXIS2_PLACEMENT_3D('',#43064,#22078,#22079);
#18472=AXIS2_PLACEMENT_3D('',#44304,#22080,#22081);
#18473=AXIS2_PLACEMENT_3D('',#44328,#22083,#22084);
#18474=AXIS2_PLACEMENT_3D('',#44336,#22085,#22086);
#18475=AXIS2_PLACEMENT_3D('',#44342,#22090,#22091);
#18476=AXIS2_PLACEMENT_3D('',#44346,#22094,#22095);
#18477=AXIS2_PLACEMENT_3D('',#44350,#22098,#22099);
#18478=AXIS2_PLACEMENT_3D('',#44356,#22103,#22104);
#18479=AXIS2_PLACEMENT_3D('',#44357,#22105,#22106);
#18480=AXIS2_PLACEMENT_3D('',#44359,#22108,#22109);
#18481=AXIS2_PLACEMENT_3D('',#44361,#22111,#22112);
#18482=AXIS2_PLACEMENT_3D('',#44362,#22113,#22114);
#18483=AXIS2_PLACEMENT_3D('',#44363,#22115,#22116);
#18484=AXIS2_PLACEMENT_3D('',#44365,#22117,#22118);
#18485=AXIS2_PLACEMENT_3D('',#44366,#22119,#22120);
#18486=AXIS2_PLACEMENT_3D('',#44368,#22122,#22123);
#21798=DIRECTION('axis',(0.,0.,1.));
#21799=DIRECTION('refdir',(1.,0.,0.));
#21800=DIRECTION('center_axis',(1.,0.,0.));
#21801=DIRECTION('ref_axis',(0.,1.,0.));
#21802=DIRECTION('',(-1.,0.,0.));
#21803=DIRECTION('center_axis',(1.,0.,0.));
#21804=DIRECTION('ref_axis',(0.,1.,0.));
#21805=DIRECTION('center_axis',(1.,0.,0.));
#21806=DIRECTION('ref_axis',(0.,1.,0.));
#21807=DIRECTION('',(-1.,0.,0.));
#21808=DIRECTION('center_axis',(1.,0.,0.));
#21809=DIRECTION('ref_axis',(0.,1.,0.));
#21810=DIRECTION('',(-1.,0.,0.));
#21811=DIRECTION('center_axis',(1.,0.,0.));
#21812=DIRECTION('ref_axis',(0.,1.,0.));
#21813=DIRECTION('',(-1.,0.,0.));
#21814=DIRECTION('center_axis',(1.,0.,0.));
#21815=DIRECTION('ref_axis',(0.,1.,0.));
#21816=DIRECTION('',(-1.,0.,0.));
#21817=DIRECTION('center_axis',(1.,0.,0.));
#21818=DIRECTION('ref_axis',(0.,1.,0.));
#21819=DIRECTION('',(-1.,0.,0.));
#21820=DIRECTION('center_axis',(1.,0.,0.));
#21821=DIRECTION('ref_axis',(0.,1.,0.));
#21822=DIRECTION('',(-1.,0.,0.));
#21823=DIRECTION('center_axis',(1.,0.,0.));
#21824=DIRECTION('ref_axis',(0.,1.,0.));
#21825=DIRECTION('',(-1.,0.,0.));
#21826=DIRECTION('center_axis',(1.,0.,0.));
#21827=DIRECTION('ref_axis',(0.,1.,0.));
#21828=DIRECTION('',(-1.,0.,0.));
#21829=DIRECTION('center_axis',(1.,0.,0.));
#21830=DIRECTION('ref_axis',(0.,1.,0.));
#21831=DIRECTION('',(-1.,0.,0.));
#21832=DIRECTION('center_axis',(1.,0.,0.));
#21833=DIRECTION('ref_axis',(0.,1.,0.));
#21834=DIRECTION('',(-1.,0.,0.));
#21835=DIRECTION('center_axis',(1.,0.,0.));
#21836=DIRECTION('ref_axis',(0.,1.,0.));
#21837=DIRECTION('',(-1.,0.,0.));
#21838=DIRECTION('center_axis',(1.,0.,0.));
#21839=DIRECTION('ref_axis',(0.,1.,0.));
#21840=DIRECTION('',(-1.,0.,0.));
#21841=DIRECTION('center_axis',(1.,0.,0.));
#21842=DIRECTION('ref_axis',(0.,1.,0.));
#21843=DIRECTION('',(-1.,0.,0.));
#21844=DIRECTION('center_axis',(1.,0.,0.));
#21845=DIRECTION('ref_axis',(0.,1.,0.));
#21846=DIRECTION('',(-1.,0.,0.));
#21847=DIRECTION('center_axis',(1.,0.,0.));
#21848=DIRECTION('ref_axis',(0.,1.,0.));
#21849=DIRECTION('',(-1.,0.,0.));
#21850=DIRECTION('center_axis',(1.,0.,0.));
#21851=DIRECTION('ref_axis',(0.,1.,0.));
#21852=DIRECTION('',(-1.,0.,0.));
#21853=DIRECTION('center_axis',(1.,0.,0.));
#21854=DIRECTION('ref_axis',(0.,1.,0.));
#21855=DIRECTION('',(-1.,0.,0.));
#21856=DIRECTION('center_axis',(1.,0.,0.));
#21857=DIRECTION('ref_axis',(0.,1.,0.));
#21858=DIRECTION('',(-1.,0.,0.));
#21859=DIRECTION('center_axis',(1.,0.,0.));
#21860=DIRECTION('ref_axis',(0.,1.,0.));
#21861=DIRECTION('',(-1.,0.,0.));
#21862=DIRECTION('center_axis',(1.,0.,0.));
#21863=DIRECTION('ref_axis',(0.,1.,0.));
#21864=DIRECTION('',(-1.,0.,0.));
#21865=DIRECTION('center_axis',(1.,0.,0.));
#21866=DIRECTION('ref_axis',(0.,1.,0.));
#21867=DIRECTION('',(-1.,0.,0.));
#21868=DIRECTION('center_axis',(1.,0.,0.));
#21869=DIRECTION('ref_axis',(0.,1.,0.));
#21870=DIRECTION('',(-1.,0.,0.));
#21871=DIRECTION('center_axis',(1.,0.,0.));
#21872=DIRECTION('ref_axis',(0.,1.,0.));
#21873=DIRECTION('',(-1.,0.,0.));
#21874=DIRECTION('center_axis',(1.,0.,0.));
#21875=DIRECTION('ref_axis',(0.,1.,0.));
#21876=DIRECTION('',(-1.,0.,0.));
#21877=DIRECTION('center_axis',(1.,0.,0.));
#21878=DIRECTION('ref_axis',(0.,1.,0.));
#21879=DIRECTION('',(-1.,0.,0.));
#21880=DIRECTION('center_axis',(1.,0.,0.));
#21881=DIRECTION('ref_axis',(0.,1.,0.));
#21882=DIRECTION('',(-1.,0.,0.));
#21883=DIRECTION('center_axis',(1.,0.,0.));
#21884=DIRECTION('ref_axis',(0.,1.,0.));
#21885=DIRECTION('',(-1.,0.,0.));
#21886=DIRECTION('center_axis',(1.,0.,0.));
#21887=DIRECTION('ref_axis',(0.,1.,0.));
#21888=DIRECTION('',(-1.,0.,0.));
#21889=DIRECTION('center_axis',(1.,0.,0.));
#21890=DIRECTION('ref_axis',(0.,1.,0.));
#21891=DIRECTION('',(-1.,0.,0.));
#21892=DIRECTION('center_axis',(1.,0.,0.));
#21893=DIRECTION('ref_axis',(0.,1.,0.));
#21894=DIRECTION('',(-1.,0.,0.));
#21895=DIRECTION('center_axis',(1.,0.,0.));
#21896=DIRECTION('ref_axis',(0.,1.,0.));
#21897=DIRECTION('',(-1.,0.,0.));
#21898=DIRECTION('center_axis',(1.,0.,0.));
#21899=DIRECTION('ref_axis',(0.,1.,0.));
#21900=DIRECTION('',(-1.,0.,0.));
#21901=DIRECTION('center_axis',(1.,0.,0.));
#21902=DIRECTION('ref_axis',(0.,1.,0.));
#21903=DIRECTION('',(-1.,0.,0.));
#21904=DIRECTION('center_axis',(1.,0.,0.));
#21905=DIRECTION('ref_axis',(0.,1.,0.));
#21906=DIRECTION('',(-1.,0.,0.));
#21907=DIRECTION('center_axis',(1.,0.,0.));
#21908=DIRECTION('ref_axis',(0.,1.,0.));
#21909=DIRECTION('',(-1.,0.,0.));
#21910=DIRECTION('center_axis',(1.,0.,0.));
#21911=DIRECTION('ref_axis',(0.,1.,0.));
#21912=DIRECTION('',(-1.,0.,0.));
#21913=DIRECTION('center_axis',(1.,0.,0.));
#21914=DIRECTION('ref_axis',(0.,1.,0.));
#21915=DIRECTION('',(-1.,0.,0.));
#21916=DIRECTION('center_axis',(1.,0.,0.));
#21917=DIRECTION('ref_axis',(0.,1.,0.));
#21918=DIRECTION('',(-1.,0.,0.));
#21919=DIRECTION('center_axis',(1.,0.,0.));
#21920=DIRECTION('ref_axis',(0.,1.,0.));
#21921=DIRECTION('',(-1.,0.,0.));
#21922=DIRECTION('center_axis',(1.,0.,0.));
#21923=DIRECTION('ref_axis',(0.,1.,0.));
#21924=DIRECTION('',(-1.,0.,0.));
#21925=DIRECTION('center_axis',(1.,0.,0.));
#21926=DIRECTION('ref_axis',(0.,1.,0.));
#21927=DIRECTION('',(-1.,0.,0.));
#21928=DIRECTION('center_axis',(1.,0.,0.));
#21929=DIRECTION('ref_axis',(0.,1.,0.));
#21930=DIRECTION('',(-1.,0.,0.));
#21931=DIRECTION('center_axis',(1.,0.,0.));
#21932=DIRECTION('ref_axis',(0.,1.,0.));
#21933=DIRECTION('',(-1.,0.,0.));
#21934=DIRECTION('center_axis',(1.,0.,0.));
#21935=DIRECTION('ref_axis',(0.,1.,-5.15647387410054E-13));
#21936=DIRECTION('',(1.,0.,0.));
#21937=DIRECTION('center_axis',(1.,0.,0.));
#21938=DIRECTION('ref_axis',(0.,1.,-5.15647387410054E-13));
#21939=DIRECTION('center_axis',(1.,0.,0.));
#21940=DIRECTION('ref_axis',(0.,1.,-5.15647387410054E-13));
#21941=DIRECTION('',(1.,0.,0.));
#21942=DIRECTION('center_axis',(1.,0.,0.));
#21943=DIRECTION('ref_axis',(0.,1.,-5.15647387410054E-13));
#21944=DIRECTION('center_axis',(1.,0.,0.));
#21945=DIRECTION('ref_axis',(0.,1.,-5.15647387410054E-13));
#21946=DIRECTION('',(1.,0.,0.));
#21947=DIRECTION('center_axis',(1.,0.,0.));
#21948=DIRECTION('ref_axis',(0.,1.,-5.15647387410054E-13));
#21949=DIRECTION('',(1.,0.,0.));
#21950=DIRECTION('center_axis',(1.,0.,0.));
#21951=DIRECTION('ref_axis',(0.,1.,-5.15647387410054E-13));
#21952=DIRECTION('',(1.,0.,0.));
#21953=DIRECTION('center_axis',(1.,0.,0.));
#21954=DIRECTION('ref_axis',(0.,1.,-5.15647387410054E-13));
#21955=DIRECTION('',(1.,0.,0.));
#21956=DIRECTION('center_axis',(1.,0.,0.));
#21957=DIRECTION('ref_axis',(0.,1.,-5.15647387410054E-13));
#21958=DIRECTION('',(1.,0.,0.));
#21959=DIRECTION('center_axis',(1.,0.,0.));
#21960=DIRECTION('ref_axis',(0.,1.,-5.15647387410054E-13));
#21961=DIRECTION('',(1.,0.,0.));
#21962=DIRECTION('center_axis',(1.,0.,0.));
#21963=DIRECTION('ref_axis',(0.,1.,-5.15647387410054E-13));
#21964=DIRECTION('',(1.,0.,0.));
#21965=DIRECTION('center_axis',(1.,0.,0.));
#21966=DIRECTION('ref_axis',(0.,1.,-5.15647387410054E-13));
#21967=DIRECTION('',(1.,0.,0.));
#21968=DIRECTION('center_axis',(1.,0.,0.));
#21969=DIRECTION('ref_axis',(0.,1.,-5.15647387410054E-13));
#21970=DIRECTION('',(1.,0.,0.));
#21971=DIRECTION('center_axis',(1.,0.,0.));
#21972=DIRECTION('ref_axis',(0.,1.,-5.15647387410054E-13));
#21973=DIRECTION('',(1.,0.,0.));
#21974=DIRECTION('center_axis',(1.,0.,0.));
#21975=DIRECTION('ref_axis',(0.,1.,-5.15647387410054E-13));
#21976=DIRECTION('',(1.,0.,0.));
#21977=DIRECTION('center_axis',(1.,0.,0.));
#21978=DIRECTION('ref_axis',(0.,1.,-5.15647387410054E-13));
#21979=DIRECTION('',(1.,0.,0.));
#21980=DIRECTION('center_axis',(1.,0.,0.));
#21981=DIRECTION('ref_axis',(0.,1.,-5.15647387410054E-13));
#21982=DIRECTION('',(1.,0.,0.));
#21983=DIRECTION('center_axis',(1.,0.,0.));
#21984=DIRECTION('ref_axis',(0.,1.,-5.15647387410054E-13));
#21985=DIRECTION('',(1.,0.,0.));
#21986=DIRECTION('center_axis',(1.,0.,0.));
#21987=DIRECTION('ref_axis',(0.,1.,-5.15647387410054E-13));
#21988=DIRECTION('',(1.,0.,0.));
#21989=DIRECTION('center_axis',(1.,0.,0.));
#21990=DIRECTION('ref_axis',(0.,1.,-5.15647387410054E-13));
#21991=DIRECTION('',(1.,0.,0.));
#21992=DIRECTION('center_axis',(1.,0.,0.));
#21993=DIRECTION('ref_axis',(0.,1.,-5.15647387410054E-13));
#21994=DIRECTION('',(1.,0.,0.));
#21995=DIRECTION('center_axis',(1.,0.,0.));
#21996=DIRECTION('ref_axis',(0.,1.,-5.15647387410054E-13));
#21997=DIRECTION('',(1.,0.,0.));
#21998=DIRECTION('center_axis',(1.,0.,0.));
#21999=DIRECTION('ref_axis',(0.,1.,-5.15647387410054E-13));
#22000=DIRECTION('',(1.,0.,0.));
#22001=DIRECTION('center_axis',(1.,0.,0.));
#22002=DIRECTION('ref_axis',(0.,1.,-5.15647387410054E-13));
#22003=DIRECTION('',(1.,0.,0.));
#22004=DIRECTION('center_axis',(1.,0.,0.));
#22005=DIRECTION('ref_axis',(0.,1.,-5.15647387410054E-13));
#22006=DIRECTION('',(1.,0.,0.));
#22007=DIRECTION('center_axis',(1.,0.,0.));
#22008=DIRECTION('ref_axis',(0.,1.,-5.15647387410054E-13));
#22009=DIRECTION('',(1.,0.,0.));
#22010=DIRECTION('center_axis',(1.,0.,0.));
#22011=DIRECTION('ref_axis',(0.,1.,-5.15647387410054E-13));
#22012=DIRECTION('',(1.,0.,0.));
#22013=DIRECTION('center_axis',(1.,0.,0.));
#22014=DIRECTION('ref_axis',(0.,1.,-5.15647387410054E-13));
#22015=DIRECTION('',(1.,0.,0.));
#22016=DIRECTION('center_axis',(1.,0.,0.));
#22017=DIRECTION('ref_axis',(0.,1.,-5.15647387410054E-13));
#22018=DIRECTION('',(1.,0.,0.));
#22019=DIRECTION('center_axis',(1.,0.,0.));
#22020=DIRECTION('ref_axis',(0.,1.,-5.15647387410054E-13));
#22021=DIRECTION('',(1.,0.,0.));
#22022=DIRECTION('center_axis',(1.,0.,0.));
#22023=DIRECTION('ref_axis',(0.,1.,-5.15647387410054E-13));
#22024=DIRECTION('',(1.,0.,0.));
#22025=DIRECTION('center_axis',(1.,0.,0.));
#22026=DIRECTION('ref_axis',(0.,1.,-5.15647387410054E-13));
#22027=DIRECTION('',(1.,0.,0.));
#22028=DIRECTION('center_axis',(1.,0.,0.));
#22029=DIRECTION('ref_axis',(0.,1.,-5.15647387410054E-13));
#22030=DIRECTION('',(1.,0.,0.));
#22031=DIRECTION('center_axis',(1.,0.,0.));
#22032=DIRECTION('ref_axis',(0.,1.,-5.15647387410054E-13));
#22033=DIRECTION('',(1.,0.,0.));
#22034=DIRECTION('center_axis',(1.,0.,0.));
#22035=DIRECTION('ref_axis',(0.,1.,-5.15647387410054E-13));
#22036=DIRECTION('',(1.,0.,0.));
#22037=DIRECTION('center_axis',(1.,0.,0.));
#22038=DIRECTION('ref_axis',(0.,1.,-5.15647387410054E-13));
#22039=DIRECTION('',(1.,0.,0.));
#22040=DIRECTION('center_axis',(1.,0.,0.));
#22041=DIRECTION('ref_axis',(0.,1.,-5.15647387410054E-13));
#22042=DIRECTION('',(1.,0.,0.));
#22043=DIRECTION('center_axis',(1.,0.,0.));
#22044=DIRECTION('ref_axis',(0.,1.,-5.15647387410054E-13));
#22045=DIRECTION('',(1.,0.,0.));
#22046=DIRECTION('center_axis',(1.,0.,0.));
#22047=DIRECTION('ref_axis',(0.,1.,-5.15647387410054E-13));
#22048=DIRECTION('',(1.,0.,0.));
#22049=DIRECTION('center_axis',(1.,0.,0.));
#22050=DIRECTION('ref_axis',(0.,1.,-5.15647387410054E-13));
#22051=DIRECTION('',(1.,0.,0.));
#22052=DIRECTION('center_axis',(1.,0.,0.));
#22053=DIRECTION('ref_axis',(0.,1.,-5.15647387410054E-13));
#22054=DIRECTION('',(1.,0.,0.));
#22055=DIRECTION('center_axis',(1.,0.,0.));
#22056=DIRECTION('ref_axis',(0.,1.,-5.15647387410054E-13));
#22057=DIRECTION('',(1.,0.,0.));
#22058=DIRECTION('center_axis',(1.,0.,0.));
#22059=DIRECTION('ref_axis',(0.,1.,-5.15647387410054E-13));
#22060=DIRECTION('',(1.,0.,0.));
#22061=DIRECTION('center_axis',(1.,0.,0.));
#22062=DIRECTION('ref_axis',(0.,1.,-5.15647387410054E-13));
#22063=DIRECTION('',(1.,0.,0.));
#22064=DIRECTION('center_axis',(1.,0.,0.));
#22065=DIRECTION('ref_axis',(0.,1.,-5.15647387410054E-13));
#22066=DIRECTION('',(1.,0.,0.));
#22067=DIRECTION('center_axis',(1.,0.,0.));
#22068=DIRECTION('ref_axis',(0.,1.,-5.15647387410054E-13));
#22069=DIRECTION('',(1.,0.,0.));
#22070=DIRECTION('center_axis',(1.,0.,0.));
#22071=DIRECTION('ref_axis',(0.,0.,-1.));
#22072=DIRECTION('center_axis',(1.,0.,0.));
#22073=DIRECTION('ref_axis',(0.,1.,0.));
#22074=DIRECTION('center_axis',(1.,0.,0.));
#22075=DIRECTION('ref_axis',(0.,1.,0.));
#22076=DIRECTION('center_axis',(-1.,0.,0.));
#22077=DIRECTION('ref_axis',(0.,1.,-5.15647387410054E-13));
#22078=DIRECTION('center_axis',(1.,0.,0.));
#22079=DIRECTION('ref_axis',(0.,1.,-5.15647387410054E-13));
#22080=DIRECTION('center_axis',(-1.,0.,0.));
#22081=DIRECTION('ref_axis',(0.,1.,0.));
#22082=DIRECTION('',(0.500490667348524,0.865741931465162,1.06022808525646E-16));
#22083=DIRECTION('center_axis',(1.,0.,0.));
#22084=DIRECTION('ref_axis',(0.,1.,0.));
#22085=DIRECTION('center_axis',(0.,-0.5,0.866025403784439));
#22086=DIRECTION('ref_axis',(0.,-0.866025403784439,-0.5));
#22087=DIRECTION('',(1.,0.,0.));
#22088=DIRECTION('',(0.,-0.866025403784439,-0.5));
#22089=DIRECTION('',(1.,0.,0.));
#22090=DIRECTION('center_axis',(0.,0.5,0.866025403784439));
#22091=DIRECTION('ref_axis',(0.,-0.866025403784439,0.5));
#22092=DIRECTION('',(1.,0.,0.));
#22093=DIRECTION('',(0.,-0.866025403784439,0.5));
#22094=DIRECTION('center_axis',(0.,1.,-4.43760619934668E-16));
#22095=DIRECTION('ref_axis',(0.,4.43760619934668E-16,1.));
#22096=DIRECTION('',(1.,0.,0.));
#22097=DIRECTION('',(0.,4.43760619934668E-16,1.));
#22098=DIRECTION('center_axis',(1.,0.,0.));
#22099=DIRECTION('ref_axis',(0.,0.,-1.));
#22100=DIRECTION('',(0.,0.866025403784439,0.5));
#22101=DIRECTION('',(0.,0.866025403784439,-0.5));
#22102=DIRECTION('',(0.,1.4792020664489E-16,-1.));
#22103=DIRECTION('center_axis',(-1.,0.,0.));
#22104=DIRECTION('ref_axis',(0.,1.,0.));
#22105=DIRECTION('center_axis',(0.,0.5,-0.866025403784439));
#22106=DIRECTION('ref_axis',(0.,0.866025403784439,0.5));
#22107=DIRECTION('',(1.,0.,0.));
#22108=DIRECTION('center_axis',(0.,-0.5,-0.866025403784439));
#22109=DIRECTION('ref_axis',(0.,0.866025403784439,-0.5));
#22110=DIRECTION('',(1.,0.,0.));
#22111=DIRECTION('center_axis',(0.,-1.,-1.4792020664489E-16));
#22112=DIRECTION('ref_axis',(0.,1.4792020664489E-16,-1.));
#22113=DIRECTION('center_axis',(1.,0.,0.));
#22114=DIRECTION('ref_axis',(0.,0.,-1.));
#22115=DIRECTION('center_axis',(-1.,0.,0.));
#22116=DIRECTION('ref_axis',(0.,0.,1.));
#22117=DIRECTION('center_axis',(1.,0.,0.));
#22118=DIRECTION('ref_axis',(0.,0.,-1.));
#22119=DIRECTION('center_axis',(1.,0.,0.));
#22120=DIRECTION('ref_axis',(0.,1.,0.));
#22121=DIRECTION('',(-0.707106781186546,0.707106781186549,8.65956056235495E-17));
#22122=DIRECTION('center_axis',(1.,0.,0.));
#22123=DIRECTION('ref_axis',(0.,1.,0.));
#38392=CARTESIAN_POINT('',(0.,0.,0.));
#38393=CARTESIAN_POINT('Origin',(-27.25,0.,0.));
#38394=CARTESIAN_POINT('',(-54.162836477965,-3.93774042332204,0.0025401470004769));
#38395=CARTESIAN_POINT('',(-54.3461635220349,-3.93688521119116,0.00404501750981942));
#38396=CARTESIAN_POINT('',(-27.25,-3.933,-4.81653586104654E-16));
#38397=CARTESIAN_POINT('',(-54.567,1.75074534075625,3.52552341725016));
#38398=CARTESIAN_POINT('Ctrl Pts',(-54.162836477965,-3.93774042332204,0.0025401470004769));
#38399=CARTESIAN_POINT('Ctrl Pts',(-54.1696144592364,-3.93866195343843,
0.136067499180593));
#38400=CARTESIAN_POINT('Ctrl Pts',(-54.1763924405079,-3.93246070603142,
0.26950274978779));
#38401=CARTESIAN_POINT('Ctrl Pts',(-54.1831704217794,-3.91885498293026,
0.402171763676285));
#38402=CARTESIAN_POINT('Ctrl Pts',(-54.2493281390221,-3.78605385147857,
1.69711176958284));
#38403=CARTESIAN_POINT('Ctrl Pts',(-54.3154858562649,-2.94782161396214,
2.91905170927145));
#38404=CARTESIAN_POINT('Ctrl Pts',(-54.3816435735076,-1.78754908268422,
3.51017407453822));
#38405=CARTESIAN_POINT('Ctrl Pts',(-54.4434290490051,-0.70395682709477,
4.06223025086027));
#38406=CARTESIAN_POINT('Ctrl Pts',(-54.5052145245025,0.660516179498767,
4.06409281016428));
#38407=CARTESIAN_POINT('Ctrl Pts',(-54.567,1.75279620618131,3.52818484004948));
#38408=CARTESIAN_POINT('',(-54.567,-1.74869447533071,3.52286199445108));
#38409=CARTESIAN_POINT('Origin',(-54.567,0.,0.));
#38410=CARTESIAN_POINT('Ctrl Pts',(-54.567,-1.74869447533071,3.52286199445108));
#38411=CARTESIAN_POINT('Ctrl Pts',(-54.5008422827573,-2.92020446772555,
2.9413424643865));
#38412=CARTESIAN_POINT('Ctrl Pts',(-54.4346845655146,-3.76871594031363,
1.73455576822158));
#38413=CARTESIAN_POINT('Ctrl Pts',(-54.3685268482719,-3.91414328439161,
0.442962886141297));
#38414=CARTESIAN_POINT('Ctrl Pts',(-54.3610724061929,-3.93052957700137,
0.297430290241746));
#38415=CARTESIAN_POINT('Ctrl Pts',(-54.3536179641139,-3.93798946516557,
0.150820989173826));
#38416=CARTESIAN_POINT('Ctrl Pts',(-54.3461635220349,-3.93688521119116,
0.00404501750981942));
#38417=CARTESIAN_POINT('Origin',(-27.25,0.,0.));
#38418=CARTESIAN_POINT('',(-52.912836477965,-3.92758587675543,0.00202738283172854));
#38419=CARTESIAN_POINT('',(-53.0961635220349,-3.92737769983192,0.00186527213366315));
#38420=CARTESIAN_POINT('',(-27.25,-3.933,-4.81653586104654E-16));
#38421=CARTESIAN_POINT('Ctrl Pts',(-52.912836477965,-3.92758587675543,0.00202738283172854));
#38422=CARTESIAN_POINT('Ctrl Pts',(-52.9393348224469,-3.93003459305733,
0.527558129595977));
#38423=CARTESIAN_POINT('Ctrl Pts',(-52.9658331669288,-3.83198391398178,
1.05221170696794));
#38424=CARTESIAN_POINT('Ctrl Pts',(-52.9923315114107,-3.62911428541967,
1.53259749559324));
#38425=CARTESIAN_POINT('Ctrl Pts',(-53.0584892286534,-3.122615038543,2.73196401424622));
#38426=CARTESIAN_POINT('Ctrl Pts',(-53.1246469458961,-1.96273954373826,
3.65539262418095));
#38427=CARTESIAN_POINT('Ctrl Pts',(-53.1908046631387,-0.680367641251685,
3.88025158114632));
#38428=CARTESIAN_POINT('Ctrl Pts',(-53.2569623803814,0.602004261234901,
4.10511053811169));
#38429=CARTESIAN_POINT('Ctrl Pts',(-53.3231200976241,2.00687257140333,3.63139984210768));
#38430=CARTESIAN_POINT('Ctrl Pts',(-53.3892778148669,2.891205608505,2.67588403906754));
#38431=CARTESIAN_POINT('Ctrl Pts',(-53.4554355321096,3.77553864560666,1.7203682360274));
#38432=CARTESIAN_POINT('Ctrl Pts',(-53.5215932493523,4.13933640964158,0.283047325951132));
#38433=CARTESIAN_POINT('Ctrl Pts',(-53.587750966595,3.81610600351479,-0.978094706542245));
#38434=CARTESIAN_POINT('Ctrl Pts',(-53.6539086838378,3.492875597388,-2.23923673903563));
#38435=CARTESIAN_POINT('Ctrl Pts',(-53.7200664010804,2.48261702109949,-3.32419989394611));
#38436=CARTESIAN_POINT('Ctrl Pts',(-53.7862241183231,1.24769529796077,-3.73659569433847));
#38437=CARTESIAN_POINT('Ctrl Pts',(-53.8523818355659,0.0127735748220346,
-4.14899149473083));
#38438=CARTESIAN_POINT('Ctrl Pts',(-53.9185395528086,-1.44681129516692,
-3.88881994060506));
#38439=CARTESIAN_POINT('Ctrl Pts',(-53.9846972700513,-2.46291871746792,
-3.07476412747992));
#38440=CARTESIAN_POINT('Ctrl Pts',(-54.0440770060226,-3.37492404306438,
-2.34410984761879));
#38441=CARTESIAN_POINT('Ctrl Pts',(-54.1034567419937,-3.92966719136564,
-1.16725047351599));
#38442=CARTESIAN_POINT('Ctrl Pts',(-54.162836477965,-3.93774042332204,0.0025401470004769));
#38443=CARTESIAN_POINT('Ctrl Pts',(-54.3461635220349,-3.93688521119116,
0.00404501750981942));
#38444=CARTESIAN_POINT('Ctrl Pts',(-54.2874602468712,-3.92818927872256,
-1.15180677672198));
#38445=CARTESIAN_POINT('Ctrl Pts',(-54.2287569717075,-3.38839097382246,
-2.31799459148723));
#38446=CARTESIAN_POINT('Ctrl Pts',(-54.1700536965438,-2.49440531842674,
-3.0500924315163));
#38447=CARTESIAN_POINT('Ctrl Pts',(-54.1038959793011,-1.48689679281598,
-3.87515579909798));
#38448=CARTESIAN_POINT('Ctrl Pts',(-54.0377382620583,-0.0295365260265515,
-4.1488834662657));
#38449=CARTESIAN_POINT('Ctrl Pts',(-53.9715805448156,1.20964880738629,-3.74878655245096));
#38450=CARTESIAN_POINT('Ctrl Pts',(-53.9054228275729,2.44883414079913,-3.34868963863622));
#38451=CARTESIAN_POINT('Ctrl Pts',(-53.8392651103302,3.46984454083539,-2.27476814383901));
#38452=CARTESIAN_POINT('Ctrl Pts',(-53.7731073930875,3.80585975657112,-1.01715165494543));
#38453=CARTESIAN_POINT('Ctrl Pts',(-53.7069496758448,4.14187497230684,0.240464833948156));
#38454=CARTESIAN_POINT('Ctrl Pts',(-53.640791958602,3.79289500374203,1.68177631693811));
#38455=CARTESIAN_POINT('Ctrl Pts',(-53.5746342413593,2.91838761167926,2.64634772696721));
#38456=CARTESIAN_POINT('Ctrl Pts',(-53.5084765241166,2.04388021961649,3.61091913699631));
#38457=CARTESIAN_POINT('Ctrl Pts',(-53.442318806874,0.643845404055756,4.09875047406455));
#38458=CARTESIAN_POINT('Ctrl Pts',(-53.3761610896313,-0.640770562895464,
3.88694001100651));
#38459=CARTESIAN_POINT('Ctrl Pts',(-53.3100033723886,-1.92538652984669,
3.67512954794847));
#38460=CARTESIAN_POINT('Ctrl Pts',(-53.2438456551458,-3.0945836481884,2.76367728476414));
#38461=CARTESIAN_POINT('Ctrl Pts',(-53.1776879379031,-3.61328184600827,
1.56956290603595));
#38462=CARTESIAN_POINT('Ctrl Pts',(-53.1505131326137,-3.82634123072092,
1.0790709863075));
#38463=CARTESIAN_POINT('Ctrl Pts',(-53.1233383273243,-3.92964710016084,
0.540887733301384));
#38464=CARTESIAN_POINT('Ctrl Pts',(-53.0961635220349,-3.92737769983192,
0.00186527213366315));
#38465=CARTESIAN_POINT('Origin',(-27.25,0.,0.));
#38466=CARTESIAN_POINT('',(-51.662836477965,-3.93040782112997,-0.00335227714350295));
#38467=CARTESIAN_POINT('',(-51.8461635220349,-3.93077288487519,-0.00342755369346778));
#38468=CARTESIAN_POINT('',(-27.25,-3.933,-4.81653586104654E-16));
#38469=CARTESIAN_POINT('Ctrl Pts',(-51.662836477965,-3.93040782112997,-0.00335227714350295));
#38470=CARTESIAN_POINT('Ctrl Pts',(-51.7090551856573,-3.92298924677534,
0.911627821618423));
#38471=CARTESIAN_POINT('Ctrl Pts',(-51.7552738933496,-3.6045908394272,1.83126267808616));
#38472=CARTESIAN_POINT('Ctrl Pts',(-51.8014926010419,-3.02075944544342,
2.52870136511396));
#38473=CARTESIAN_POINT('Ctrl Pts',(-51.8676503182846,-2.185059915769,3.52701901081092));
#38474=CARTESIAN_POINT('Ctrl Pts',(-51.9338080355273,-0.805508898715437,
4.07007403534115));
#38475=CARTESIAN_POINT('Ctrl Pts',(-51.99996575277,0.486460775265182,3.90930586499069));
#38476=CARTESIAN_POINT('Ctrl Pts',(-52.0661234700127,1.7784304492458,3.74853769464024));
#38477=CARTESIAN_POINT('Ctrl Pts',(-52.1322811872554,2.98281878015347,2.88394632940911));
#38478=CARTESIAN_POINT('Ctrl Pts',(-52.1984389044981,3.54836614375573,1.71126187008268));
#38479=CARTESIAN_POINT('Ctrl Pts',(-52.2645966217408,4.113913507358,0.538577410756249));
#38480=CARTESIAN_POINT('Ctrl Pts',(-52.3307543389835,4.04061990365484,-0.942200142665483));
#38481=CARTESIAN_POINT('Ctrl Pts',(-52.3969120562262,3.36203289749339,-2.05330331430663));
#38482=CARTESIAN_POINT('Ctrl Pts',(-52.463069773469,2.68344589133195,-3.16440648594777));
#38483=CARTESIAN_POINT('Ctrl Pts',(-52.5292274907117,1.39956548271222,-3.90583527580832));
#38484=CARTESIAN_POINT('Ctrl Pts',(-52.5953852079544,0.098034511021366,
-3.93823530609415));
#38485=CARTESIAN_POINT('Ctrl Pts',(-52.6615429251971,-1.2034964606695,-3.97063533637998));
#38486=CARTESIAN_POINT('Ctrl Pts',(-52.7277006424398,-2.5226779954315,-3.29400660709107));
#38487=CARTESIAN_POINT('Ctrl Pts',(-52.7938583596825,-3.25570726333821,
-2.218040028761));
#38488=CARTESIAN_POINT('Ctrl Pts',(-52.8335177324433,-3.69513416910437,
-1.57303349911237));
#38489=CARTESIAN_POINT('Ctrl Pts',(-52.8731771052042,-3.92392094770037,
-0.784520614438989));
#38490=CARTESIAN_POINT('Ctrl Pts',(-52.912836477965,-3.92758587675543,0.00202738283172854));
#38491=CARTESIAN_POINT('Ctrl Pts',(-53.0961635220349,-3.92737769983192,
0.00186527213366315));
#38492=CARTESIAN_POINT('Ctrl Pts',(-53.0571806100816,-3.92412219046333,
-0.771375416098045));
#38493=CARTESIAN_POINT('Ctrl Pts',(-53.0181976981283,-3.70360763326856,
-1.54634307662655));
#38494=CARTESIAN_POINT('Ctrl Pts',(-52.979214786175,-3.27816841217882,-2.18472795751501));
#38495=CARTESIAN_POINT('Ctrl Pts',(-52.9130570689323,-2.55615750323147,
-3.26812794806574));
#38496=CARTESIAN_POINT('Ctrl Pts',(-52.8468993516896,-1.24393640803873,
-3.95815143489514));
#38497=CARTESIAN_POINT('Ctrl Pts',(-52.7807416344468,0.0578597559599706,
-3.93902318709568));
#38498=CARTESIAN_POINT('Ctrl Pts',(-52.7145839172041,1.35965591995867,-3.91989493929621));
#38499=CARTESIAN_POINT('Ctrl Pts',(-52.6484261999614,2.65102715276333,-3.19161495686788));
#38500=CARTESIAN_POINT('Ctrl Pts',(-52.5822684827187,3.34091148436537,-2.08749493259359));
#38501=CARTESIAN_POINT('Ctrl Pts',(-52.516110765476,4.03079581596742,-0.983374908319293));
#38502=CARTESIAN_POINT('Ctrl Pts',(-52.4499530482333,4.11919324636686,0.496585157800968));
#38503=CARTESIAN_POINT('Ctrl Pts',(-52.3837953309906,3.5656380921564,1.67497922474918));
#38504=CARTESIAN_POINT('Ctrl Pts',(-52.3176376137479,3.01208293794595,2.8533732916974));
#38505=CARTESIAN_POINT('Ctrl Pts',(-52.2514798965051,1.81657519912561,3.73020135947356));
#38506=CARTESIAN_POINT('Ctrl Pts',(-52.1853221792624,0.526312366823295,
3.90413913807549));
#38507=CARTESIAN_POINT('Ctrl Pts',(-52.1191644620197,-0.763950465479025,
4.07807691667742));
#38508=CARTESIAN_POINT('Ctrl Pts',(-52.0530067447771,-2.14896839126332,
3.54912440610509));
#38509=CARTESIAN_POINT('Ctrl Pts',(-51.9868490275344,-2.99480768303467,
2.55938384971904));
#38510=CARTESIAN_POINT('Ctrl Pts',(-51.9399538590345,-3.59437153989906,
1.85781716789794));
#38511=CARTESIAN_POINT('Ctrl Pts',(-51.8930586905347,-3.92302364013206,
0.924726291586686));
#38512=CARTESIAN_POINT('Ctrl Pts',(-51.8461635220349,-3.93077288487519,
-0.00342755369346778));
#38513=CARTESIAN_POINT('Origin',(-27.25,0.,0.));
#38514=CARTESIAN_POINT('',(-50.412836477965,-3.9394544622989,-8.04257353526072E-5));
#38515=CARTESIAN_POINT('',(-50.5961635220349,-3.93944735561455,0.000168331762536079));
#38516=CARTESIAN_POINT('',(-27.25,-3.933,-4.81653586104654E-16));
#38517=CARTESIAN_POINT('Ctrl Pts',(-50.412836477965,-3.9394544622989,-8.04257353526072E-5));
#38518=CARTESIAN_POINT('Ctrl Pts',(-50.4787755488677,-3.93906386773341,
1.29755258648731));
#38519=CARTESIAN_POINT('Ctrl Pts',(-50.5447146197704,-3.23516481471532,
2.59554871145119));
#38520=CARTESIAN_POINT('Ctrl Pts',(-50.6106536906731,-2.14723319787632,
3.30283324761193));
#38521=CARTESIAN_POINT('Ctrl Pts',(-50.6768114079158,-1.05569412550357,
4.01246305756969));
#38522=CARTESIAN_POINT('Ctrl Pts',(-50.7429691251586,0.422428548377894,
4.12745732105086));
#38523=CARTESIAN_POINT('Ctrl Pts',(-50.8091268424013,1.61058474395983,3.59518213874312));
#38524=CARTESIAN_POINT('Ctrl Pts',(-50.875284559644,2.79874093954177,3.06290695643538));
#38525=CARTESIAN_POINT('Ctrl Pts',(-50.9414422768866,3.69693065682417,1.88336232833872));
#38526=CARTESIAN_POINT('Ctrl Pts',(-51.0075999941293,3.89404435502893,0.596436447717042));
#38527=CARTESIAN_POINT('Ctrl Pts',(-51.073757711372,4.09115805323369,-0.690489432904646));
#38528=CARTESIAN_POINT('Ctrl Pts',(-51.1399154286147,3.58719573236078,-2.08479656605136));
#38529=CARTESIAN_POINT('Ctrl Pts',(-51.2060731458575,2.61282550158419,-2.94829795308546));
#38530=CARTESIAN_POINT('Ctrl Pts',(-51.2722308631002,1.63845527080759,-3.81179934011955));
#38531=CARTESIAN_POINT('Ctrl Pts',(-51.3383885803429,0.193677130127309,
-4.14449498104103));
#38532=CARTESIAN_POINT('Ctrl Pts',(-51.4045462975856,-1.0602209484054,-3.79410716689309));
#38533=CARTESIAN_POINT('Ctrl Pts',(-51.4707040148283,-2.3141190269381,-3.44371935274515));
#38534=CARTESIAN_POINT('Ctrl Pts',(-51.536861732071,-3.37713704332323,-2.41024808352779));
#38535=CARTESIAN_POINT('Ctrl Pts',(-51.6030194493137,-3.76272203036817,
-1.16672231548726));
#38536=CARTESIAN_POINT('Ctrl Pts',(-51.6229584588641,-3.87893194600034,
-0.791941062467227));
#38537=CARTESIAN_POINT('Ctrl Pts',(-51.6428974684146,-3.93360823568704,
-0.398079820136163));
#38538=CARTESIAN_POINT('Ctrl Pts',(-51.662836477965,-3.93040782112997,-0.00335227714350295));
#38539=CARTESIAN_POINT('Ctrl Pts',(-51.8461635220349,-3.93077288487519,
-0.00342755369346778));
#38540=CARTESIAN_POINT('Ctrl Pts',(-51.826900973292,-3.93395594635807,-0.384673836787234));
#38541=CARTESIAN_POINT('Ctrl Pts',(-51.8076384245491,-3.88299568796656,
-0.765087134926914));
#38542=CARTESIAN_POINT('Ctrl Pts',(-51.7883758758062,-3.77442753736563,
-1.1282797903303));
#38543=CARTESIAN_POINT('Ctrl Pts',(-51.7222181585635,-3.40154744216686,
-2.37567427179388));
#38544=CARTESIAN_POINT('Ctrl Pts',(-51.6560604413208,-2.34912659401091,
-3.41993463252129));
#38545=CARTESIAN_POINT('Ctrl Pts',(-51.5899027240781,-1.09886791146382,
-3.78309460396163));
#38546=CARTESIAN_POINT('Ctrl Pts',(-51.5237450068354,0.151390771083265,
-4.14625457540197));
#38547=CARTESIAN_POINT('Ctrl Pts',(-51.4575872895927,1.59948728802148,-3.82831415755525));
#38548=CARTESIAN_POINT('Ctrl Pts',(-51.3914295723499,2.58261501047815,-2.97479696275541));
#38549=CARTESIAN_POINT('Ctrl Pts',(-51.3252718551072,3.56574273293481,-2.12127976795557));
#38550=CARTESIAN_POINT('Ctrl Pts',(-51.2591141378645,4.08390166090993,-0.732185796202606));
#38551=CARTESIAN_POINT('Ctrl Pts',(-51.1929564206218,3.8999256686853,0.556683804504271));
#38552=CARTESIAN_POINT('Ctrl Pts',(-51.1267987033791,3.71594967646068,1.84555340521114));
#38553=CARTESIAN_POINT('Ctrl Pts',(-51.0606409861364,2.82983876403635,3.03419863487192));
#38554=CARTESIAN_POINT('Ctrl Pts',(-50.9944832688937,1.64717394726657,3.5785660089322));
#38555=CARTESIAN_POINT('Ctrl Pts',(-50.928325551651,0.464509130496774,4.12293338299248));
#38556=CARTESIAN_POINT('Ctrl Pts',(-50.8621678344082,-1.01470959061848,
4.02302290145225));
#38557=CARTESIAN_POINT('Ctrl Pts',(-50.7960101171655,-2.11343049329063,
3.32456440936727));
#38558=CARTESIAN_POINT('Ctrl Pts',(-50.7298523999228,-3.21215139596279,
2.6261059172823));
#38559=CARTESIAN_POINT('Ctrl Pts',(-50.6636946826802,-3.93037448019184,
1.32909941465258));
#38560=CARTESIAN_POINT('Ctrl Pts',(-50.5975369654374,-3.9393625454203,0.0271965219255519));
#38561=CARTESIAN_POINT('Ctrl Pts',(-50.5970791509699,-3.93942474324798,
0.0181872936082175));
#38562=CARTESIAN_POINT('Ctrl Pts',(-50.5966213365024,-3.93945297790921,
0.00917783081723566));
#38563=CARTESIAN_POINT('Ctrl Pts',(-50.5961635220349,-3.93944735561455,
0.000168331762536079));
#38564=CARTESIAN_POINT('Origin',(-27.25,0.,0.));
#38565=CARTESIAN_POINT('',(-49.1628364779651,-3.93064273659572,0.00340251455877419));
#38566=CARTESIAN_POINT('',(-49.3461635220349,-3.93028113905034,0.00332252600905021));
#38567=CARTESIAN_POINT('',(-27.25,-3.933,-4.81653586104654E-16));
#38568=CARTESIAN_POINT('Ctrl Pts',(-49.1628364779651,-3.93064273659572,
0.00340251455877419));
#38569=CARTESIAN_POINT('Ctrl Pts',(-49.1823381948354,-3.93383376403491,
0.3894146749438));
#38570=CARTESIAN_POINT('Ctrl Pts',(-49.2018399117058,-3.8815753953419,0.774581617987376));
#38571=CARTESIAN_POINT('Ctrl Pts',(-49.2213416285762,-3.77033377843617,
1.14188486973955));
#38572=CARTESIAN_POINT('Ctrl Pts',(-49.2874993458189,-3.39295718714497,
2.38792617129552));
#38573=CARTESIAN_POINT('Ctrl Pts',(-49.3536570630616,-2.3367771868834,3.42838478771917));
#38574=CARTESIAN_POINT('Ctrl Pts',(-49.4198147803043,-1.08521689172491,
3.78703342403622));
#38575=CARTESIAN_POINT('Ctrl Pts',(-49.485972497547,0.16634340343358,4.14568206035329));
#38576=CARTESIAN_POINT('Ctrl Pts',(-49.5521302147897,1.61328399348899,3.82252071656374));
#38577=CARTESIAN_POINT('Ctrl Pts',(-49.6182879320324,2.59332711739344,2.96546325525251));
#38578=CARTESIAN_POINT('Ctrl Pts',(-49.6844456492752,3.57337024129788,2.10840579394128));
#38579=CARTESIAN_POINT('Ctrl Pts',(-49.7506033665179,4.08651589905138,0.717452215108368));
#38580=CARTESIAN_POINT('Ctrl Pts',(-49.8167610837606,3.89789269385868,-0.570745480739336));
#38581=CARTESIAN_POINT('Ctrl Pts',(-49.8829188010033,3.70926948866598,-1.85894317658704));
#38582=CARTESIAN_POINT('Ctrl Pts',(-49.949076518246,2.81887742052708,-3.04438498944954));
#38583=CARTESIAN_POINT('Ctrl Pts',(-50.0152342354887,1.63425697154039,-3.58448350663335));
#38584=CARTESIAN_POINT('Ctrl Pts',(-50.0813919527314,0.449636522553694,
-4.12458202381717));
#38585=CARTESIAN_POINT('Ctrl Pts',(-50.1475496699741,-1.0292123072808,-4.0193372453223));
#38586=CARTESIAN_POINT('Ctrl Pts',(-50.2137073872168,-2.12540706800835,
-3.31692065747272));
#38587=CARTESIAN_POINT('Ctrl Pts',(-50.2798651044595,-3.22160182873591,
-2.61450406962314));
#38588=CARTESIAN_POINT('Ctrl Pts',(-50.3460228217023,-3.93514252035653,
-1.31491567241883));
#38589=CARTESIAN_POINT('Ctrl Pts',(-50.412180538945,-3.93943513073482,-0.0129887955995017));
#38590=CARTESIAN_POINT('Ctrl Pts',(-50.412399185285,-3.93944931749318,-0.00868602400368631));
#38591=CARTESIAN_POINT('Ctrl Pts',(-50.412617831625,-3.93945575746534,-0.00438322686574803));
#38592=CARTESIAN_POINT('Ctrl Pts',(-50.412836477965,-3.9394544622989,-8.04257353526072E-5));
#38593=CARTESIAN_POINT('Ctrl Pts',(-50.5961635220349,-3.93944735561455,
0.000168331762536079));
#38594=CARTESIAN_POINT('Ctrl Pts',(-50.5304636192597,-3.93864051302073,
-1.29276418554459));
#38595=CARTESIAN_POINT('Ctrl Pts',(-50.4647637164844,-3.24056791593096,
-2.58644353485226));
#38596=CARTESIAN_POINT('Ctrl Pts',(-50.3990638137092,-2.15913104008258,
-3.29506752887434));
#38597=CARTESIAN_POINT('Ctrl Pts',(-50.3329060964666,-1.07015842328851,
-4.00862940412288));
#38598=CARTESIAN_POINT('Ctrl Pts',(-50.2667483792239,0.407539856527492,
-4.12895387179563));
#38599=CARTESIAN_POINT('Ctrl Pts',(-50.2005906619812,1.59760797049748,-3.6009673256178));
#38600=CARTESIAN_POINT('Ctrl Pts',(-50.1344329447385,2.78767608446746,-3.07298077943997));
#38601=CARTESIAN_POINT('Ctrl Pts',(-50.0682752274957,3.69011403259143,-1.89668321941156));
#38602=CARTESIAN_POINT('Ctrl Pts',(-50.002117510253,3.89186782276165,-0.61047665653478));
#38603=CARTESIAN_POINT('Ctrl Pts',(-49.9359597930103,4.09362161293187,0.675729906342009));
#38604=CARTESIAN_POINT('Ctrl Pts',(-49.8698020757676,3.59469124514835,2.07184547206718));
#38605=CARTESIAN_POINT('Ctrl Pts',(-49.8036443585249,2.62344165083307,2.93885535494938));
#38606=CARTESIAN_POINT('Ctrl Pts',(-49.7374866412822,1.6521920565178,3.80586523783157));
#38607=CARTESIAN_POINT('Ctrl Pts',(-49.6713289240395,0.208623235670778,
4.14376943787079));
#38608=CARTESIAN_POINT('Ctrl Pts',(-49.6051712067968,-1.0465303404107,3.7979061527243));
#38609=CARTESIAN_POINT('Ctrl Pts',(-49.539013489554,-2.30168391649217,3.4520428675778));
#38610=CARTESIAN_POINT('Ctrl Pts',(-49.4728557723114,-3.3684222478081,2.42241209724558));
#38611=CARTESIAN_POINT('Ctrl Pts',(-49.4066980550687,-3.7584895766171,1.18028513462752));
#38612=CARTESIAN_POINT('Ctrl Pts',(-49.3865198773907,-3.87746054773126,
0.80143502318402));
#38613=CARTESIAN_POINT('Ctrl Pts',(-49.3663416997128,-3.93348373764373,
0.402817308623724));
#38614=CARTESIAN_POINT('Ctrl Pts',(-49.3461635220349,-3.93028113905034,
0.00332252600905021));
#38615=CARTESIAN_POINT('Origin',(-27.25,0.,0.));
#38616=CARTESIAN_POINT('',(-47.912836477965,-3.92745622955471,-0.00190287763193742));
#38617=CARTESIAN_POINT('',(-48.0961635220349,-3.92766141711679,-0.00208726053621665));
#38618=CARTESIAN_POINT('',(-27.25,-3.933,-4.81653586104654E-16));
#38619=CARTESIAN_POINT('Ctrl Pts',(-47.912836477965,-3.92745622955471,-0.00190287763193742));
#38620=CARTESIAN_POINT('Ctrl Pts',(-47.9520585580458,-3.92405313224557,
0.776035286917171));
#38621=CARTESIAN_POINT('Ctrl Pts',(-47.9912806381266,-3.70062824945331,
1.55577560236864));
#38622=CARTESIAN_POINT('Ctrl Pts',(-48.0305027182074,-3.2702621470808,2.19652073651571));
#38623=CARTESIAN_POINT('Ctrl Pts',(-48.0966604354501,-2.54434351010488,
3.27729552771056));
#38624=CARTESIAN_POINT('Ctrl Pts',(-48.1628181526928,-1.22965336798294,
3.96261308582911));
#38625=CARTESIAN_POINT('Ctrl Pts',(-48.2289758699355,0.0720627412551513,
3.93879738218449));
#38626=CARTESIAN_POINT('Ctrl Pts',(-48.2951335871782,1.37377885049323,3.91498167853987));
#38627=CARTESIAN_POINT('Ctrl Pts',(-48.3612913044209,2.66252092684747,3.1820327131321));
#38628=CARTESIAN_POINT('Ctrl Pts',(-48.4274490216636,3.34842009607204,2.07542783945553));
#38629=CARTESIAN_POINT('Ctrl Pts',(-48.4936067389064,4.03431926529661,0.96882296577896));
#38630=CARTESIAN_POINT('Ctrl Pts',(-48.5597644561491,4.11737552739151,-0.511437816166413));
#38631=CARTESIAN_POINT('Ctrl Pts',(-48.6259221733918,3.55957328193336,-1.68782579288106));
#38632=CARTESIAN_POINT('Ctrl Pts',(-48.6920798906345,3.00177103647522,-2.86421376959571));
#38633=CARTESIAN_POINT('Ctrl Pts',(-48.7582376078772,1.80311028346402,-3.73672894107964));
#38634=CARTESIAN_POINT('Ctrl Pts',(-48.8243953251199,0.512228862821446,
-3.90601324225985));
#38635=CARTESIAN_POINT('Ctrl Pts',(-48.8905530423626,-0.778652557821136,
-4.07529754344005));
#38636=CARTESIAN_POINT('Ctrl Pts',(-48.9567107596053,-2.16175464609509,
-3.54135097431652));
#38637=CARTESIAN_POINT('Ctrl Pts',(-49.022868476848,-3.00401909907165,-2.54856569641061));
#38638=CARTESIAN_POINT('Ctrl Pts',(-49.0695244772204,-3.59800408328001,
-1.84842983583234));
#38639=CARTESIAN_POINT('Ctrl Pts',(-49.1161804775927,-3.92300850734398,
-0.920094817411913));
#38640=CARTESIAN_POINT('Ctrl Pts',(-49.1628364779651,-3.93064273659572,
0.00340251455877419));
#38641=CARTESIAN_POINT('Ctrl Pts',(-49.3461635220349,-3.93028113905034,
0.00332252600905021));
#38642=CARTESIAN_POINT('Ctrl Pts',(-49.3001839824701,-3.92298345285264,
-0.906996852497206));
#38643=CARTESIAN_POINT('Ctrl Pts',(-49.2542044429053,-3.60816375734389,
-1.82187028992255));
#38644=CARTESIAN_POINT('Ctrl Pts',(-49.2082249033405,-3.02985964262966,
-2.51779019021933));
#38645=CARTESIAN_POINT('Ctrl Pts',(-49.1420671860978,-2.19776605353114,
-3.51911539754416));
#38646=CARTESIAN_POINT('Ctrl Pts',(-49.0759094688551,-0.820182549032034,
-4.06714265728989));
#38647=CARTESIAN_POINT('Ctrl Pts',(-49.0097517516124,0.472358473597488,
-3.9110349486057));
#38648=CARTESIAN_POINT('Ctrl Pts',(-48.9435940343697,1.76489949622702,-3.75492723992151));
#38649=CARTESIAN_POINT('Ctrl Pts',(-48.877436317127,2.97239803698697,-2.89468456280739));
#38650=CARTESIAN_POINT('Ctrl Pts',(-48.8112785998842,3.54217112073391,-1.72404775106041));
#38651=CARTESIAN_POINT('Ctrl Pts',(-48.7451208826415,4.11194420448085,-0.553410939313448));
#38652=CARTESIAN_POINT('Ctrl Pts',(-48.6789631653988,4.0439918312148,0.92762000706637));
#38653=CARTESIAN_POINT('Ctrl Pts',(-48.6128054481561,3.36941641521032,2.04116386342701));
#38654=CARTESIAN_POINT('Ctrl Pts',(-48.5466477309134,2.69484099920583,3.15470771978765));
#38655=CARTESIAN_POINT('Ctrl Pts',(-48.4804900136707,1.4136425404629,3.90076448612912));
#38656=CARTESIAN_POINT('Ctrl Pts',(-48.414332296428,0.112237131383173,3.93785725019289));
#38657=CARTESIAN_POINT('Ctrl Pts',(-48.3481745791853,-1.18916827769656,
3.97495001425665));
#38658=CARTESIAN_POINT('Ctrl Pts',(-48.2820168619426,-2.51078063711309,
3.30307877604271));
#38659=CARTESIAN_POINT('Ctrl Pts',(-48.2158591446998,-3.2476860475286,2.22976506233225));
#38660=CARTESIAN_POINT('Ctrl Pts',(-48.1759606038115,-3.69210057501947,
1.5824686791246));
#38661=CARTESIAN_POINT('Ctrl Pts',(-48.1360620629232,-3.92385243391373,
0.789164405514797));
#38662=CARTESIAN_POINT('Ctrl Pts',(-48.0961635220349,-3.92766141711679,
-0.00208726053621665));
#38663=CARTESIAN_POINT('Origin',(-27.25,0.,0.));
#38664=CARTESIAN_POINT('',(-46.662836477965,-3.93759335115904,-0.00239393627812612));
#38665=CARTESIAN_POINT('',(-46.8461635220349,-3.93789469888383,-0.00220862991458794));
#38666=CARTESIAN_POINT('',(-27.25,-3.933,-4.81653586104654E-16));
#38667=CARTESIAN_POINT('Ctrl Pts',(-46.662836477965,-3.93759335115904,-0.00239393627812612));
#38668=CARTESIAN_POINT('Ctrl Pts',(-46.7217789212562,-3.92926765874005,
1.15900568512445));
#38669=CARTESIAN_POINT('Ctrl Pts',(-46.7807213645474,-3.38362267933311,
2.32720491863261));
#38670=CARTESIAN_POINT('Ctrl Pts',(-46.8396638078386,-2.48311790104751,
3.05833996574477));
#38671=CARTESIAN_POINT('Ctrl Pts',(-46.9058215250814,-1.47238035487552,
3.87897485992643));
#38672=CARTESIAN_POINT('Ctrl Pts',(-46.9719792423241,-0.0145871910493715,
4.14899229780223));
#38673=CARTESIAN_POINT('Ctrl Pts',(-47.0381369595668,1.22301650841775,3.7448028621961));
#38674=CARTESIAN_POINT('Ctrl Pts',(-47.1042946768095,2.46062020788489,3.34061342658998));
#38675=CARTESIAN_POINT('Ctrl Pts',(-47.1704523940522,3.478034442993,2.26221711750192));
#38676=CARTESIAN_POINT('Ctrl Pts',(-47.2366101112949,3.80957954011521,1.00320565394629));
#38677=CARTESIAN_POINT('Ctrl Pts',(-47.3027678285376,4.14112463723742,-0.255805809609345));
#38678=CARTESIAN_POINT('Ctrl Pts',(-47.3689255457803,3.78680059637373,-1.69543242763256));
#38679=CARTESIAN_POINT('Ctrl Pts',(-47.435083263023,2.90878472742779,-2.65674411000701));
#38680=CARTESIAN_POINT('Ctrl Pts',(-47.5012409802657,2.03076885848187,-3.61805579238144));
#38681=CARTESIAN_POINT('Ctrl Pts',(-47.5673986975084,0.629061161453717,
-4.10105253910711));
#38682=CARTESIAN_POINT('Ctrl Pts',(-47.6335564147511,-0.6547641057507,-3.88466238203473));
#38683=CARTESIAN_POINT('Ctrl Pts',(-47.6997141319938,-1.93858937295514,
-3.66827222496235));
#38684=CARTESIAN_POINT('Ctrl Pts',(-47.7658718492365,-3.10453221033583,
-2.75249516409189));
#38685=CARTESIAN_POINT('Ctrl Pts',(-47.8320295664793,-3.61893006311123,
-1.55649062152109));
#38686=CARTESIAN_POINT('Ctrl Pts',(-47.8589652036412,-3.82836343682328,
-1.0695460027322));
#38687=CARTESIAN_POINT('Ctrl Pts',(-47.8859008408031,-3.92979329567044,
-0.536149406412223));
#38688=CARTESIAN_POINT('Ctrl Pts',(-47.912836477965,-3.92745622955471,-0.00190287763193742));
#38689=CARTESIAN_POINT('Ctrl Pts',(-48.0961635220349,-3.92766141711679,
-0.00208726053621665));
#38690=CARTESIAN_POINT('Ctrl Pts',(-48.0699043456805,-3.93016829479786,
-0.522848586061526));
#38691=CARTESIAN_POINT('Ctrl Pts',(-48.0436451693261,-3.83393947565168,
-1.04272080444973));
#38692=CARTESIAN_POINT('Ctrl Pts',(-48.0173859929717,-3.63461882298519,
-1.51949429354273));
#38693=CARTESIAN_POINT('Ctrl Pts',(-47.951228275729,-3.13244772661179,-2.72068374650028));
#38694=CARTESIAN_POINT('Ctrl Pts',(-47.8850705584863,-1.9759070724505,-3.6483064632084));
#38695=CARTESIAN_POINT('Ctrl Pts',(-47.8189128412436,-0.694355951203478,
-3.8777811580271));
#38696=CARTESIAN_POINT('Ctrl Pts',(-47.7527551240009,0.587195170043544,
-4.1072558528458));
#38697=CARTESIAN_POINT('Ctrl Pts',(-47.6865974067582,1.9937567583763,-3.6385825257751));
#38698=CARTESIAN_POINT('Ctrl Pts',(-47.6204396895155,2.88153288605031,-2.68627718657711));
#38699=CARTESIAN_POINT('Ctrl Pts',(-47.5542819722727,3.76930901372432,-1.73397184737912));
#38700=CARTESIAN_POINT('Ctrl Pts',(-47.48812425503,4.13829968073957,-0.298034496053816));
#38701=CARTESIAN_POINT('Ctrl Pts',(-47.4219665377873,3.81961453009384,0.964293387932535));
#38702=CARTESIAN_POINT('Ctrl Pts',(-47.3558088205446,3.50092937944811,2.22662127191887));
#38703=CARTESIAN_POINT('Ctrl Pts',(-47.2896511033019,2.49456841114145,3.31533968856626));
#38704=CARTESIAN_POINT('Ctrl Pts',(-47.2234933860592,1.26115211887257,3.73213239711288));
#38705=CARTESIAN_POINT('Ctrl Pts',(-47.1573356688165,0.0277358266036876,
4.14892510565949));
#38706=CARTESIAN_POINT('Ctrl Pts',(-47.0911779515738,-1.43273578962741,
3.89379210610531));
#38707=CARTESIAN_POINT('Ctrl Pts',(-47.0250202343311,-2.451791695979,3.08351007393255));
#38708=CARTESIAN_POINT('Ctrl Pts',(-46.9654013302323,-3.37012743796263,
2.35331367686203));
#38709=CARTESIAN_POINT('Ctrl Pts',(-46.9057824261336,-3.92999159195356,
1.17228340405631));
#38710=CARTESIAN_POINT('Ctrl Pts',(-46.8461635220349,-3.93789469888383,
-0.00220862991458794));
#38711=CARTESIAN_POINT('Origin',(-27.25,0.,0.));
#38712=CARTESIAN_POINT('',(-45.412836477965,-3.93474092475559,0.00340612917001049));
#38713=CARTESIAN_POINT('',(-45.5961635220349,-3.93433860385037,0.003473953574826));
#38714=CARTESIAN_POINT('',(-27.25,-3.933,-4.81653586104654E-16));
#38715=CARTESIAN_POINT('Ctrl Pts',(-45.412836477965,-3.93474092475559,0.00340612917001049));
#38716=CARTESIAN_POINT('Ctrl Pts',(-45.4253415672239,-3.93699281657843,
0.250270820522606));
#38717=CARTESIAN_POINT('Ctrl Pts',(-45.4378466564828,-3.91575262884963,
0.496749281650563));
#38718=CARTESIAN_POINT('Ctrl Pts',(-45.4503517457417,-3.86962127480358,
0.738477519063283));
#38719=CARTESIAN_POINT('Ctrl Pts',(-45.5165094629844,-3.62556503387504,
2.01733191580052));
#38720=CARTESIAN_POINT('Ctrl Pts',(-45.5826671802271,-2.68482986023644,
3.16323228596122));
#38721=CARTESIAN_POINT('Ctrl Pts',(-45.6488248974698,-1.47799872934894,
3.65168969281581));
#38722=CARTESIAN_POINT('Ctrl Pts',(-45.7149826147126,-0.271167598461425,
4.14014709967041));
#38723=CARTESIAN_POINT('Ctrl Pts',(-45.7811403319553,1.201759489675,3.97116154321891));
#38724=CARTESIAN_POINT('Ctrl Pts',(-45.847298049198,2.26661051936538,3.22207923708846));
#38725=CARTESIAN_POINT('Ctrl Pts',(-45.9134557664407,3.33146154905574,2.47299693095802));
#38726=CARTESIAN_POINT('Ctrl Pts',(-45.9796134836834,3.98823652030005,1.14381787514865));
#38727=CARTESIAN_POINT('Ctrl Pts',(-46.0457712009261,3.93632360391267,-0.157080685809306));
#38728=CARTESIAN_POINT('Ctrl Pts',(-46.1119289181688,3.88441068752528,-1.45797924676727));
#38729=CARTESIAN_POINT('Ctrl Pts',(-46.1780866354115,3.12380988350618,-2.73059731287383));
#38730=CARTESIAN_POINT('Ctrl Pts',(-46.2442443526542,2.00265504132755,-3.39244611482919));
#38731=CARTESIAN_POINT('Ctrl Pts',(-46.3104020698969,0.88150019914892,-4.05429491678456));
#38732=CARTESIAN_POINT('Ctrl Pts',(-46.3765597871397,-0.600208681189243,
-4.10537445458874));
#38733=CARTESIAN_POINT('Ctrl Pts',(-46.4427175043824,-1.76428007847962,
-3.52230516299402));
#38734=CARTESIAN_POINT('Ctrl Pts',(-46.5088752216251,-2.92835147576999,
-2.9392358713993));
#38735=CARTESIAN_POINT('Ctrl Pts',(-46.5750329388678,-3.77478539001258,
-1.72201775040568));
#38736=CARTESIAN_POINT('Ctrl Pts',(-46.6411906561105,-3.91616138287496,
-0.427782514665089));
#38737=CARTESIAN_POINT('Ctrl Pts',(-46.648405930062,-3.93158009079269,-0.286631003204834));
#38738=CARTESIAN_POINT('Ctrl Pts',(-46.6556212040135,-3.93861251745559,
-0.144563414971144));
#38739=CARTESIAN_POINT('Ctrl Pts',(-46.662836477965,-3.93759335115904,-0.00239393627812612));
#38740=CARTESIAN_POINT('Ctrl Pts',(-46.8461635220349,-3.93789469888383,
-0.00220862991458794));
#38741=CARTESIAN_POINT('Ctrl Pts',(-46.8396247088909,-3.93876148669644,
-0.131023207527449));
#38742=CARTESIAN_POINT('Ctrl Pts',(-46.8330858957469,-3.93298872969746,
-0.259759136601678));
#38743=CARTESIAN_POINT('Ctrl Pts',(-46.826547082603,-3.9203211565074,-0.387813004366422));
#38744=CARTESIAN_POINT('Ctrl Pts',(-46.7603893653603,-3.79215451421213,
-1.68342298570133));
#38745=CARTESIAN_POINT('Ctrl Pts',(-46.6942316481175,-2.95818103314946,
-2.90921188357983));
#38746=CARTESIAN_POINT('Ctrl Pts',(-46.6280739308748,-1.80011789897827,
-3.50412506145166));
#38747=CARTESIAN_POINT('Ctrl Pts',(-46.5619162136321,-0.642054764807075,
-4.09903823932348));
#38748=CARTESIAN_POINT('Ctrl Pts',(-46.4957584963894,0.840098022472642,
-4.06307569718863));
#38749=CARTESIAN_POINT('Ctrl Pts',(-46.4296007791467,1.96794576144187,-3.41269781500477));
#38750=CARTESIAN_POINT('Ctrl Pts',(-46.363443061904,3.0957935004111,-2.76231993282091));
#38751=CARTESIAN_POINT('Ctrl Pts',(-46.2972853446612,3.86933619106982,-1.49752671058804));
#38752=CARTESIAN_POINT('Ctrl Pts',(-46.2311276274185,3.93451636568059,-0.197225415976034));
#38753=CARTESIAN_POINT('Ctrl Pts',(-46.1649699101758,3.99969654029137,1.10307587863597));
#38754=CARTESIAN_POINT('Ctrl Pts',(-46.0988121929332,3.35651419885418,2.43888524562711));
#38755=CARTESIAN_POINT('Ctrl Pts',(-46.0326544756904,2.29935970127119,3.19879068722626));
#38756=CARTESIAN_POINT('Ctrl Pts',(-45.9664967584477,1.2422052036882,3.95869612882542));
#38757=CARTESIAN_POINT('Ctrl Pts',(-45.900339041205,-0.228921450040587,
4.1426976450326));
#38758=CARTESIAN_POINT('Ctrl Pts',(-45.8341813239623,-1.44067231929053,
3.66657608197968));
#38759=CARTESIAN_POINT('Ctrl Pts',(-45.7680236067196,-2.65242318854047,
3.19045451892675));
#38760=CARTESIAN_POINT('Ctrl Pts',(-45.7018658894769,-3.60479827331157,
2.0542098766137));
#38761=CARTESIAN_POINT('Ctrl Pts',(-45.6357081722342,-3.86188690581226,
0.777911578028733));
#38762=CARTESIAN_POINT('Ctrl Pts',(-45.6225266221678,-3.91311035822352,
0.52361637825961));
#38763=CARTESIAN_POINT('Ctrl Pts',(-45.6093450721013,-3.93673211827082,
0.263761285985406));
#38764=CARTESIAN_POINT('Ctrl Pts',(-45.5961635220349,-3.93433860385037,
0.003473953574826));
#38765=CARTESIAN_POINT('Origin',(-27.25,0.,0.));
#38766=CARTESIAN_POINT('',(-44.162836477965,-3.92656883402695,0.000277810122669975));
#38767=CARTESIAN_POINT('',(-44.3461635220349,-3.92655167676131,5.76543438965291E-5));
#38768=CARTESIAN_POINT('',(-27.25,-3.933,-4.81653586104654E-16));
#38769=CARTESIAN_POINT('Ctrl Pts',(-44.162836477965,-3.92656883402695,0.000277810122669975));
#38770=CARTESIAN_POINT('Ctrl Pts',(-44.1950619304343,-3.92697179969628,
0.639804442392745));
#38771=CARTESIAN_POINT('Ctrl Pts',(-44.2272873829036,-3.77958365909042,
1.27915600723495));
#38772=CARTESIAN_POINT('Ctrl Pts',(-44.2595128353729,-3.48339515771394,
1.83991196305406));
#38773=CARTESIAN_POINT('Ctrl Pts',(-44.3256705526156,-2.8753306117383,2.99112416100792));
#38774=CARTESIAN_POINT('Ctrl Pts',(-44.3918282698584,-1.64012251647393,
3.81108226155247));
#38775=CARTESIAN_POINT('Ctrl Pts',(-44.4579859871011,-0.343136760086226,
3.92448404512643));
#38776=CARTESIAN_POINT('Ctrl Pts',(-44.5241437043438,0.953848996301473,
4.03788582870038));
#38777=CARTESIAN_POINT('Ctrl Pts',(-44.5903014215865,2.31261241381248,3.44473129530375));
#38778=CARTESIAN_POINT('Ctrl Pts',(-44.6564591388292,3.11123521868153,2.41651262579156));
#38779=CARTESIAN_POINT('Ctrl Pts',(-44.7226168560719,3.90985802355059,1.38829395627936));
#38780=CARTESIAN_POINT('Ctrl Pts',(-44.7887745733146,4.14834021577764,-0.0749888493484113));
#38781=CARTESIAN_POINT('Ctrl Pts',(-44.8549322905573,3.71752634460343,-1.30357805050323));
#38782=CARTESIAN_POINT('Ctrl Pts',(-44.9210900078001,3.28671247342922,-2.53216725165805));
#38783=CARTESIAN_POINT('Ctrl Pts',(-44.9872477250427,2.18660253885373,-3.52606284833993));
#38784=CARTESIAN_POINT('Ctrl Pts',(-45.0534054422855,0.920726782158098,
-3.83034985989415));
#38785=CARTESIAN_POINT('Ctrl Pts',(-45.1195631595282,-0.345148974537538,
-4.13463687144837));
#38786=CARTESIAN_POINT('Ctrl Pts',(-45.1857208767709,-1.77679055335334,
-3.74931529787494));
#38787=CARTESIAN_POINT('Ctrl Pts',(-45.2518785940136,-2.71892268865198,
-2.85075029943133));
#38788=CARTESIAN_POINT('Ctrl Pts',(-45.3055312219974,-3.48297361231569,
-2.12203148037195));
#38789=CARTESIAN_POINT('Ctrl Pts',(-45.3591838499812,-3.92507926527206,
-1.05575779787344));
#38790=CARTESIAN_POINT('Ctrl Pts',(-45.412836477965,-3.93474092475559,0.00340612917001049));
#38791=CARTESIAN_POINT('Ctrl Pts',(-45.5961635220349,-3.93433860385037,
0.003473953574826));
#38792=CARTESIAN_POINT('Ctrl Pts',(-45.5431873548586,-3.92471915701462,
-1.04261130697134));
#38793=CARTESIAN_POINT('Ctrl Pts',(-45.4902111876823,-3.49489926040405,
-2.0956781390531));
#38794=CARTESIAN_POINT('Ctrl Pts',(-45.437235020506,-2.74786054164776,-2.82286721972017));
#38795=CARTESIAN_POINT('Ctrl Pts',(-45.3710773032633,-1.81494336475224,
-3.73099576402723));
#38796=CARTESIAN_POINT('Ctrl Pts',(-45.3049195860206,-0.387306830730913,
-4.13090089778447));
#38797=CARTESIAN_POINT('Ctrl Pts',(-45.2387618687779,0.881606939911368,
-3.8395424336782));
#38798=CARTESIAN_POINT('Ctrl Pts',(-45.1726041515352,2.15052071055363,-3.54818396957193));
#38799=CARTESIAN_POINT('Ctrl Pts',(-45.1064464342925,3.26071171781685,-2.56556190760216));
#38800=CARTESIAN_POINT('Ctrl Pts',(-45.0402887170498,3.70403552250813,-1.34143122988594));
#38801=CARTESIAN_POINT('Ctrl Pts',(-44.9741309998071,4.14735932719942,-0.117300552169714));
#38802=CARTESIAN_POINT('Ctrl Pts',(-44.9079732825644,3.92381592931878,1.34833874129297));
#38803=CARTESIAN_POINT('Ctrl Pts',(-44.8418155653217,3.13572315868845,2.3846503241734));
#38804=CARTESIAN_POINT('Ctrl Pts',(-44.7756578480789,2.34763038805812,3.42096190705384));
#38805=CARTESIAN_POINT('Ctrl Pts',(-44.7095001308362,0.994988244678091,
4.02794577935202));
#38806=CARTESIAN_POINT('Ctrl Pts',(-44.6433424135935,-0.30308676007683,
3.92777994704152));
#38807=CARTESIAN_POINT('Ctrl Pts',(-44.5771846963508,-1.60116176483176,
3.82761411473103));
#38808=CARTESIAN_POINT('Ctrl Pts',(-44.5110269791081,-2.84466963096158,
3.02029857781185));
#38809=CARTESIAN_POINT('Ctrl Pts',(-44.4448692618654,-3.46444559030253,
1.87534894042382));
#38810=CARTESIAN_POINT('Ctrl Pts',(-44.4119673485886,-3.77267591799805,
1.30593640254117));
#38811=CARTESIAN_POINT('Ctrl Pts',(-44.3790654353117,-3.92663703969061,
0.653015960009206));
#38812=CARTESIAN_POINT('Ctrl Pts',(-44.3461635220349,-3.92655167676131,
5.76543438965291E-5));
#38813=CARTESIAN_POINT('Origin',(-27.25,0.,0.));
#38814=CARTESIAN_POINT('',(-42.912836477965,-3.93372101951109,-0.00354898223331679));
#38815=CARTESIAN_POINT('',(-43.0961635220349,-3.93412692362359,-0.00350358252896577));
#38816=CARTESIAN_POINT('',(-27.25,-3.933,-4.81653586104654E-16));
#38817=CARTESIAN_POINT('Ctrl Pts',(-42.912836477965,-3.93372101951109,-0.00354898223331679));
#38818=CARTESIAN_POINT('Ctrl Pts',(-42.9647822936447,-3.92424142884988,
1.02260461028873));
#38819=CARTESIAN_POINT('Ctrl Pts',(-43.0167281093244,-3.51272955475539,
2.05549339592713));
#38820=CARTESIAN_POINT('Ctrl Pts',(-43.0686739250041,-2.79138702348944,
2.779833869437));
#38821=CARTESIAN_POINT('Ctrl Pts',(-43.1348316422469,-1.87269175238464,
3.70234729245046));
#38822=CARTESIAN_POINT('Ctrl Pts',(-43.2009893594896,-0.45144070276789,
4.12438494387334));
#38823=CARTESIAN_POINT('Ctrl Pts',(-43.2671470767323,0.82184669867214,3.85277638339627));
#38824=CARTESIAN_POINT('Ctrl Pts',(-43.333304793975,2.09513410011217,3.5811678229192));
#38825=CARTESIAN_POINT('Ctrl Pts',(-43.3994625112177,3.22045785337548,2.61591305054217));
#38826=CARTESIAN_POINT('Ctrl Pts',(-43.4656202284604,3.68274712491062,1.3988178832632));
#38827=CARTESIAN_POINT('Ctrl Pts',(-43.5317779457031,4.14503639644575,0.181722715984218));
#38828=CARTESIAN_POINT('Ctrl Pts',(-43.5979356629459,3.94429118625271,-1.28721284619671));
#38829=CARTESIAN_POINT('Ctrl Pts',(-43.6640933801886,3.17239438798388,-2.3356437450225));
#38830=CARTESIAN_POINT('Ctrl Pts',(-43.7302510974313,2.40049758971504,-3.38407464384829));
#38831=CARTESIAN_POINT('Ctrl Pts',(-43.7964088146739,1.05744920337041,-4.01200087931894));
#38832=CARTESIAN_POINT('Ctrl Pts',(-43.8625665319166,-0.242025408816761,
-3.93201494886037));
#38833=CARTESIAN_POINT('Ctrl Pts',(-43.9287242491593,-1.54150002100394,
-3.8520290184018));
#38834=CARTESIAN_POINT('Ctrl Pts',(-43.9948819664021,-2.79740085903366,
-3.06413092201401));
#38835=CARTESIAN_POINT('Ctrl Pts',(-44.0610396836448,-3.43489077970507,
-1.92894872613853));
#38836=CARTESIAN_POINT('Ctrl Pts',(-44.0949719484182,-3.76185908635389,
-1.34671426518835));
#38837=CARTESIAN_POINT('Ctrl Pts',(-44.1289042131916,-3.9261445253908,-0.673121175865286));
#38838=CARTESIAN_POINT('Ctrl Pts',(-44.162836477965,-3.92656883402695,0.000277810122669975));
#38839=CARTESIAN_POINT('Ctrl Pts',(-44.3461635220349,-3.92655167676131,
5.76543438965291E-5));
#38840=CARTESIAN_POINT('Ctrl Pts',(-44.312907718069,-3.92646539567429,-0.659923825407093));
#38841=CARTESIAN_POINT('Ctrl Pts',(-44.2796519141031,-3.7690009817897,-1.31994398717828));
#38842=CARTESIAN_POINT('Ctrl Pts',(-44.2463961101372,-3.45438842079276,
-1.89381032176095));
#38843=CARTESIAN_POINT('Ctrl Pts',(-44.1802383928945,-2.82851123938996,
-3.03543620870082));
#38844=CARTESIAN_POINT('Ctrl Pts',(-44.1140806756519,-1.58071282403231,
-3.83610424472369));
#38845=CARTESIAN_POINT('Ctrl Pts',(-44.0479229584092,-0.282121765970689,
-3.9293414468179));
#38846=CARTESIAN_POINT('Ctrl Pts',(-43.9817652411665,1.01646929209093,-4.0225786489121));
#38847=CARTESIAN_POINT('Ctrl Pts',(-43.9156075239237,2.36585299285652,-3.40838501707761));
#38848=CARTESIAN_POINT('Ctrl Pts',(-43.849449806681,3.14840424353069,-2.36788251732077));
#38849=CARTESIAN_POINT('Ctrl Pts',(-43.7832920894383,3.93095549420486,-1.32738001756392));
#38850=CARTESIAN_POINT('Ctrl Pts',(-43.7171343721956,4.14667429478762,0.139431350115277));
#38851=CARTESIAN_POINT('Ctrl Pts',(-43.6509766549529,3.69682420422663,1.36117879044582));
#38852=CARTESIAN_POINT('Ctrl Pts',(-43.5848189377102,3.24697411366564,2.58292623077635));
#38853=CARTESIAN_POINT('Ctrl Pts',(-43.5186612204675,2.13155513196088,3.55960974375823));
#38854=CARTESIAN_POINT('Ctrl Pts',(-43.4525035032247,0.861104589369346,
3.84419247471851));
#38855=CARTESIAN_POINT('Ctrl Pts',(-43.386345785982,-0.409345953222192,
4.12877520567879));
#38856=CARTESIAN_POINT('Ctrl Pts',(-43.3201880687393,-1.83482805670052,
3.7212571546175));
#38857=CARTESIAN_POINT('Ctrl Pts',(-43.2540303514966,-2.76288570285569,
2.80816300977543));
#38858=CARTESIAN_POINT('Ctrl Pts',(-43.2014080750094,-3.50106876127229,
2.08188201715149));
#38859=CARTESIAN_POINT('Ctrl Pts',(-43.1487857985221,-3.92454556393865,
1.03573746106949));
#38860=CARTESIAN_POINT('Ctrl Pts',(-43.0961635220349,-3.93412692362359,
-0.00350358252896577));
#38861=CARTESIAN_POINT('Origin',(-27.25,0.,0.));
#38862=CARTESIAN_POINT('',(-41.662836477965,-3.93831397248116,0.00190595679815712));
#38863=CARTESIAN_POINT('',(-41.8461635220348,-3.93804437062894,0.00210735149479831));
#38864=CARTESIAN_POINT('',(-27.25,-3.933,-4.81653586104654E-16));
#38865=CARTESIAN_POINT('Ctrl Pts',(-41.662836477965,-3.93831397248116,0.00190595679815712));
#38866=CARTESIAN_POINT('Ctrl Pts',(-41.6683449396124,-3.93896170190249,
0.110392148591447));
#38867=CARTESIAN_POINT('Ctrl Pts',(-41.6738534012598,-3.93486758661977,
0.218828713482624));
#38868=CARTESIAN_POINT('Ctrl Pts',(-41.6793618629072,-3.92587342546206,
0.326857314168025));
#38869=CARTESIAN_POINT('Ctrl Pts',(-41.7455195801499,-3.8178517655515,1.62430224085299));
#38870=CARTESIAN_POINT('Ctrl Pts',(-41.8116772973927,-3.00302364739276,
2.86290042554131));
#38871=CARTESIAN_POINT('Ctrl Pts',(-41.8778350146354,-1.85434325133095,
3.47573430555584));
#38872=CARTESIAN_POINT('Ctrl Pts',(-41.9439927318781,-0.70566285526915,
4.08856818557036));
#38873=CARTESIAN_POINT('Ctrl Pts',(-42.0101504491208,0.776869818695703,
4.07563776091109));
#38874=CARTESIAN_POINT('Ctrl Pts',(-42.0763081663635,1.91468619158182,3.44286140359153));
#38875=CARTESIAN_POINT('Ctrl Pts',(-42.1424658836062,3.05250256446794,2.81008504627197));
#38876=CARTESIAN_POINT('Ctrl Pts',(-42.2086236008489,3.84560263627532,1.55746275629211));
#38877=CARTESIAN_POINT('Ctrl Pts',(-42.2747813180916,3.93097734948523,0.258331055834204));
#38878=CARTESIAN_POINT('Ctrl Pts',(-42.3409390353344,4.01635206269515,-1.0408006446237));
#38879=CARTESIAN_POINT('Ctrl Pts',(-42.4070967525771,3.39400141730759,-2.38644175555967));
#38880=CARTESIAN_POINT('Ctrl Pts',(-42.4732544698198,2.34878091801755,-3.16268020130568));
#38881=CARTESIAN_POINT('Ctrl Pts',(-42.5394121870625,1.30356041872751,-3.93891864705171));
#38882=CARTESIAN_POINT('Ctrl Pts',(-42.6055699043052,-0.164529934465034,
-4.14575442760779));
#38883=CARTESIAN_POINT('Ctrl Pts',(-42.6717276215479,-1.3835319430817,-3.68851694032262));
#38884=CARTESIAN_POINT('Ctrl Pts',(-42.7378853387906,-2.60253395169839,
-3.23127945303743));
#38885=CARTESIAN_POINT('Ctrl Pts',(-42.8040430560333,-3.57244761573919,
-2.10996869791097));
#38886=CARTESIAN_POINT('Ctrl Pts',(-42.870200773276,-3.84933470146315,-0.837818723045716));
#38887=CARTESIAN_POINT('Ctrl Pts',(-42.884412674839,-3.90881516981029,-0.56453737402596));
#38888=CARTESIAN_POINT('Ctrl Pts',(-42.898624576402,-3.93631454908748,-0.284295249369827));
#38889=CARTESIAN_POINT('Ctrl Pts',(-42.912836477965,-3.93372101951109,-0.00354898223331679));
#38890=CARTESIAN_POINT('Ctrl Pts',(-43.0961635220349,-3.93412692362359,
-0.00350358252896577));
#38891=CARTESIAN_POINT('Ctrl Pts',(-43.0826280812794,-3.93659142981811,
-0.270815955069072));
#38892=CARTESIAN_POINT('Ctrl Pts',(-43.0690926405239,-3.91167198021206,
-0.537671580660341));
#38893=CARTESIAN_POINT('Ctrl Pts',(-43.0555571997685,-3.85768057402877,
-0.79850953987816));
#38894=CARTESIAN_POINT('Ctrl Pts',(-42.9893994825258,-3.59378461021468,
-2.07341770606684));
#38895=CARTESIAN_POINT('Ctrl Pts',(-42.9232417652831,-2.63535949375449,
-3.20456379982134));
#38896=CARTESIAN_POINT('Ctrl Pts',(-42.8570840480404,-1.42108504652191,
-3.67421204982336));
#38897=CARTESIAN_POINT('Ctrl Pts',(-42.7909263307977,-0.20681059928933,
-4.14386029982538));
#38898=CARTESIAN_POINT('Ctrl Pts',(-42.7247686135549,1.26331317871563,-3.95201070607491));
#38899=CARTESIAN_POINT('Ctrl Pts',(-42.6586108963122,2.31639737213419,-3.18647455833013));
#38900=CARTESIAN_POINT('Ctrl Pts',(-42.5924531790695,3.36948156555278,-2.42093841058533));
#38901=CARTESIAN_POINT('Ctrl Pts',(-42.5262954618268,4.00552617438494,-1.08171570884617));
#38902=CARTESIAN_POINT('Ctrl Pts',(-42.4601377445841,3.93340784333217,0.218219235009942));
#38903=CARTESIAN_POINT('Ctrl Pts',(-42.3939800273414,3.86128951227941,1.51815417886602));
#38904=CARTESIAN_POINT('Ctrl Pts',(-42.3278223100986,3.08100824134177,2.77880136483906));
#38905=CARTESIAN_POINT('Ctrl Pts',(-42.2616645928559,1.94970580723992,3.42315120345717));
#38906=CARTESIAN_POINT('Ctrl Pts',(-42.1955068756132,0.818403373138075,
4.06750104207528));
#38907=CARTESIAN_POINT('Ctrl Pts',(-42.1293491583706,-0.663920224127962,
4.09555353333847));
#38908=CARTESIAN_POINT('Ctrl Pts',(-42.0631914411279,-1.81879210186756,
3.49446879893061));
#38909=CARTESIAN_POINT('Ctrl Pts',(-41.9970337238852,-2.97366397960716,
2.89338406452276));
#38910=CARTESIAN_POINT('Ctrl Pts',(-41.9308760066424,-3.80108413782031,
1.66316210444388));
#38911=CARTESIAN_POINT('Ctrl Pts',(-41.8647182893997,-3.92233490583468,
0.366886607804419));
#38912=CARTESIAN_POINT('Ctrl Pts',(-41.8585333669447,-3.93367034225883,
0.245700996191627));
#38913=CARTESIAN_POINT('Ctrl Pts',(-41.8523484444898,-3.93883391417578,
0.123938081903965));
#38914=CARTESIAN_POINT('Ctrl Pts',(-41.8461635220348,-3.93804437062894,
0.00210735149479831));
#38915=CARTESIAN_POINT('Origin',(-27.25,0.,0.));
#38916=CARTESIAN_POINT('',(-40.412836477965,-3.92801100457036,0.00235306236043675));
#38917=CARTESIAN_POINT('',(-40.5961635220348,-3.92777652835409,0.00218069315271673));
#38918=CARTESIAN_POINT('',(-27.25,-3.933,-4.81653586104654E-16));
#38919=CARTESIAN_POINT('Ctrl Pts',(-40.412836477965,-3.92801100457036,0.00235306236043675));
#38920=CARTESIAN_POINT('Ctrl Pts',(-40.4380653028228,-3.93074080988322,
0.502569384095045));
#38921=CARTESIAN_POINT('Ctrl Pts',(-40.4632941276807,-3.84214798031435,
1.00185495457367));
#38922=CARTESIAN_POINT('Ctrl Pts',(-40.4885229525385,-3.65778817178925,
1.46284091646802));
#38923=CARTESIAN_POINT('Ctrl Pts',(-40.5546806697812,-3.17434020494728,
2.67168750729197));
#38924=CARTESIAN_POINT('Ctrl Pts',(-40.6208383870239,-2.03235131675089,
3.61716712340826));
#38925=CARTESIAN_POINT('Ctrl Pts',(-40.6869961042666,-0.754520123348716,
3.86652521523346));
#38926=CARTESIAN_POINT('Ctrl Pts',(-40.7531538215093,0.523311070053491,
4.11588330705867));
#38927=CARTESIAN_POINT('Ctrl Pts',(-40.819311538752,1.93698456866149,3.66911987459282));
#38928=CARTESIAN_POINT('Ctrl Pts',(-40.8854692559947,2.83944925924138,2.73072257118293));
#38929=CARTESIAN_POINT('Ctrl Pts',(-40.9516269732374,3.74191394982125,1.79232526777306));
#38930=CARTESIAN_POINT('Ctrl Pts',(-41.0177846904802,4.133169832373,0.362294093419191));
#38931=CARTESIAN_POINT('Ctrl Pts',(-41.0839424077229,3.83413555988564,-0.904832782891263));
#38932=CARTESIAN_POINT('Ctrl Pts',(-41.1501001249656,3.53510128739829,-2.17195965920172));
#38933=CARTESIAN_POINT('Ctrl Pts',(-41.2162578422083,2.54577685987183,-3.27618223746875));
#38934=CARTESIAN_POINT('Ctrl Pts',(-41.282415559451,1.31898499260147,-3.71208788229299));
#38935=CARTESIAN_POINT('Ctrl Pts',(-41.3485732766937,0.0921931253310943,
-4.14799352711723));
#38936=CARTESIAN_POINT('Ctrl Pts',(-41.4147309939364,-1.3720661816832,-3.91558223849864));
#38937=CARTESIAN_POINT('Ctrl Pts',(-41.4808887111791,-2.40358823435914,
-3.12123075984854));
#38938=CARTESIAN_POINT('Ctrl Pts',(-41.5415379667744,-3.34922310860086,
-2.39301902780813));
#38939=CARTESIAN_POINT('Ctrl Pts',(-41.6021872223697,-3.93118234304533,
-1.19254853808352));
#38940=CARTESIAN_POINT('Ctrl Pts',(-41.662836477965,-3.93831397248116,0.00190595679815712));
#38941=CARTESIAN_POINT('Ctrl Pts',(-41.8461635220348,-3.93804437062894,
0.00210735149479831));
#38942=CARTESIAN_POINT('Ctrl Pts',(-41.7861907272471,-3.93038847300766,
-1.17923800034984));
#38943=CARTESIAN_POINT('Ctrl Pts',(-41.7262179324593,-3.36299512682459,
-2.36695971479872));
#38944=CARTESIAN_POINT('Ctrl Pts',(-41.6662451376716,-2.4353015692775,-3.09655020356362));
#38945=CARTESIAN_POINT('Ctrl Pts',(-41.6000874204289,-1.41193608689036,
-3.90138248509218));
#38946=CARTESIAN_POINT('Ctrl Pts',(-41.5339297031862,0.0498762556995175,
-4.14871801494928));
#38947=CARTESIAN_POINT('Ctrl Pts',(-41.4677719859434,1.28105076210131,-3.72534908987534));
#38948=CARTESIAN_POINT('Ctrl Pts',(-41.4016142687007,2.5122252685031,-3.3019801648014));
#38949=CARTESIAN_POINT('Ctrl Pts',(-41.335456551458,3.51276193871678,-2.20790678479643));
#38950=CARTESIAN_POINT('Ctrl Pts',(-41.2692988342153,3.82470611282222,-0.943896205658093));
#38951=CARTESIAN_POINT('Ctrl Pts',(-41.2031411169726,4.13665028692766,0.320114373480223));
#38952=CARTESIAN_POINT('Ctrl Pts',(-41.1369833997299,3.76000196492484,1.75406215175193));
#38953=CARTESIAN_POINT('Ctrl Pts',(-41.0708256824872,2.86715648158494,2.70161629522418));
#38954=CARTESIAN_POINT('Ctrl Pts',(-41.0046679652445,1.97431099824503,3.64917043869645));
#38955=CARTESIAN_POINT('Ctrl Pts',(-40.9385102480018,0.565268353568015,
4.1103309473693));
#38956=CARTESIAN_POINT('Ctrl Pts',(-40.8723525307591,-0.715039922831877,
3.87402049623798));
#38957=CARTESIAN_POINT('Ctrl Pts',(-40.8061948135164,-1.99534819923177,
3.63771004510666));
#38958=CARTESIAN_POINT('Ctrl Pts',(-40.7400370962736,-3.14692210735452,
2.70392863417116));
#38959=CARTESIAN_POINT('Ctrl Pts',(-40.6738793790309,-3.64267588096367,
1.50007643897266));
#38960=CARTESIAN_POINT('Ctrl Pts',(-40.6479740933656,-3.83679749912515,
1.02868570308809));
#38961=CARTESIAN_POINT('Ctrl Pts',(-40.6220688077002,-3.930364852657,0.515886099618727));
#38962=CARTESIAN_POINT('Ctrl Pts',(-40.5961635220348,-3.92777652835409,
0.00218069315271673));
#38963=CARTESIAN_POINT('Origin',(-27.25,0.,0.));
#38964=CARTESIAN_POINT('',(-39.162836477965,-3.92975286260395,-0.00317618749887255));
#38965=CARTESIAN_POINT('',(-39.3461635220348,-3.93009648465997,-0.00327554246926138));
#38966=CARTESIAN_POINT('',(-27.25,-3.933,-4.81653586104654E-16));
#38967=CARTESIAN_POINT('Ctrl Pts',(-39.162836477965,-3.92975286260395,-0.00317618749887255));
#38968=CARTESIAN_POINT('Ctrl Pts',(-39.2077856660332,-3.92299702030768,
0.887046174022243));
#38969=CARTESIAN_POINT('Ctrl Pts',(-39.2527348541015,-3.6233189159279,1.78138571892125));
#38970=CARTESIAN_POINT('Ctrl Pts',(-39.2976840421697,-3.06861220208183,
2.47041231574991));
#38971=CARTESIAN_POINT('Ctrl Pts',(-39.3638417594124,-2.2521763218261,3.48454468887551));
#38972=CARTESIAN_POINT('Ctrl Pts',(-39.4299994766551,-0.883273592225803,
4.05390893270202));
#38973=CARTESIAN_POINT('Ctrl Pts',(-39.4961571938978,0.411536858342489,
3.91790189652574));
#38974=CARTESIAN_POINT('Ctrl Pts',(-39.5623149111405,1.7063473089108,3.78189486034945));
#38975=CARTESIAN_POINT('Ctrl Pts',(-39.6284726283832,2.92706548044712,2.94051654417035));
#38976=CARTESIAN_POINT('Ctrl Pts',(-39.6946303456259,3.51495765359173,1.77887339348006));
#38977=CARTESIAN_POINT('Ctrl Pts',(-39.7607880628686,4.10284982673633,0.61723024278978));
#38978=CARTESIAN_POINT('Ctrl Pts',(-39.8269457801114,4.05791600148925,-0.864677742411652));
#38979=CARTESIAN_POINT('Ctrl Pts',(-39.8931034973541,3.40072279501961,-1.98856790882493));
#38980=CARTESIAN_POINT('Ctrl Pts',(-39.9592612145968,2.74352958854996,-3.11245807523822));
#38981=CARTESIAN_POINT('Ctrl Pts',(-40.0254189318395,1.47407700085769,-3.87833042286331));
#38982=CARTESIAN_POINT('Ctrl Pts',(-40.0915766490822,0.173404933216231,
-3.93563826916431));
#38983=CARTESIAN_POINT('Ctrl Pts',(-40.1577343663249,-1.12726713442519,
-3.9929461154653));
#38984=CARTESIAN_POINT('Ctrl Pts',(-40.2238920835676,-2.45915868201583,
-3.34168946044224));
#38985=CARTESIAN_POINT('Ctrl Pts',(-40.2900498008103,-3.21265093306733,
-2.27995435016492));
#38986=CARTESIAN_POINT('Ctrl Pts',(-40.3309786931952,-3.67880370467823,
-1.62310517397008));
#38987=CARTESIAN_POINT('Ctrl Pts',(-40.3719075855801,-3.92358242303668,
-0.809151243401977));
#38988=CARTESIAN_POINT('Ctrl Pts',(-40.412836477965,-3.92801100457036,0.00235306236043675));
#38989=CARTESIAN_POINT('Ctrl Pts',(-40.5961635220348,-3.92777652835409,
0.00218069315271673));
#38990=CARTESIAN_POINT('Ctrl Pts',(-40.5559110904575,-3.92375471024914,
-0.796030605954551));
#38991=CARTESIAN_POINT('Ctrl Pts',(-40.5156586588801,-3.68757556068199,
-1.59642886698926));
#38992=CARTESIAN_POINT('Ctrl Pts',(-40.4754062273028,-3.23574061561438,
-2.24706465527338));
#38993=CARTESIAN_POINT('Ctrl Pts',(-40.4092485100601,-2.49311793756043,
-3.31643057485933));
#38994=CARTESIAN_POINT('Ctrl Pts',(-40.3430907928174,-1.16793894235701,
-3.98123943456976));
#38995=CARTESIAN_POINT('Ctrl Pts',(-40.2769330755747,0.13324998928991,-3.93720222199338));
#38996=CARTESIAN_POINT('Ctrl Pts',(-40.210775358332,1.43443892093683,-3.89316500941701));
#38997=CARTESIAN_POINT('Ctrl Pts',(-40.1446176410892,2.71163778902724,-3.14028172455383));
#38998=CARTESIAN_POINT('Ctrl Pts',(-40.0784599238465,3.3802611498694,-2.02315383873767));
#38999=CARTESIAN_POINT('Ctrl Pts',(-40.0123022066038,4.04888451071156,-0.906025952921513));
#39000=CARTESIAN_POINT('Ctrl Pts',(-39.9461444893611,4.10893236430546,0.575346533847623));
#39001=CARTESIAN_POINT('Ctrl Pts',(-39.8799867721184,3.53292026636216,1.74292607073361));
#39002=CARTESIAN_POINT('Ctrl Pts',(-39.8138290548757,2.95690816841886,2.9105056076196));
#39003=CARTESIAN_POINT('Ctrl Pts',(-39.747671337633,1.74483611893836,3.76429219462244));
#39004=CARTESIAN_POINT('Ctrl Pts',(-39.6815136203903,0.451480429217691,
3.91350000875799));
#39005=CARTESIAN_POINT('Ctrl Pts',(-39.6153559031476,-0.84187526050298,
4.06270782289354));
#39006=CARTESIAN_POINT('Ctrl Pts',(-39.5491981859049,-2.21651459046383,
3.5073368641618));
#39007=CARTESIAN_POINT('Ctrl Pts',(-39.4830404686621,-3.0432527385527,2.50158543044344));
#39008=CARTESIAN_POINT('Ctrl Pts',(-39.4374148197864,-3.61341244219722,
1.80796927070229));
#39009=CARTESIAN_POINT('Ctrl Pts',(-39.3917891709106,-3.92298120014008,
0.900144640920363));
#39010=CARTESIAN_POINT('Ctrl Pts',(-39.3461635220348,-3.93009648465997,
-0.00327554246926138));
#39011=CARTESIAN_POINT('Origin',(-27.25,0.,0.));
#39012=CARTESIAN_POINT('',(-37.912836477965,-3.93936327777038,-0.000544856984334152));
#39013=CARTESIAN_POINT('',(-38.0961635220349,-3.93942817610916,-0.000298174263498583));
#39014=CARTESIAN_POINT('',(-27.25,-3.933,-4.81653586104654E-16));
#39015=CARTESIAN_POINT('Ctrl Pts',(-37.912836477965,-3.93936327777038,-0.000544856984334152));
#39016=CARTESIAN_POINT('Ctrl Pts',(-37.9775060292436,-3.93689177231164,
1.2721842897132));
#39017=CARTESIAN_POINT('Ctrl Pts',(-38.0421755805223,-3.26357656031174,
2.54715895566795));
#39018=CARTESIAN_POINT('Ctrl Pts',(-38.1068451318009,-2.21006500503054,
3.2611241206237));
#39019=CARTESIAN_POINT('Ctrl Pts',(-38.1730028490436,-1.13231020067255,
3.991518944314));
#39020=CARTESIAN_POINT('Ctrl Pts',(-38.2391605662863,0.343340319979478,
4.13478745500189));
#39021=CARTESIAN_POINT('Ctrl Pts',(-38.305318283529,1.54146800159971,3.62535436290282));
#39022=CARTESIAN_POINT('Ctrl Pts',(-38.3714760007717,2.73959568321995,3.11592127080375));
#39023=CARTESIAN_POINT('Ctrl Pts',(-38.4376337180145,3.66020052580842,1.95378657591777));
#39024=CARTESIAN_POINT('Ctrl Pts',(-38.5037914352572,3.88191338802384,0.670869811852932));
#39025=CARTESIAN_POINT('Ctrl Pts',(-38.5699491524999,4.10362625023927,-0.612046952211922));
#39026=CARTESIAN_POINT('Ctrl Pts',(-38.6361068697426,3.62644713208157,-2.01574578545561));
#39027=CARTESIAN_POINT('Ctrl Pts',(-38.7022645869853,2.66878522062258,-2.89774106896403));
#39028=CARTESIAN_POINT('Ctrl Pts',(-38.768422304228,1.7111233091636,-3.77973635247244));
#39029=CARTESIAN_POINT('Ctrl Pts',(-38.8345800214707,0.272978604403351,
-4.14002808624563));
#39030=CARTESIAN_POINT('Ctrl Pts',(-38.9007377387134,-0.987397088610618,
-3.81370749349994));
#39031=CARTESIAN_POINT('Ctrl Pts',(-38.9668954559561,-2.24777278162459,
-3.48738690075425));
#39032=CARTESIAN_POINT('Ctrl Pts',(-39.0330531731989,-3.33037946289226,
-2.47445398148969));
#39033=CARTESIAN_POINT('Ctrl Pts',(-39.0992108904416,-3.73969828807051,
-1.23853727064504));
#39034=CARTESIAN_POINT('Ctrl Pts',(-39.120419419616,-3.87091578781602,-0.842332916691583));
#39035=CARTESIAN_POINT('Ctrl Pts',(-39.1416279487905,-3.9329404947859,-0.423212849728327));
#39036=CARTESIAN_POINT('Ctrl Pts',(-39.162836477965,-3.92975286260395,-0.00317618749887255));
#39037=CARTESIAN_POINT('Ctrl Pts',(-39.3461635220348,-3.93009648465997,
-0.00327554246926138));
#39038=CARTESIAN_POINT('Ctrl Pts',(-39.3256314536679,-3.93329844478136,
-0.409825047550122));
#39039=CARTESIAN_POINT('Ctrl Pts',(-39.305099385301,-3.8752504360904,-0.815482606504164));
#39040=CARTESIAN_POINT('Ctrl Pts',(-39.284567316934,-3.75213744234363,-1.20032558511363));
#39041=CARTESIAN_POINT('Ctrl Pts',(-39.2184095996913,-3.3554470318288,-2.44035325824738));
#39042=CARTESIAN_POINT('Ctrl Pts',(-39.1522518824486,-2.28322924458223,
-3.46427669580993));
#39043=CARTESIAN_POINT('Ctrl Pts',(-39.0860941652059,-1.02624783443413,
-3.80343690349066));
#39044=CARTESIAN_POINT('Ctrl Pts',(-39.0199364479632,0.230733575713977,
-4.1425971111714));
#39045=CARTESIAN_POINT('Ctrl Pts',(-38.9537787307205,1.67247860876359,-3.79699408897032));
#39046=CARTESIAN_POINT('Ctrl Pts',(-38.8876210134778,2.63908755693015,-2.92481345787587));
#39047=CARTESIAN_POINT('Ctrl Pts',(-38.821463296235,3.60569650509673,-2.05263282678141));
#39048=CARTESIAN_POINT('Ctrl Pts',(-38.7553055789924,4.09716936838019,-0.653874586793549));
#39049=CARTESIAN_POINT('Ctrl Pts',(-38.6891478617496,3.88855458361905,0.631236997276519));
#39050=CARTESIAN_POINT('Ctrl Pts',(-38.6229901445069,3.67993979885791,1.91634858134655));
#39051=CARTESIAN_POINT('Ctrl Pts',(-38.5568324272642,2.77123736605219,3.08781350949882));
#39052=CARTESIAN_POINT('Ctrl Pts',(-38.4906747100215,1.57836858621257,3.60944171619002));
#39053=CARTESIAN_POINT('Ctrl Pts',(-38.4245169927788,0.385499806372948,
4.13106992288121));
#39054=CARTESIAN_POINT('Ctrl Pts',(-38.3583592755361,-1.09153532050054,
4.00286140811134));
#39055=CARTESIAN_POINT('Ctrl Pts',(-38.2922015582934,-2.17668449232393,
3.28349836567523));
#39056=CARTESIAN_POINT('Ctrl Pts',(-38.2268555462072,-3.24851970449009,
2.57296136372699));
#39057=CARTESIAN_POINT('Ctrl Pts',(-38.161509534121,-3.93802625789471,1.28568688300243));
#39058=CARTESIAN_POINT('Ctrl Pts',(-38.0961635220349,-3.93942817610916,
-0.000298174263498583));
#39059=CARTESIAN_POINT('Origin',(-27.25,0.,0.));
#39060=CARTESIAN_POINT('',(-36.662836477965,-3.93134770437533,0.00351664141719457));
#39061=CARTESIAN_POINT('',(-36.8461635220348,-3.93096795489117,0.00346177198455457));
#39062=CARTESIAN_POINT('',(-27.25,-3.933,-4.81653586104654E-16));
#39063=CARTESIAN_POINT('Ctrl Pts',(-36.662836477965,-3.93134770437533,0.00351664141719457));
#39064=CARTESIAN_POINT('Ctrl Pts',(-36.6810686752113,-3.93447342139821,
0.36423620257401));
#39065=CARTESIAN_POINT('Ctrl Pts',(-36.6993008724577,-3.88890920393724,
0.724180603369993));
#39066=CARTESIAN_POINT('Ctrl Pts',(-36.717533069704,-3.79150170657231,1.06950112932788));
#39067=CARTESIAN_POINT('Ctrl Pts',(-36.7836907869467,-3.43804690455791,
2.32253812787313));
#39068=CARTESIAN_POINT('Ctrl Pts',(-36.8498485041894,-2.40197766182226,
3.38302426616653));
#39069=CARTESIAN_POINT('Ctrl Pts',(-36.9160062214321,-1.15751221727247,
3.76556547193636));
#39070=CARTESIAN_POINT('Ctrl Pts',(-36.9821639386749,0.0869532272773088,
4.1481066777062));
#39071=CARTESIAN_POINT('Ctrl Pts',(-37.0483216559175,1.53981487364122,3.85270295095248));
#39072=CARTESIAN_POINT('Ctrl Pts',(-37.1144793731602,2.53608483983638,3.01456324228343));
#39073=CARTESIAN_POINT('Ctrl Pts',(-37.180637090403,3.53235480603154,2.17642353361439));
#39074=CARTESIAN_POINT('Ctrl Pts',(-37.2467948076457,4.07203309205794,0.795547843030021));
#39075=CARTESIAN_POINT('Ctrl Pts',(-37.3129525248884,3.90810407789765,-0.49602456884117));
#39076=CARTESIAN_POINT('Ctrl Pts',(-37.3791102421311,3.74417506373737,-1.78759698071236));
#39077=CARTESIAN_POINT('Ctrl Pts',(-37.4452679593738,2.87663874939039,-2.98986611387037));
#39078=CARTESIAN_POINT('Ctrl Pts',(-37.5114256766165,1.70257433208425,-3.55254254025229));
#39079=CARTESIAN_POINT('Ctrl Pts',(-37.5775833938592,0.528509914778081,
-4.11521896663422));
#39080=CARTESIAN_POINT('Ctrl Pts',(-37.643741111102,-0.952082605487279,
-4.03830268624002));
#39081=CARTESIAN_POINT('Ctrl Pts',(-37.7098988283447,-2.06152267558061,
-3.35699897447725));
#39082=CARTESIAN_POINT('Ctrl Pts',(-37.7760565455874,-3.17096274567392,
-2.6756952627145));
#39083=CARTESIAN_POINT('Ctrl Pts',(-37.8422142628301,-3.90925036559522,
-1.39000411958323));
#39084=CARTESIAN_POINT('Ctrl Pts',(-37.9083719800728,-3.93846463152386,
-0.0883979796712423));
#39085=CARTESIAN_POINT('Ctrl Pts',(-37.9098601460368,-3.93912178352415,
-0.0591193703603289));
#39086=CARTESIAN_POINT('Ctrl Pts',(-37.9113483120009,-3.93942015168138,
-0.0298327082243094));
#39087=CARTESIAN_POINT('Ctrl Pts',(-37.912836477965,-3.93936327777038,-0.000544856984334152));
#39088=CARTESIAN_POINT('Ctrl Pts',(-38.0961635220349,-3.93942817610916,
-0.000298174263498583));
#39089=CARTESIAN_POINT('Ctrl Pts',(-38.0953518168783,-3.93944559024367,
-0.0162722279033564));
#39090=CARTESIAN_POINT('Ctrl Pts',(-38.0945401117218,-3.93935683166498,
-0.032246082588608));
#39091=CARTESIAN_POINT('Ctrl Pts',(-38.0937284065652,-3.93916131431453,
-0.0482186304571659));
#39092=CARTESIAN_POINT('Ctrl Pts',(-38.0275706893225,-3.92322574770849,
-1.35005501405111));
#39093=CARTESIAN_POINT('Ctrl Pts',(-37.9614129720798,-3.19809139772313,
-2.64321021113658));
#39094=CARTESIAN_POINT('Ctrl Pts',(-37.8952552548371,-2.09565879787217,
-3.33579542229681));
#39095=CARTESIAN_POINT('Ctrl Pts',(-37.8290975375944,-0.993226198021244,
-4.02838063345702));
#39096=CARTESIAN_POINT('Ctrl Pts',(-37.7629398203517,0.486504651695298,
-4.12039585869199));
#39097=CARTESIAN_POINT('Ctrl Pts',(-37.696782103109,1.66624759252964,-3.56972489933111));
#39098=CARTESIAN_POINT('Ctrl Pts',(-37.6306243858663,2.84599053336401,-3.01905393997023));
#39099=CARTESIAN_POINT('Ctrl Pts',(-37.5644666686236,3.72574556531621,-1.8256967960135));
#39100=CARTESIAN_POINT('Ctrl Pts',(-37.4983089513809,3.90284087388428,-0.535863797670248));
#39101=CARTESIAN_POINT('Ctrl Pts',(-37.4321512341382,4.07993618245235,0.753969200673001));
#39102=CARTESIAN_POINT('Ctrl Pts',(-37.3659935168954,3.55437176763629,2.14027805340274));
#39103=CARTESIAN_POINT('Ctrl Pts',(-37.2998357996527,2.56670320327809,2.98853669256333));
#39104=CARTESIAN_POINT('Ctrl Pts',(-37.23367808241,1.5790346389199,3.83679533172392));
#39105=CARTESIAN_POINT('Ctrl Pts',(-37.1675203651673,0.129261925019584,
4.14700375731534));
#39106=CARTESIAN_POINT('Ctrl Pts',(-37.1013626479246,-1.1190408886942,3.77717677451637));
#39107=CARTESIAN_POINT('Ctrl Pts',(-37.0352049306819,-2.36734370240797,
3.4073497917174));
#39108=CARTESIAN_POINT('Ctrl Pts',(-36.9690472134392,-3.41417661593523,
2.35748740052801));
#39109=CARTESIAN_POINT('Ctrl Pts',(-36.9028894961965,-3.78039476114712,
1.10812108833231));
#39110=CARTESIAN_POINT('Ctrl Pts',(-36.8839808381426,-3.88506423841353,
0.751037419700503));
#39111=CARTESIAN_POINT('Ctrl Pts',(-36.8650721800887,-3.93413538382226,
0.377656594845544));
#39112=CARTESIAN_POINT('Ctrl Pts',(-36.8461635220348,-3.93096795489117,
0.00346177198455457));
#39113=CARTESIAN_POINT('Origin',(-27.25,0.,0.));
#39114=CARTESIAN_POINT('',(-35.412836477965,-3.92712485552383,-0.0015385046896832));
#39115=CARTESIAN_POINT('',(-35.5961635220348,-3.92729240225598,-0.00173544043971706));
#39116=CARTESIAN_POINT('',(-27.25,-3.933,-4.81653586104654E-16));
#39117=CARTESIAN_POINT('Ctrl Pts',(-35.412836477965,-3.92712485552383,-0.0015385046896832));
#39118=CARTESIAN_POINT('Ctrl Pts',(-35.4507890384217,-3.92447549046237,
0.751378600752031));
#39119=CARTESIAN_POINT('Ctrl Pts',(-35.4887415988785,-3.71620164740591,
1.50565253191416));
#39120=CARTESIAN_POINT('Ctrl Pts',(-35.5266941593352,-3.3117103233741,2.13351648473401));
#39121=CARTESIAN_POINT('Ctrl Pts',(-35.5928518765779,-2.60661368903953,
3.22798930442411));
#39122=CARTESIAN_POINT('Ctrl Pts',(-35.6590095938206,-1.30528330217824,
3.93834805145753));
#39123=CARTESIAN_POINT('Ctrl Pts',(-35.7251673110634,-0.00334982031690134,
3.93945511908414));
#39124=CARTESIAN_POINT('Ctrl Pts',(-35.7913250283061,1.29858366154446,3.94056218671074));
#39125=CARTESIAN_POINT('Ctrl Pts',(-35.8574827455488,2.60112023840593,3.23241757493054));
#39126=CARTESIAN_POINT('Ctrl Pts',(-35.9236404627915,3.30807716869666,2.13914546081425));
#39127=CARTESIAN_POINT('Ctrl Pts',(-35.9897981800342,4.01503409898737,1.045873346698));
#39128=CARTESIAN_POINT('Ctrl Pts',(-36.0559558972769,4.12641138270738,-0.432526269754304));
#39129=CARTESIAN_POINT('Ctrl Pts',(-36.1221136145196,3.59123063234998,-1.61937654726919));
#39130=CARTESIAN_POINT('Ctrl Pts',(-36.1882713317623,3.05604988199257,-2.8062268247841));
#39131=CARTESIAN_POINT('Ctrl Pts',(-36.254429049005,1.87431109755773,-3.70152776336159));
#39132=CARTESIAN_POINT('Ctrl Pts',(-36.3205867662477,0.586906781291004,
-3.89549204679576));
#39133=CARTESIAN_POINT('Ctrl Pts',(-36.3867444834904,-0.700497534975741,
-4.08945633022993));
#39134=CARTESIAN_POINT('Ctrl Pts',(-36.4529022007332,-2.09356738307438,
-3.58208395852077));
#39135=CARTESIAN_POINT('Ctrl Pts',(-36.5190599179759,-2.95468212647712,
-2.60560384326762));
#39136=CARTESIAN_POINT('Ctrl Pts',(-36.5669854379723,-3.57848496572447,
-1.89822881220443));
#39137=CARTESIAN_POINT('Ctrl Pts',(-36.6149109579686,-3.92313138180822,
-0.944678044485885));
#39138=CARTESIAN_POINT('Ctrl Pts',(-36.662836477965,-3.93134770437533,0.00351664141719457));
#39139=CARTESIAN_POINT('Ctrl Pts',(-36.8461635220348,-3.93096795489117,
0.00346177198455457));
#39140=CARTESIAN_POINT('Ctrl Pts',(-36.798914462846,-3.92305316598257,-0.931578318282404));
#39141=CARTESIAN_POINT('Ctrl Pts',(-36.7516654036572,-3.58895920163905,
-1.87170103574137));
#39142=CARTESIAN_POINT('Ctrl Pts',(-36.7044163444683,-2.98110706244138,
-2.57532863510223));
#39143=CARTESIAN_POINT('Ctrl Pts',(-36.6382586272256,-2.12999784162727,
-3.56054181313891));
#39144=CARTESIAN_POINT('Ctrl Pts',(-36.5721009099829,-0.742176023102554,
-4.08209793601023));
#39145=CARTESIAN_POINT('Ctrl Pts',(-36.5059431927402,0.547139827084099,
-3.9012760612566));
#39146=CARTESIAN_POINT('Ctrl Pts',(-36.4397854754975,1.83645567727075,-3.72045418650296));
#39147=CARTESIAN_POINT('Ctrl Pts',(-36.3736277582548,3.02726555911932,-2.83725431412436));
#39148=CARTESIAN_POINT('Ctrl Pts',(-36.3074700410121,3.57452504726655,-1.65592499316225));
#39149=CARTESIAN_POINT('Ctrl Pts',(-36.2413123237694,4.12178453541378,-0.474595672200148));
#39150=CARTESIAN_POINT('Ctrl Pts',(-36.1751546065266,4.02549362985964,1.0048630973455));
#39151=CARTESIAN_POINT('Ctrl Pts',(-36.1089968892839,3.32972554672827,2.10528969027555));
#39152=CARTESIAN_POINT('Ctrl Pts',(-36.0428391720412,2.6339574635969,3.20571628320559));
#39153=CARTESIAN_POINT('Ctrl Pts',(-35.9766814547985,1.33871220288834,3.92711069952008));
#39154=CARTESIAN_POINT('Ctrl Pts',(-35.9105237375558,0.0368352049943507,
3.93928420708489));
#39155=CARTESIAN_POINT('Ctrl Pts',(-35.8443660203131,-1.26504179289966,
3.95145771464969));
#39156=CARTESIAN_POINT('Ctrl Pts',(-35.7782083030704,-2.57355052797908,
3.25441031346478));
#39157=CARTESIAN_POINT('Ctrl Pts',(-35.7120505858277,-3.28977474798118,
2.16718688720211));
#39158=CARTESIAN_POINT('Ctrl Pts',(-35.6734215645634,-3.70797298361485,
1.53236484976624));
#39159=CARTESIAN_POINT('Ctrl Pts',(-35.6347925432991,-3.92424311660023,
0.764519742442217));
#39160=CARTESIAN_POINT('Ctrl Pts',(-35.5961635220348,-3.92729240225598,
-0.00173544043971706));
#39161=CARTESIAN_POINT('Origin',(-27.25,0.,0.));
#39162=CARTESIAN_POINT('',(-34.162836477965,-3.93697895265161,-0.00271025535696023));
#39163=CARTESIAN_POINT('',(-34.3461635220348,-3.93731358771045,-0.00254698605159045));
#39164=CARTESIAN_POINT('',(-27.25,-3.933,-4.81653586104654E-16));
#39165=CARTESIAN_POINT('Ctrl Pts',(-34.162836477965,-3.93697895265161,-0.00271025535696023));
#39166=CARTESIAN_POINT('Ctrl Pts',(-34.2205094016322,-3.92802881866666,
1.13413956848541));
#39167=CARTESIAN_POINT('Ctrl Pts',(-34.2781823252993,-3.40846140270135,
2.27812248496691));
#39168=CARTESIAN_POINT('Ctrl Pts',(-34.3358552489664,-2.54120789046762,
3.01024588929201));
#39169=CARTESIAN_POINT('Ctrl Pts',(-34.4020129662092,-1.54636474758752,
3.85007869280399));
#39170=CARTESIAN_POINT('Ctrl Pts',(-34.4681706834519,-0.0940075806728428,
4.14795280206281));
#39171=CARTESIAN_POINT('Ctrl Pts',(-34.5343284006946,1.15110663308848,3.76752855010205));
#39172=CARTESIAN_POINT('Ctrl Pts',(-34.6004861179373,2.39622084684978,3.38710429814129));
#39173=CARTESIAN_POINT('Ctrl Pts',(-34.66664383518,3.43409210745772,2.32838168496089));
#39174=CARTESIAN_POINT('Ctrl Pts',(-34.7328015524227,3.78967737616872,1.07594760147943));
#39175=CARTESIAN_POINT('Ctrl Pts',(-34.7989592696654,4.14526264487973,-0.176486482002049));
#39176=CARTESIAN_POINT('Ctrl Pts',(-34.8651169869081,3.81856192169385,-1.62263203578459));
#39177=CARTESIAN_POINT('Ctrl Pts',(-34.9312747041508,2.95910907482034,-2.60057519404655));
#39178=CARTESIAN_POINT('Ctrl Pts',(-34.9974324213936,2.09965622794684,-3.5785183523085));
#39179=CARTESIAN_POINT('Ctrl Pts',(-35.0635901386363,0.707451257385696,
-4.08825911504983));
#39180=CARTESIAN_POINT('Ctrl Pts',(-35.129747855879,-0.58028106258638,-3.89648453673025));
#39181=CARTESIAN_POINT('Ctrl Pts',(-35.1959055731217,-1.86801338255846,
-3.70470995841067));
#39182=CARTESIAN_POINT('Ctrl Pts',(-35.2620632903644,-3.05127305194149,
-2.81142003903016));
#39183=CARTESIAN_POINT('Ctrl Pts',(-35.3282210076071,-3.58847144572904,
-1.62548163316652));
#39184=CARTESIAN_POINT('Ctrl Pts',(-35.3564261643931,-3.81749635096215,
-1.11987805326706));
#39185=CARTESIAN_POINT('Ctrl Pts',(-35.384631321179,-3.92909378083592,-0.561082966255875));
#39186=CARTESIAN_POINT('Ctrl Pts',(-35.412836477965,-3.92712485552383,-0.0015385046896832));
#39187=CARTESIAN_POINT('Ctrl Pts',(-35.5961635220348,-3.92729240225598,
-0.00173544043971706));
#39188=CARTESIAN_POINT('Ctrl Pts',(-35.5686348260564,-3.92946545388974,
-0.547801721206673));
#39189=CARTESIAN_POINT('Ctrl Pts',(-35.541106130078,-3.82335220054039,-1.09306054320404));
#39190=CARTESIAN_POINT('Ctrl Pts',(-35.5135774340996,-3.60486554173621,
-1.58879241013994));
#39191=CARTESIAN_POINT('Ctrl Pts',(-35.4474197168568,-3.07979241056439,
-2.78014882987897));
#39192=CARTESIAN_POINT('Ctrl Pts',(-35.3812619996142,-1.90570644329594,
-3.68546221801658));
#39193=CARTESIAN_POINT('Ctrl Pts',(-35.3151042823714,-0.619997378722377,
-3.89036246985969));
#39194=CARTESIAN_POINT('Ctrl Pts',(-35.2489465651287,0.665711685851162,
-4.09526272170278));
#39195=CARTESIAN_POINT('Ctrl Pts',(-35.182788847886,2.06304384772982,-3.59974983725139));
#39196=CARTESIAN_POINT('Ctrl Pts',(-35.1166311306433,2.93242757091785,-2.63062453380109));
#39197=CARTESIAN_POINT('Ctrl Pts',(-35.0504734134006,3.80181129410592,-1.66149923035074));
#39198=CARTESIAN_POINT('Ctrl Pts',(-34.9843156961579,4.14324657860332,-0.218761507901483));
#39199=CARTESIAN_POINT('Ctrl Pts',(-34.9181579789152,3.80045541456625,1.03723456286872));
#39200=CARTESIAN_POINT('Ctrl Pts',(-34.8520002616725,3.45766425052919,2.29323063363886));
#39201=CARTESIAN_POINT('Ctrl Pts',(-34.7858425444298,2.4306466379577,3.36248505272994));
#39202=CARTESIAN_POINT('Ctrl Pts',(-34.7196848271871,1.18947780297691,3.7555904266494));
#39203=CARTESIAN_POINT('Ctrl Pts',(-34.6535271099443,-0.0516910320038823,
4.14869580056886));
#39204=CARTESIAN_POINT('Ctrl Pts',(-34.5873693927016,-1.50701108939393,
3.86565212931673));
#39205=CARTESIAN_POINT('Ctrl Pts',(-34.5212116754589,-2.51036925030615,
3.0360110545966));
#39206=CARTESIAN_POINT('Ctrl Pts',(-34.4628622909842,-3.39530503008972,
2.30428922285262));
#39207=CARTESIAN_POINT('Ctrl Pts',(-34.4045129065095,-3.92866955648817,
1.14738125101164));
#39208=CARTESIAN_POINT('Ctrl Pts',(-34.3461635220348,-3.93731358771045,
-0.00254698605159045));
#39209=CARTESIAN_POINT('Origin',(-27.25,0.,0.));
#39210=CARTESIAN_POINT('',(-32.912836477965,-3.93548209384035,0.00323960751162838));
#39211=CARTESIAN_POINT('',(-33.0961635220348,-3.93508971521476,0.00333466163741802));
#39212=CARTESIAN_POINT('',(-27.25,-3.933,-4.81653586104654E-16));
#39213=CARTESIAN_POINT('Ctrl Pts',(-32.912836477965,-3.93548209384035,0.00323960751162838));
#39214=CARTESIAN_POINT('Ctrl Pts',(-32.9240720475999,-3.93745101947663,
0.224934599518961));
#39215=CARTESIAN_POINT('Ctrl Pts',(-32.9353076172347,-3.92033161139393,
0.446325502292901));
#39216=CARTESIAN_POINT('Ctrl Pts',(-32.9465431868695,-3.88304868935319,
0.664267064279747));
#39217=CARTESIAN_POINT('Ctrl Pts',(-33.0127009041123,-3.66351794062248,
1.94755902917007));
#39218=CARTESIAN_POINT('Ctrl Pts',(-33.078858621355,-2.74489081412106,3.11125767044752));
#39219=CARTESIAN_POINT('Ctrl Pts',(-33.1450163385977,-1.54763123269596,
3.62272762213202));
#39220=CARTESIAN_POINT('Ctrl Pts',(-33.2111740558404,-0.35037165127085,
4.13419757381653));
#39221=CARTESIAN_POINT('Ctrl Pts',(-33.2773317730831,1.12552038507792,3.99343883590807));
#39222=CARTESIAN_POINT('Ctrl Pts',(-33.3434894903258,2.20451577711144,3.26487795254908));
#39223=CARTESIAN_POINT('Ctrl Pts',(-33.4096472075685,3.28351116914494,2.53631706919011));
#39224=CARTESIAN_POINT('Ctrl Pts',(-33.4758049248112,3.96560991686318,1.21995404038064));
#39225=CARTESIAN_POINT('Ctrl Pts',(-33.5419626420539,3.93860927013953,-0.0816999005217973));
#39226=CARTESIAN_POINT('Ctrl Pts',(-33.6081203592966,3.91160862341588,-1.38335384142423));
#39227=CARTESIAN_POINT('Ctrl Pts',(-33.6742780765394,3.1755085822503,-2.67029869441967));
#39228=CARTESIAN_POINT('Ctrl Pts',(-33.7404357937821,2.06722877593257,-3.35348819060552));
#39229=CARTESIAN_POINT('Ctrl Pts',(-33.8065935110248,0.958948969614857,
-4.03667768679136));
#39230=CARTESIAN_POINT('Ctrl Pts',(-33.8727512282675,-0.521510601854994,
-4.11611182616768));
#39231=CARTESIAN_POINT('Ctrl Pts',(-33.9389089455102,-1.69653023720889,
-3.55543288655689));
#39232=CARTESIAN_POINT('Ctrl Pts',(-34.0050666627529,-2.87154987256281,
-2.99475394694609));
#39233=CARTESIAN_POINT('Ctrl Pts',(-34.0712243799956,-3.74112957180075,
-1.79396192834816));
#39234=CARTESIAN_POINT('Ctrl Pts',(-34.1373820972383,-3.90725486199698,
-0.502670170166627));
#39235=CARTESIAN_POINT('Ctrl Pts',(-34.1458668908139,-3.92856059704561,
-0.337060707346072));
#39236=CARTESIAN_POINT('Ctrl Pts',(-34.1543516843894,-3.93829568907673,
-0.169962675875666));
#39237=CARTESIAN_POINT('Ctrl Pts',(-34.162836477965,-3.93697895265161,-0.00271025535696023));
#39238=CARTESIAN_POINT('Ctrl Pts',(-34.3461635220348,-3.93731358771045,
-0.00254698605159045));
#39239=CARTESIAN_POINT('Ctrl Pts',(-34.3383551892668,-3.93847033465557,
-0.156430740185009));
#39240=CARTESIAN_POINT('Ctrl Pts',(-34.3305468564988,-3.93023045225109,
-0.310189502096346));
#39241=CARTESIAN_POINT('Ctrl Pts',(-34.3227385237308,-3.91217899916458,
-0.462787613286053));
#39242=CARTESIAN_POINT('Ctrl Pts',(-34.2565808064881,-3.75923432267645,
-1.75570672826033));
#39243=CARTESIAN_POINT('Ctrl Pts',(-34.1904230892453,-2.90194870526589,
-2.96530648002073));
#39244=CARTESIAN_POINT('Ctrl Pts',(-34.1242653720026,-1.73270950769983,
-3.5379421502396));
#39245=CARTESIAN_POINT('Ctrl Pts',(-34.0581076547599,-0.563470310133773,
-4.11057782045846));
#39246=CARTESIAN_POINT('Ctrl Pts',(-33.9919499375172,0.917722467587795,
-4.04624940913581));
#39247=CARTESIAN_POINT('Ctrl Pts',(-33.9257922202745,2.03291352908098,-3.37440061044845));
#39248=CARTESIAN_POINT('Ctrl Pts',(-33.8596345030318,3.14810459057416,-2.7025518117611));
#39249=CARTESIAN_POINT('Ctrl Pts',(-33.7934767857891,3.89729393583897,-1.42318262570904));
#39250=CARTESIAN_POINT('Ctrl Pts',(-33.7273190685464,3.93757084301924,-0.121871870093793));
#39251=CARTESIAN_POINT('Ctrl Pts',(-33.6611613513037,3.9778477501995,1.17943888552147));
#39252=CARTESIAN_POINT('Ctrl Pts',(-33.595003634061,3.30921221929523,2.50269121069989));
#39253=CARTESIAN_POINT('Ctrl Pts',(-33.5288459168182,2.23770476464396,3.24222057898674));
#39254=CARTESIAN_POINT('Ctrl Pts',(-33.4626881995756,1.16619730999271,3.98174994727357));
#39255=CARTESIAN_POINT('Ctrl Pts',(-33.3965304823328,-0.308182068405588,
4.1375563586688));
#39256=CARTESIAN_POINT('Ctrl Pts',(-33.3303727650901,-1.5105966285017,3.63832581312816));
#39257=CARTESIAN_POINT('Ctrl Pts',(-33.2642150478474,-2.71301118859784,
3.13909526758751));
#39258=CARTESIAN_POINT('Ctrl Pts',(-33.1980573306047,-3.64346093039182,
1.98482776511106));
#39259=CARTESIAN_POINT('Ctrl Pts',(-33.131899613362,-3.87607061336398,0.703841954370138));
#39260=CARTESIAN_POINT('Ctrl Pts',(-33.1199875829196,-3.91795315919898,
0.47319400263047));
#39261=CARTESIAN_POINT('Ctrl Pts',(-33.1080755524772,-3.93721185766393,
0.238437866459535));
#39262=CARTESIAN_POINT('Ctrl Pts',(-33.0961635220348,-3.93508971521476,
0.00333466163741802));
#39263=CARTESIAN_POINT('Origin',(-27.25,0.,0.));
#39264=CARTESIAN_POINT('',(-31.662836477965,-3.92666097892795,0.000687624971145162));
#39265=CARTESIAN_POINT('',(-31.8461635220349,-3.92660201554812,0.000470019213647162));
#39266=CARTESIAN_POINT('',(-27.25,-3.933,-4.81653586104654E-16));
#39267=CARTESIAN_POINT('Ctrl Pts',(-31.662836477965,-3.92666097892795,0.000687624971145162));
#39268=CARTESIAN_POINT('Ctrl Pts',(-31.6937924108103,-3.92762034739937,
0.614984183704047));
#39269=CARTESIAN_POINT('Ctrl Pts',(-31.7247483436555,-3.79213432965767,
1.22888030589506));
#39270=CARTESIAN_POINT('Ctrl Pts',(-31.7557042765008,-3.51797781227477,
1.77289310701935));
#39271=CARTESIAN_POINT('Ctrl Pts',(-31.8218619937435,-2.93206203813433,
2.93553437688886));
#39272=CARTESIAN_POINT('Ctrl Pts',(-31.8880197109862,-1.71277652222822,
3.77898749115005));
#39273=CARTESIAN_POINT('Ctrl Pts',(-31.9541774282289,-0.418199244510039,
3.91719635051213));
#39274=CARTESIAN_POINT('Ctrl Pts',(-32.0203351454716,0.87637803320812,4.05540520987422));
#39275=CARTESIAN_POINT('Ctrl Pts',(-32.0864928627143,2.24624707273834,3.48836981433722));
#39276=CARTESIAN_POINT('Ctrl Pts',(-32.152650579957,3.06440645693195,2.47562737973389));
#39277=CARTESIAN_POINT('Ctrl Pts',(-32.2188082971997,3.88256584112558,1.46288494513054));
#39278=CARTESIAN_POINT('Ctrl Pts',(-32.2849660144424,4.14901556998256,0.0044354714608888));
#39279=CARTESIAN_POINT('Ctrl Pts',(-32.3511237316851,3.74179919892956,-1.23217556032592));
#39280=CARTESIAN_POINT('Ctrl Pts',(-32.4172814489278,3.33458282787656,-2.46878659211269));
#39281=CARTESIAN_POINT('Ctrl Pts',(-32.4834391661706,2.25370035691356,-3.48355918201663));
#39282=CARTESIAN_POINT('Ctrl Pts',(-32.5495968834133,0.993881443772989,
-3.81202276125131));
#39283=CARTESIAN_POINT('Ctrl Pts',(-32.615754600656,-0.265937469367559,
-4.14048634048598));
#39284=CARTESIAN_POINT('Ctrl Pts',(-32.6819123178987,-1.7046928246857,-3.78264090905147));
#39285=CARTESIAN_POINT('Ctrl Pts',(-32.7480700351414,-2.66385331686478,
-2.90227554908263));
#39286=CARTESIAN_POINT('Ctrl Pts',(-32.8029921827493,-3.46011951719077,
-2.17142269828554));
#39287=CARTESIAN_POINT('Ctrl Pts',(-32.8579143303571,-3.92585751511942,
-1.08045845771079));
#39288=CARTESIAN_POINT('Ctrl Pts',(-32.912836477965,-3.93548209384035,0.00323960751162838));
#39289=CARTESIAN_POINT('Ctrl Pts',(-33.0961635220348,-3.93508971521476,
0.00333466163741802));
#39290=CARTESIAN_POINT('Ctrl Pts',(-33.0419178352345,-3.92542578132876,
-1.06729178414136));
#39291=CARTESIAN_POINT('Ctrl Pts',(-32.9876721484342,-3.4723741720033,-2.14511560644448));
#39292=CARTESIAN_POINT('Ctrl Pts',(-32.9334264616339,-2.69331962574125,
-2.87495152830659));
#39293=CARTESIAN_POINT('Ctrl Pts',(-32.8672687443912,-1.74318933099608,
-3.76505508123703));
#39294=CARTESIAN_POINT('Ctrl Pts',(-32.8011110271485,-0.308159117355434,
-4.13755806809258));
#39295=CARTESIAN_POINT('Ctrl Pts',(-32.7349533099057,0.954944740814757,
-3.82196251139459));
#39296=CARTESIAN_POINT('Ctrl Pts',(-32.668795592663,2.21804859898495,-3.50636695469659));
#39297=CARTESIAN_POINT('Ctrl Pts',(-32.6026378754203,3.30922610168469,-2.50267285444504));
#39298=CARTESIAN_POINT('Ctrl Pts',(-32.5364801581776,3.72903546228296,-1.27028005477198));
#39299=CARTESIAN_POINT('Ctrl Pts',(-32.4703224409349,4.14884482288123,-0.0378872550989129));
#39300=CARTESIAN_POINT('Ctrl Pts',(-32.4041647236922,3.89728604137803,1.42320424399567));
#39301=CARTESIAN_POINT('Ctrl Pts',(-32.3380070064495,3.08949984140983,2.44423968269154));
#39302=CARTESIAN_POINT('Ctrl Pts',(-32.2718492892068,2.28171364144163,3.46527512138741));
#39303=CARTESIAN_POINT('Ctrl Pts',(-32.205691571964,0.917700023008417,4.04625449968457));
#39304=CARTESIAN_POINT('Ctrl Pts',(-32.1395338547213,-0.378219675799687,
3.92125831505059));
#39305=CARTESIAN_POINT('Ctrl Pts',(-32.0733761374786,-1.67413937460779,
3.7962621304166));
#39306=CARTESIAN_POINT('Ctrl Pts',(-32.0072184202359,-2.90196515379079,
2.96529038285145));
#39307=CARTESIAN_POINT('Ctrl Pts',(-31.9410607029932,-3.49971007785051,
1.80868633751321));
#39308=CARTESIAN_POINT('Ctrl Pts',(-31.9094283093405,-3.78551351137053,
1.2556721769985));
#39309=CARTESIAN_POINT('Ctrl Pts',(-31.8777959156877,-3.92727155150004,
0.628213868479639));
#39310=CARTESIAN_POINT('Ctrl Pts',(-31.8461635220349,-3.92660201554812,
0.000470019213647162));
#39311=CARTESIAN_POINT('Origin',(-27.25,0.,0.));
#39312=CARTESIAN_POINT('',(-30.412836477965,-3.93295883055164,-0.00359432436683793));
#39313=CARTESIAN_POINT('',(-30.5961635220349,-3.93336445157121,-0.00357663055094762));
#39314=CARTESIAN_POINT('',(-27.25,-3.933,-4.81653586104654E-16));
#39315=CARTESIAN_POINT('Ctrl Pts',(-30.412836477965,-3.93295883055164,-0.00359432436683793));
#39316=CARTESIAN_POINT('Ctrl Pts',(-30.4635127740207,-3.923765255997,0.997977755989756));
#39317=CARTESIAN_POINT('Ctrl Pts',(-30.5141890700763,-3.5341466447474,2.00591009962987));
#39318=CARTESIAN_POINT('Ctrl Pts',(-30.564865366132,-2.84408915743405,2.72588971184463));
#39319=CARTESIAN_POINT('Ctrl Pts',(-30.6310230833747,-1.94322165763196,
3.66582043513792));
#39320=CARTESIAN_POINT('Ctrl Pts',(-30.6971808006174,-0.530309991741809,
4.11498738588874));
#39321=CARTESIAN_POINT('Ctrl Pts',(-30.7633385178601,0.74794342470998,3.86780279874859));
#39322=CARTESIAN_POINT('Ctrl Pts',(-30.8294962351028,2.02619684116181,3.62061821160844));
#39323=CARTESIAN_POINT('Ctrl Pts',(-30.8956539523455,3.16979200817529,2.67708208657726));
#39324=CARTESIAN_POINT('Ctrl Pts',(-30.9618116695882,3.65529510129681,1.46905941983634));
#39325=CARTESIAN_POINT('Ctrl Pts',(-31.027969386831,4.14079819441831,0.26103675309547));
#39326=CARTESIAN_POINT('Ctrl Pts',(-31.0941271040737,3.96820921364796,-1.21147245535508));
#39327=CARTESIAN_POINT('Ctrl Pts',(-31.1602848213164,3.21652369243056,-2.27448745712242));
#39328=CARTESIAN_POINT('Ctrl Pts',(-31.2264425385591,2.46483817121316,-3.33750245888977));
#39329=CARTESIAN_POINT('Ctrl Pts',(-31.2926002558018,1.13405610954868,-3.99102325397385));
#39330=CARTESIAN_POINT('Ctrl Pts',(-31.3587579730445,-0.166711537791714,
-3.93592747897385));
#39331=CARTESIAN_POINT('Ctrl Pts',(-31.4249156902872,-1.46747918513211,
-3.88083170397386));
#39332=CARTESIAN_POINT('Ctrl Pts',(-31.4910734075299,-2.73823241814845,
-3.1171193588898));
#39333=CARTESIAN_POINT('Ctrl Pts',(-31.5572311247726,-3.39733601846922,
-1.99434847360887));
#39334=CARTESIAN_POINT('Ctrl Pts',(-31.5924329091701,-3.74803770227979,
-1.39693459237704));
#39335=CARTESIAN_POINT('Ctrl Pts',(-31.6276346935675,-3.92557002546655,
-0.697864575820828));
#39336=CARTESIAN_POINT('Ctrl Pts',(-31.662836477965,-3.92666097892795,0.000687624971145162));
#39337=CARTESIAN_POINT('Ctrl Pts',(-31.8461635220349,-3.92660201554812,
0.000470019213647162));
#39338=CARTESIAN_POINT('Ctrl Pts',(-31.8116381984449,-3.92587124741059,
-0.684683932946426));
#39339=CARTESIAN_POINT('Ctrl Pts',(-31.777112874855,-3.75547031300368,-1.37017804217001));
#39340=CARTESIAN_POINT('Ctrl Pts',(-31.7425875512651,-3.41750273201399,
-1.95958974614389));
#39341=CARTESIAN_POINT('Ctrl Pts',(-31.6764298340224,-2.76988639318133,
-3.08902544135141));
#39342=CARTESIAN_POINT('Ctrl Pts',(-31.6102721167797,-1.50698964657953,
-3.86566048865513));
#39343=CARTESIAN_POINT('Ctrl Pts',(-31.544114399537,-0.206851725873873,
-3.93402202078463));
#39344=CARTESIAN_POINT('Ctrl Pts',(-31.4779566822943,1.09328619483184,-4.00238355291413));
#39345=CARTESIAN_POINT('Ctrl Pts',(-31.4117989650515,2.4306652896414,-3.36247156986939));
#39346=CARTESIAN_POINT('Ctrl Pts',(-31.3456412478088,3.19315508220056,-2.30717955901402));
#39347=CARTESIAN_POINT('Ctrl Pts',(-31.2794835305661,3.95564487475968,-1.2518875481587));
#39348=CARTESIAN_POINT('Ctrl Pts',(-31.2133258133234,4.1432453650684,0.218784490507221));
#39349=CARTESIAN_POINT('Ctrl Pts',(-31.1471680960807,3.67009011634552,1.43169669777447));
#39350=CARTESIAN_POINT('Ctrl Pts',(-31.081010378838,3.19693486762262,2.64460890504174));
#39351=CARTESIAN_POINT('Ctrl Pts',(-31.0148526615953,2.06302387986814,3.59976128091032));
#39352=CARTESIAN_POINT('Ctrl Pts',(-30.9486949443526,0.787358441326591,
3.85997196639913));
#39353=CARTESIAN_POINT('Ctrl Pts',(-30.8825372271099,-0.488306997214944,
4.12018265188792));
#39354=CARTESIAN_POINT('Ctrl Pts',(-30.8163795098671,-1.90572688654355,
3.68545164699692));
#39355=CARTESIAN_POINT('Ctrl Pts',(-30.7502217926244,-2.81613535659577,
2.75475925442616));
#39356=CARTESIAN_POINT('Ctrl Pts',(-30.6988690357612,-3.52281005392954,
2.03233982790978));
#39357=CARTESIAN_POINT('Ctrl Pts',(-30.647516278898,-3.92400372217985,1.01109716125747));
#39358=CARTESIAN_POINT('Ctrl Pts',(-30.5961635220349,-3.93336445157121,
-0.00357663055094761));
#39359=CARTESIAN_POINT('Origin',(-27.25,0.,0.));
#39360=CARTESIAN_POINT('',(-29.162836477965,-3.93875478927679,0.00150291653159836));
#39361=CARTESIAN_POINT('',(-29.3461635220348,-3.93853086460256,0.00172150567391906));
#39362=CARTESIAN_POINT('',(-27.25,-3.933,-4.81653586104654E-16));
#39363=CARTESIAN_POINT('Ctrl Pts',(-29.162836477965,-3.93875478927679,0.00150291653159836));
#39364=CARTESIAN_POINT('Ctrl Pts',(-29.1670754199883,-3.93916252700776,
0.0849618398189939));
#39365=CARTESIAN_POINT('Ctrl Pts',(-29.1713143620117,-3.93673966426794,
0.168396650786846));
#39366=CARTESIAN_POINT('Ctrl Pts',(-29.1755533040351,-3.93141099567647,
0.251645464192195));
#39367=CARTESIAN_POINT('Ctrl Pts',(-29.2417110212778,-3.84824577472923,
1.55092047850407));
#39368=CARTESIAN_POINT('Ctrl Pts',(-29.3078687385205,-3.05727712238509,
2.80488974298552));
#39369=CARTESIAN_POINT('Ctrl Pts',(-29.3740264557632,-1.92053852624666,
3.4396002130737));
#39370=CARTESIAN_POINT('Ctrl Pts',(-29.4401841730059,-0.783799930108228,
4.07431068316188));
#39371=CARTESIAN_POINT('Ctrl Pts',(-29.5063418902486,0.698708609824502,
4.08976235885678));
#39372=CARTESIAN_POINT('Ctrl Pts',(-29.5724996074913,1.84842956093395,3.4788828688014));
#39373=CARTESIAN_POINT('Ctrl Pts',(-29.638657324734,2.99815051204339,2.86800337874602));
#39374=CARTESIAN_POINT('Ctrl Pts',(-29.7048150419767,3.81508387432956,1.63079272294036));
#39375=CARTESIAN_POINT('Ctrl Pts',(-29.7709727592195,3.92531187821855,0.333533379574904));
#39376=CARTESIAN_POINT('Ctrl Pts',(-29.8371304764622,4.03553988210755,-0.963725963790554));
#39377=CARTESIAN_POINT('Ctrl Pts',(-29.9032881937049,3.43906252759938,-2.32103399471581));
#39378=CARTESIAN_POINT('Ctrl Pts',(-29.9694459109476,2.40889288074741,-3.11713858300506));
#39379=CARTESIAN_POINT('Ctrl Pts',(-30.0356036281903,1.3787232338954,-3.91324317129434));
#39380=CARTESIAN_POINT('Ctrl Pts',(-30.101761345433,-0.085138705300437,
-4.14814431694758));
#39381=CARTESIAN_POINT('Ctrl Pts',(-30.1679190626757,-1.31267012159303,
-3.71432564652741));
#39382=CARTESIAN_POINT('Ctrl Pts',(-30.2340767799184,-2.54020153788559,
-3.28050697610725));
#39383=CARTESIAN_POINT('Ctrl Pts',(-30.3002344971611,-3.53140243127492,
-2.17796848961372));
#39384=CARTESIAN_POINT('Ctrl Pts',(-30.3663922144039,-3.83259121111256,
-0.911351998449073));
#39385=CARTESIAN_POINT('Ctrl Pts',(-30.3818736355909,-3.90307173178068,
-0.614953872887294));
#39386=CARTESIAN_POINT('Ctrl Pts',(-30.397355056778,-3.93576743360619,-0.309570893928312));
#39387=CARTESIAN_POINT('Ctrl Pts',(-30.412836477965,-3.93295883055164,-0.00359432436683793));
#39388=CARTESIAN_POINT('Ctrl Pts',(-30.5961635220349,-3.93336445157121,
-0.00357663055094761));
#39389=CARTESIAN_POINT('Ctrl Pts',(-30.5813585616553,-3.93606314266839,
-0.29610630575176));
#39390=CARTESIAN_POINT('Ctrl Pts',(-30.5665536012758,-3.90619407193774,
-0.588089999412536));
#39391=CARTESIAN_POINT('Ctrl Pts',(-30.5517486408963,-3.84168803968927,
-0.872209781087009));
#39392=CARTESIAN_POINT('Ctrl Pts',(-30.4855909236536,-3.55343520195466,
-2.14183264377887));
#39393=CARTESIAN_POINT('Ctrl Pts',(-30.4194332064109,-2.57353247570956,
-3.25442458891207));
#39394=CARTESIAN_POINT('Ctrl Pts',(-30.3532754891682,-1.3504901785784,-3.70074224637148));
#39395=CARTESIAN_POINT('Ctrl Pts',(-30.2871177719255,-0.127447881447261,
-4.14705990383089));
#39396=CARTESIAN_POINT('Ctrl Pts',(-30.2209600546827,1.33873398656992,-3.92710327361655));
#39397=CARTESIAN_POINT('Ctrl Pts',(-30.15480233744,2.37697075787629,-3.14154848963316));
#39398=CARTESIAN_POINT('Ctrl Pts',(-30.0886446201973,3.41520752918271,-2.35599370564973));
#39399=CARTESIAN_POINT('Ctrl Pts',(-30.0224869029546,4.02549920377824,-1.00484076789717));
#39400=CARTESIAN_POINT('Ctrl Pts',(-29.9563291857119,3.92850977668485,0.293475435099665));
#39401=CARTESIAN_POINT('Ctrl Pts',(-29.8901714684692,3.83152034959146,1.5917916380965));
#39402=CARTESIAN_POINT('Ctrl Pts',(-29.8240137512265,3.02724982080915,2.83727110633764));
#39403=CARTESIAN_POINT('Ctrl Pts',(-29.7578560339838,1.88382006678415,3.45984665158685));
#39404=CARTESIAN_POINT('Ctrl Pts',(-29.6916983167411,0.74039031275917,4.08242219683605));
#39405=CARTESIAN_POINT('Ctrl Pts',(-29.6255405994984,-0.74219866650845,
4.08209381909339));
#39406=CARTESIAN_POINT('Ctrl Pts',(-29.5593828822557,-1.88535252059195,
3.459011819814));
#39407=CARTESIAN_POINT('Ctrl Pts',(-29.493225165013,-3.02850637467544,2.83592982053462));
#39408=CARTESIAN_POINT('Ctrl Pts',(-29.4270674477702,-3.8322251035748,1.59009419971851));
#39409=CARTESIAN_POINT('Ctrl Pts',(-29.3609097305275,-3.92863939462808,
0.29173515984833));
#39410=CARTESIAN_POINT('Ctrl Pts',(-29.3559943276966,-3.93580280804277,
0.195269351079819));
#39411=CARTESIAN_POINT('Ctrl Pts',(-29.3510789248657,-3.93906173797095,
0.0985136009347571));
#39412=CARTESIAN_POINT('Ctrl Pts',(-29.3461635220348,-3.93853086460256,
0.00172150567391906));
#39413=CARTESIAN_POINT('Origin',(-27.25,0.,0.));
#39414=CARTESIAN_POINT('',(-27.912836477965,-3.92849944027351,0.00265245323384067));
#39415=CARTESIAN_POINT('',(-28.0961635220349,-3.92823136251108,0.00249701373361682));
#39416=CARTESIAN_POINT('',(-27.25,-3.933,-4.81653586104654E-16));
#39417=CARTESIAN_POINT('Ctrl Pts',(-27.912836477965,-3.92849944027351,0.00265245323384067));
#39418=CARTESIAN_POINT('Ctrl Pts',(-27.9367957831988,-3.93144429728796,
0.477549615694625));
#39419=CARTESIAN_POINT('Ctrl Pts',(-27.9607550884325,-3.85179092258685,
0.95149239765976));
#39420=CARTESIAN_POINT('Ctrl Pts',(-27.9847143936663,-3.68512069940966,
1.39255279517753));
#39421=CARTESIAN_POINT('Ctrl Pts',(-28.050872110909,-3.22490194973579,2.61043239482561));
#39422=CARTESIAN_POINT('Ctrl Pts',(-28.1170298281517,-2.10122138469273,
3.57759955359381));
#39423=CARTESIAN_POINT('Ctrl Pts',(-28.1831875453944,-0.82839773576013,
3.85137313798103));
#39424=CARTESIAN_POINT('Ctrl Pts',(-28.2493452626371,0.444425913172473,
4.12514672236825));
#39425=CARTESIAN_POINT('Ctrl Pts',(-28.3155029798798,1.86639264599462,3.70552673237448));
#39426=CARTESIAN_POINT('Ctrl Pts',(-28.3816606971225,2.78665546135827,2.78457702286299));
#39427=CARTESIAN_POINT('Ctrl Pts',(-28.4478184143653,3.70691827672194,1.86362731335147));
#39428=CARTESIAN_POINT('Ctrl Pts',(-28.513976131608,4.12547717462709,0.441347884322195));
#39429=CARTESIAN_POINT('Ctrl Pts',(-28.5801338488507,3.85075397163164,-0.83127113900189));
#39430=CARTESIAN_POINT('Ctrl Pts',(-28.6462915660934,3.5760307686362,-2.10389016232594));
#39431=CARTESIAN_POINT('Ctrl Pts',(-28.7124492833361,2.60802546474021,-3.22684877994481));
#39432=CARTESIAN_POINT('Ctrl Pts',(-28.7786070005788,1.38980282003078,-3.68615870222768));
#39433=CARTESIAN_POINT('Ctrl Pts',(-28.8447647178215,0.171580175321349,
-4.14546862451055));
#39434=CARTESIAN_POINT('Ctrl Pts',(-28.9109224350642,-1.29685981020152,
-3.94112985145742));
#39435=CARTESIAN_POINT('Ctrl Pts',(-28.9770801523069,-2.34339890818778,
-3.1666700828597));
#39436=CARTESIAN_POINT('Ctrl Pts',(-29.0389989275263,-3.32288281221589,
-2.44183249282753));
#39437=CARTESIAN_POINT('Ctrl Pts',(-29.1009177027456,-3.93279891142486,
-1.21759238663821));
#39438=CARTESIAN_POINT('Ctrl Pts',(-29.162836477965,-3.93875478927679,0.00150291653159836));
#39439=CARTESIAN_POINT('Ctrl Pts',(-29.3461635220348,-3.93853086460256,
0.00172150567391906));
#39440=CARTESIAN_POINT('Ctrl Pts',(-29.284921207623,-3.93191657176457,-1.20423701582998));
#39441=CARTESIAN_POINT('Ctrl Pts',(-29.2236788932112,-3.33699851326665,
-2.41583751049172));
#39442=CARTESIAN_POINT('Ctrl Pts',(-29.1624365787994,-2.3755788853513,-3.14260112899942));
#39443=CARTESIAN_POINT('Ctrl Pts',(-29.0962788615567,-1.33699423181405,
-3.9276959190527));
#39444=CARTESIAN_POINT('Ctrl Pts',(-29.030121144314,0.129284928467726,-4.14700304023501));
#39445=CARTESIAN_POINT('Ctrl Pts',(-28.9639634270713,1.35212939634983,-3.70014364478489));
#39446=CARTESIAN_POINT('Ctrl Pts',(-28.8978057098285,2.57497386423193,-3.25328424933478));
#39447=CARTESIAN_POINT('Ctrl Pts',(-28.8316479925859,3.55438363971437,-2.14025833725233));
#39448=CARTESIAN_POINT('Ctrl Pts',(-28.7654902753432,3.84207403318388,-0.870507909240087));
#39449=CARTESIAN_POINT('Ctrl Pts',(-28.6993325581004,4.1297644266534,0.399242518772191));
#39450=CARTESIAN_POINT('Ctrl Pts',(-28.6331748408577,3.72573543810985,1.82571746271425));
#39451=CARTESIAN_POINT('Ctrl Pts',(-28.567017123615,2.81491478040445,2.75600647233927));
#39452=CARTESIAN_POINT('Ctrl Pts',(-28.5008594063723,1.90409412269907,3.68629548196426));
#39453=CARTESIAN_POINT('Ctrl Pts',(-28.4347016891296,0.486481795831812,
4.12039855727229));
#39454=CARTESIAN_POINT('Ctrl Pts',(-28.3685439718869,-0.789068249736409,
3.85962280459805));
#39455=CARTESIAN_POINT('Ctrl Pts',(-28.3023862546442,-2.0646182953047,3.59884705192379));
#39456=CARTESIAN_POINT('Ctrl Pts',(-28.2362285374015,-3.19810605957393,
2.64319247126727));
#39457=CARTESIAN_POINT('Ctrl Pts',(-28.1700708201588,-3.67072396750674,
1.43007078527147));
#39458=CARTESIAN_POINT('Ctrl Pts',(-28.1454350541175,-3.84671710469501,
0.978329351597568));
#39459=CARTESIAN_POINT('Ctrl Pts',(-28.1207992880762,-3.93106982372138,
0.490885891314328));
#39460=CARTESIAN_POINT('Ctrl Pts',(-28.0961635220349,-3.92823136251108,
0.00249701373361682));
#39461=CARTESIAN_POINT('Origin',(-27.25,0.,0.));
#39462=CARTESIAN_POINT('',(-26.662836477965,-3.92914366735242,-0.00295733212259536));
#39463=CARTESIAN_POINT('',(-26.8461635220349,-3.92946204260484,-0.00307907422078526));
#39464=CARTESIAN_POINT('',(-27.25,-3.933,-4.81653586104654E-16));
#39465=CARTESIAN_POINT('Ctrl Pts',(-26.662836477965,-3.92914366735242,-0.00295733212259536));
#39466=CARTESIAN_POINT('Ctrl Pts',(-26.7065161464092,-3.92309441571187,
0.862460122396525));
#39467=CARTESIAN_POINT('Ctrl Pts',(-26.7501958148533,-3.64146415129019,
1.73145588387443));
#39468=CARTESIAN_POINT('Ctrl Pts',(-26.7938754832975,-3.11534036258412,
2.411218007943));
#39469=CARTESIAN_POINT('Ctrl Pts',(-26.8600332005402,-2.31846735306552,
3.44079336870641));
#39470=CARTESIAN_POINT('Ctrl Pts',(-26.9261909177829,-0.960714648945873,
4.03625782584134));
#39471=CARTESIAN_POINT('Ctrl Pts',(-26.9923486350256,0.336462088646539,
3.92506192555964));
#39472=CARTESIAN_POINT('Ctrl Pts',(-27.0585063522684,1.63363882623891,3.81386602527794));
#39473=CARTESIAN_POINT('Ctrl Pts',(-27.1246640695111,2.87023959730411,2.99600976757956));
#39474=CARTESIAN_POINT('Ctrl Pts',(-27.1908217867538,3.48026107339907,1.8458333395942));
#39475=CARTESIAN_POINT('Ctrl Pts',(-27.2569795039965,4.09028254949405,0.695656911608815));
#39476=CARTESIAN_POINT('Ctrl Pts',(-27.3231372212392,4.07372473061887,-0.786839686663616));
#39477=CARTESIAN_POINT('Ctrl Pts',(-27.3892949384819,3.43816627984279,-1.92310438841117));
#39478=CARTESIAN_POINT('Ctrl Pts',(-27.4554526557246,2.80260782906669,-3.05936909015876));
#39479=CARTESIAN_POINT('Ctrl Pts',(-27.5216103729673,1.54804874638969,-3.84940189538143));
#39480=CARTESIAN_POINT('Ctrl Pts',(-27.58776809021,0.248712041483546,-3.93159766214645));
#39481=CARTESIAN_POINT('Ctrl Pts',(-27.6539258074527,-1.05062466342256,
-4.01379342891147));
#39482=CARTESIAN_POINT('Ctrl Pts',(-27.7200835246955,-2.39473899055777,
-3.3881521572189));
#39483=CARTESIAN_POINT('Ctrl Pts',(-27.7862412419382,-3.16841768697301,
-2.34103550110863));
#39484=CARTESIAN_POINT('Ctrl Pts',(-27.8284396539471,-3.6619052762455,-1.67313669931251));
#39485=CARTESIAN_POINT('Ctrl Pts',(-27.8706380659561,-3.92331280032755,
-0.83376187213494));
#39486=CARTESIAN_POINT('Ctrl Pts',(-27.912836477965,-3.92849944027351,0.00265245323384067));
#39487=CARTESIAN_POINT('Ctrl Pts',(-28.0961635220349,-3.92823136251108,
0.00249701373361682));
#39488=CARTESIAN_POINT('Ctrl Pts',(-28.0546415708335,-3.92344732422855,
-0.820650076891716));
#39489=CARTESIAN_POINT('Ctrl Pts',(-28.013119619632,-3.67098044429315,-1.64648280202908));
#39490=CARTESIAN_POINT('Ctrl Pts',(-27.9715976684306,-3.19213273732399,
-2.30859383257857));
#39491=CARTESIAN_POINT('Ctrl Pts',(-27.9054399511879,-2.42917554761208,
-3.36354797309789));
#39492=CARTESIAN_POINT('Ctrl Pts',(-27.8392822339452,-1.09151311659189,
-4.00286746280153));
#39493=CARTESIAN_POINT('Ctrl Pts',(-27.7731245167025,0.208594393842709,
-3.93393000387307));
#39494=CARTESIAN_POINT('Ctrl Pts',(-27.7069667994598,1.50870190427727,-3.8649925449446));
#39495=CARTESIAN_POINT('Ctrl Pts',(-27.6408090822171,2.7712544941262,-3.08779813738407));
#39496=CARTESIAN_POINT('Ctrl Pts',(-27.5746513649744,3.4183704533748,-1.95807567269744));
#39497=CARTESIAN_POINT('Ctrl Pts',(-27.5084936477317,4.06548641262342,-0.828353208010779));
#39498=CARTESIAN_POINT('Ctrl Pts',(-27.4423359304889,4.09716574127161,0.653897313802084));
#39499=CARTESIAN_POINT('Ctrl Pts',(-27.3761782132462,3.49890852481402,1.81023645734449));
#39500=CARTESIAN_POINT('Ctrl Pts',(-27.3100204960035,2.90065130835643,2.9665756008869));
#39501=CARTESIAN_POINT('Ctrl Pts',(-27.2438627787608,1.6724575467931,3.79700336615891));
#39502=CARTESIAN_POINT('Ctrl Pts',(-27.1777050615181,0.376482604477266,
3.92142547360541));
#39503=CARTESIAN_POINT('Ctrl Pts',(-27.1115473442754,-0.919492337838605,
4.0458475810519));
#39504=CARTESIAN_POINT('Ctrl Pts',(-27.0453896270327,-2.28324846090694,
3.46426403067282));
#39505=CARTESIAN_POINT('Ctrl Pts',(-26.97923190979,-3.09058228458904,2.44287086001282));
#39506=CARTESIAN_POINT('Ctrl Pts',(-26.9348757805383,-3.6318676391175,1.75806719110156));
#39507=CARTESIAN_POINT('Ctrl Pts',(-26.8905196512866,-3.92303163210045,
0.875561558831162));
#39508=CARTESIAN_POINT('Ctrl Pts',(-26.8461635220349,-3.92946204260484,
-0.00307907422078526));
#39509=CARTESIAN_POINT('Origin',(-27.25,0.,0.));
#39510=CARTESIAN_POINT('',(-25.412836477965,-3.93914704469817,-0.000998409943392953));
#39511=CARTESIAN_POINT('',(-25.5961635220349,-3.93927687571695,-0.00075861444495069));
#39512=CARTESIAN_POINT('',(-27.25,-3.933,-4.81653586104654E-16));
#39513=CARTESIAN_POINT('Ctrl Pts',(-25.412836477965,-3.93914704469817,-0.000998409943392953));
#39514=CARTESIAN_POINT('Ctrl Pts',(-25.4762365096196,-3.93490039704559,
1.24692954761248));
#39515=CARTESIAN_POINT('Ctrl Pts',(-25.5396365412741,-3.29132887644148,
2.49862752120908));
#39516=CARTESIAN_POINT('Ctrl Pts',(-25.6030365729287,-2.2720868718378,3.21821986560842));
#39517=CARTESIAN_POINT('Ctrl Pts',(-25.6691942901714,-1.20851130913384,
3.96911202777905));
#39518=CARTESIAN_POINT('Ctrl Pts',(-25.7353520074142,0.26412626364417,4.14060227385076));
#39519=CARTESIAN_POINT('Ctrl Pts',(-25.8015097246569,1.47178634459257,3.6541979711621));
#39520=CARTESIAN_POINT('Ctrl Pts',(-25.8676674418996,2.67944642554097,3.16779366847344));
#39521=CARTESIAN_POINT('Ctrl Pts',(-25.9338251591423,3.62212901465975,2.02349481702441));
#39522=CARTESIAN_POINT('Ctrl Pts',(-25.999982876385,3.86835978685463,0.745057323982752));
#39523=CARTESIAN_POINT('Ctrl Pts',(-26.0661405936277,4.11459055904951,-0.533380169058908));
#39524=CARTESIAN_POINT('Ctrl Pts',(-26.1322983108704,3.66436951432049,-1.9459563036932));
#39525=CARTESIAN_POINT('Ctrl Pts',(-26.1984560281131,2.723766886339,-2.8461222400764));
#39526=CARTESIAN_POINT('Ctrl Pts',(-26.2646137453558,1.78316425835751,-3.7462881764596));
#39527=CARTESIAN_POINT('Ctrl Pts',(-26.3307714625985,0.352180047123545,
-4.13404391459171));
#39528=CARTESIAN_POINT('Ctrl Pts',(-26.3969291798412,-0.914211364797984,
-3.83191015513785));
#39529=CARTESIAN_POINT('Ctrl Pts',(-26.4630868970839,-2.18060277671955,
-3.52977639568397));
#39530=CARTESIAN_POINT('Ctrl Pts',(-26.5292446143267,-3.28240138932867,
-2.53775313864409));
#39531=CARTESIAN_POINT('Ctrl Pts',(-26.5954023315694,-3.71530403817446,
-1.30989837792818));
#39532=CARTESIAN_POINT('Ctrl Pts',(-26.6178803803679,-3.8623890234389,-0.892716824827767));
#39533=CARTESIAN_POINT('Ctrl Pts',(-26.6403584291665,-3.93225668030363,
-0.448310890578607));
#39534=CARTESIAN_POINT('Ctrl Pts',(-26.662836477965,-3.92914366735242,-0.00295733212259536));
#39535=CARTESIAN_POINT('Ctrl Pts',(-26.8461635220349,-3.92946204260484,
-0.00307907422078526));
#39536=CARTESIAN_POINT('Ctrl Pts',(-26.8243619340439,-3.93262266916976,
-0.434941849379828));
#39537=CARTESIAN_POINT('Ctrl Pts',(-26.8025603460529,-3.86699609002072,
-0.865870900831215));
#39538=CARTESIAN_POINT('Ctrl Pts',(-26.7807587580619,-3.72847238930294,
-1.27193181370741));
#39539=CARTESIAN_POINT('Ctrl Pts',(-26.7146010408191,-3.30811714603892,
-2.50413852582693));
#39540=CARTESIAN_POINT('Ctrl Pts',(-26.6484433235764,-2.216495135215,-3.5073491591251));
#39541=CARTESIAN_POINT('Ctrl Pts',(-26.5822856063337,-0.953251598840578,
-3.82238515665588));
#39542=CARTESIAN_POINT('Ctrl Pts',(-26.516127889091,0.309991937533875,-4.13742115418667));
#39543=CARTESIAN_POINT('Ctrl Pts',(-26.4499701718483,1.7448569994588,-3.76428251595003));
#39544=CARTESIAN_POINT('Ctrl Pts',(-26.3838124546056,2.69459290399842,-2.87375816279602));
#39545=CARTESIAN_POINT('Ctrl Pts',(-26.3176547373629,3.64432880853801,-1.98323380964204));
#39546=CARTESIAN_POINT('Ctrl Pts',(-26.2514970201202,4.10893555569232,-0.575323741570636));
#39547=CARTESIAN_POINT('Ctrl Pts',(-26.1853393028774,3.87575844601461,0.705558902333295));
#39548=CARTESIAN_POINT('Ctrl Pts',(-26.1191815856347,3.64258133633691,1.98644154623723));
#39549=CARTESIAN_POINT('Ctrl Pts',(-26.053023868392,2.71162036982735,3.14029676597366));
#39550=CARTESIAN_POINT('Ctrl Pts',(-25.9868661511493,1.50898477916967,3.63899461840075));
#39551=CARTESIAN_POINT('Ctrl Pts',(-25.9207084339066,0.306349188512026,
4.13769247082782));
#39552=CARTESIAN_POINT('Ctrl Pts',(-25.8545507166639,-1.16796102629378,
3.98123295594543));
#39553=CARTESIAN_POINT('Ctrl Pts',(-25.7883929994212,-2.23914077999871,
3.24122900515563));
#39554=CARTESIAN_POINT('Ctrl Pts',(-25.7243165069591,-3.27662278927113,
2.52450449362568));
#39555=CARTESIAN_POINT('Ctrl Pts',(-25.660240014497,-3.93593917010812,1.26037295231601));
#39556=CARTESIAN_POINT('Ctrl Pts',(-25.5961635220349,-3.93927687571695,
-0.00075861444495069));
#39557=CARTESIAN_POINT('Origin',(-27.25,0.,0.));
#39558=CARTESIAN_POINT('',(-24.162836477965,-3.93208044729297,0.00358197651929196));
#39559=CARTESIAN_POINT('',(-24.3461635220348,-3.93168694540681,0.00355335107693575));
#39560=CARTESIAN_POINT('',(-27.25,-3.933,-4.81653586104654E-16));
#39561=CARTESIAN_POINT('Ctrl Pts',(-24.162836477965,-3.93208044729297,0.00358197651929196));
#39562=CARTESIAN_POINT('Ctrl Pts',(-24.1797991555873,-3.93508766644803,
0.33902540008706));
#39563=CARTESIAN_POINT('Ctrl Pts',(-24.1967618332096,-3.89573838320665,
0.673773865534885));
#39564=CARTESIAN_POINT('Ctrl Pts',(-24.2137245108318,-3.81128013311853,
0.99672544036477));
#39565=CARTESIAN_POINT('Ctrl Pts',(-24.2798822280745,-3.48187665375216,
2.25629892554613));
#39566=CARTESIAN_POINT('Ctrl Pts',(-24.3460399453173,-2.46629786501127,
3.33642394104913));
#39567=CARTESIAN_POINT('Ctrl Pts',(-24.41219766256,-1.2293833401628,3.74271752333842));
#39568=CARTESIAN_POINT('Ctrl Pts',(-24.4783553798027,0.00753118468553859,
4.14901110562767));
#39569=CARTESIAN_POINT('Ctrl Pts',(-24.5445130970454,1.46578144564145,3.8814732547034));
#39570=CARTESIAN_POINT('Ctrl Pts',(-24.6106708142881,2.47791314321192,3.06255845842524));
#39571=CARTESIAN_POINT('Ctrl Pts',(-24.6768285315308,3.49004484078246,2.24364366214702));
#39572=CARTESIAN_POINT('Ctrl Pts',(-24.7429862487735,4.05605797496752,0.873351920514928));
#39573=CARTESIAN_POINT('Ctrl Pts',(-24.8091439660162,3.91688322817713,-0.421121874757202));
#39574=CARTESIAN_POINT('Ctrl Pts',(-24.8753016832589,3.77770848138675,-1.71559567002929));
#39575=CARTESIAN_POINT('Ctrl Pts',(-24.9414594005016,2.93334585362089,-2.93425151894138));
#39576=CARTESIAN_POINT('Ctrl Pts',(-25.0076171177443,1.77026773670627,-3.5192996458033));
#39577=CARTESIAN_POINT('Ctrl Pts',(-25.073774834987,0.607189619791642,-4.10434777266522));
#39578=CARTESIAN_POINT('Ctrl Pts',(-25.1399325522298,-0.874603986271784,
-4.05578817747699));
#39579=CARTESIAN_POINT('Ctrl Pts',(-25.2060902694725,-1.99688278054788,
-3.39584702501831));
#39580=CARTESIAN_POINT('Ctrl Pts',(-25.2722479867152,-3.11916157482398,
-2.73590587255962));
#39581=CARTESIAN_POINT('Ctrl Pts',(-25.3384057039579,-3.88192555731279,
-1.46458316283046));
#39582=CARTESIAN_POINT('Ctrl Pts',(-25.4045634212006,-3.93605077224223,
-0.163774768831114));
#39583=CARTESIAN_POINT('Ctrl Pts',(-25.4073211067887,-3.93830690095081,
-0.109552514639702));
#39584=CARTESIAN_POINT('Ctrl Pts',(-25.4100787923769,-3.93933175941713,
-0.0552790286398185));
#39585=CARTESIAN_POINT('Ctrl Pts',(-25.412836477965,-3.93914704469817,-0.000998409943392953));
#39586=CARTESIAN_POINT('Ctrl Pts',(-25.5961635220349,-3.93927687571695,
-0.00075861444495069));
#39587=CARTESIAN_POINT('Ctrl Pts',(-25.5940822972543,-3.93938528545282,
-0.0417205673778243));
#39588=CARTESIAN_POINT('Ctrl Pts',(-25.5920010724737,-3.93880165671922,
-0.082679355424592));
#39589=CARTESIAN_POINT('Ctrl Pts',(-25.5899198476931,-3.93751647003208,
-0.12361611845337));
#39590=CARTESIAN_POINT('Ctrl Pts',(-25.5237621304504,-3.89666311375636,
-1.42490890457529));
#39591=CARTESIAN_POINT('Ctrl Pts',(-25.4576044132076,-3.14690710860075,
-2.70394609012188));
#39592=CARTESIAN_POINT('Ctrl Pts',(-25.3914466959649,-2.03141854176537,
-3.37530081691799));
#39593=CARTESIAN_POINT('Ctrl Pts',(-25.3252889787222,-0.915929974929986,
-4.0466555437141));
#39594=CARTESIAN_POINT('Ctrl Pts',(-25.2591312614795,0.565291153585176,
-4.11032781175974));
#39595=CARTESIAN_POINT('Ctrl Pts',(-25.1929735442368,1.73427657098226,-3.53717424957513));
#39596=CARTESIAN_POINT('Ctrl Pts',(-25.1268158269941,2.90326198837934,-2.96402068739052));
#39597=CARTESIAN_POINT('Ctrl Pts',(-25.0606581097514,3.76001169465834,-1.75404129497565));
#39598=CARTESIAN_POINT('Ctrl Pts',(-24.9945003925087,3.91238362041176,-0.461054555610493));
#39599=CARTESIAN_POINT('Ctrl Pts',(-24.928342675266,4.06475554616517,0.831932183754663));
#39600=CARTESIAN_POINT('Ctrl Pts',(-24.8621849580232,3.512749691393,2.2079262700701));
#39601=CARTESIAN_POINT('Ctrl Pts',(-24.7960272407805,2.50902411553662,3.03712279701876));
#39602=CARTESIAN_POINT('Ctrl Pts',(-24.7298695235378,1.50529853968021,3.86631932396744));
#39603=CARTESIAN_POINT('Ctrl Pts',(-24.6637118062951,0.0498532427395583,
4.1487182915493));
#39604=CARTESIAN_POINT('Ctrl Pts',(-24.5975540890524,-1.19114133312601,
3.75506314474659));
#39605=CARTESIAN_POINT('Ctrl Pts',(-24.5313963718097,-2.43213590899152,
3.36140799794391));
#39606=CARTESIAN_POINT('Ctrl Pts',(-24.465238654567,-3.45867976378196,2.29169873675672));
#39607=CARTESIAN_POINT('Ctrl Pts',(-24.3990809373243,-3.80091451458247,
1.03555094000812));
#39608=CARTESIAN_POINT('Ctrl Pts',(-24.3814417988945,-3.89216201217545,
0.700633627280088));
#39609=CARTESIAN_POINT('Ctrl Pts',(-24.3638026604647,-3.93476363339442,
0.352462850730819));
#39610=CARTESIAN_POINT('Ctrl Pts',(-24.3461635220348,-3.93168694540681,
0.00355335107693575));
#39611=CARTESIAN_POINT('Origin',(-27.25,0.,0.));
#39612=CARTESIAN_POINT('',(-22.912836477965,-3.92686657274101,-0.00115429526849065));
#39613=CARTESIAN_POINT('',(-23.0961635220349,-3.92699480624753,-0.00136118811112632));
#39614=CARTESIAN_POINT('',(-27.25,-3.933,-4.81653586104654E-16));
#39615=CARTESIAN_POINT('Ctrl Pts',(-22.912836477965,-3.92686657274101,-0.00115429526849065));
#39616=CARTESIAN_POINT('Ctrl Pts',(-22.9495195187977,-3.92495252483706,
0.726697173104542));
#39617=CARTESIAN_POINT('Ctrl Pts',(-22.9862025596304,-3.73121721702526,
1.45549568713423));
#39618=CARTESIAN_POINT('Ctrl Pts',(-23.022885600463,-3.35194483101353,2.06973034630505));
#39619=CARTESIAN_POINT('Ctrl Pts',(-23.0890433177058,-2.66792860165602,
3.17750009438718));
#39620=CARTESIAN_POINT('Ctrl Pts',(-23.1552010349485,-1.38043487888614,
3.91263969955316));
#39621=CARTESIAN_POINT('Ctrl Pts',(-23.2213587521912,-0.0787611542536249,
3.93866913273443));
#39622=CARTESIAN_POINT('Ctrl Pts',(-23.2875164694339,1.22291257037878,3.9646985659157));
#39623=CARTESIAN_POINT('Ctrl Pts',(-23.3536741866766,2.53876629687382,3.28161782711241));
#39624=CARTESIAN_POINT('Ctrl Pts',(-23.4198319039193,3.26652190413782,2.20207913262947));
#39625=CARTESIAN_POINT('Ctrl Pts',(-23.485989621162,3.99427751140188,1.12254043814643));
#39626=CARTESIAN_POINT('Ctrl Pts',(-23.5521473384047,4.13393499943478,-0.353456212016352));
#39627=CARTESIAN_POINT('Ctrl Pts',(-23.6183050556474,3.62157187609663,-1.55033383593352));
#39628=CARTESIAN_POINT('Ctrl Pts',(-23.6844627728902,3.10920875275847,-2.74721145985068));
#39629=CARTESIAN_POINT('Ctrl Pts',(-23.7506204901329,1.94482501804926,-3.66497005752223));
#39630=CARTESIAN_POINT('Ctrl Pts',(-23.8167782073756,0.661369611393123,
-3.88354323958161));
#39631=CARTESIAN_POINT('Ctrl Pts',(-23.8829359246183,-0.622085795262939,
-4.10211642164099));
#39632=CARTESIAN_POINT('Ctrl Pts',(-23.949093641861,-2.02461287386591,-3.62150418808829));
#39633=CARTESIAN_POINT('Ctrl Pts',(-24.0152513591037,-2.90426232817139,
-2.66168709388216));
#39634=CARTESIAN_POINT('Ctrl Pts',(-24.0644463987241,-3.55837180413624,
-1.94796476569749));
#39635=CARTESIAN_POINT('Ctrl Pts',(-24.1136414383446,-3.92335893122251,
-0.969268706628277));
#39636=CARTESIAN_POINT('Ctrl Pts',(-24.162836477965,-3.93208044729297,0.00358197651929196));
#39637=CARTESIAN_POINT('Ctrl Pts',(-24.3461635220348,-3.93168694540681,
0.00355335107693575));
#39638=CARTESIAN_POINT('Ctrl Pts',(-24.2976449432219,-3.92322414382476,
-0.95616433155768));
#39639=CARTESIAN_POINT('Ctrl Pts',(-24.249126364409,-3.56916317924449,-1.9214711297343));
#39640=CARTESIAN_POINT('Ctrl Pts',(-24.2006077855961,-2.93126197236318,
-2.63192327887667));
#39641=CARTESIAN_POINT('Ctrl Pts',(-24.1344500683534,-2.06144903253297,
-3.60066336870251));
#39642=CARTESIAN_POINT('Ctrl Pts',(-24.0682923511107,-0.663897506062122,
-4.0955572160442));
#39643=CARTESIAN_POINT('Ctrl Pts',(-24.002134633868,0.621720665900904,-3.8900874424757));
#39644=CARTESIAN_POINT('Ctrl Pts',(-23.9359769166253,1.90733883786397,-3.68461766890719));
#39645=CARTESIAN_POINT('Ctrl Pts',(-23.8698191993826,3.0810236553192,-2.77878427442845));
#39646=CARTESIAN_POINT('Ctrl Pts',(-23.8036614821399,3.60556898936345,-1.58719537532593));
#39647=CARTESIAN_POINT('Ctrl Pts',(-23.7375037648972,4.1301143234077,-0.39560647622341));
#39648=CARTESIAN_POINT('Ctrl Pts',(-23.6713460476545,4.00552017404096,1.08173792750288));
#39649=CARTESIAN_POINT('Ctrl Pts',(-23.6051883304118,3.28881440740741,2.16864397496335));
#39650=CARTESIAN_POINT('Ctrl Pts',(-23.5390306131691,2.57210864077385,3.25555002242383));
#39651=CARTESIAN_POINT('Ctrl Pts',(-23.4728728959263,1.26329125687349,3.95201771361849));
#39652=CARTESIAN_POINT('Ctrl Pts',(-23.4067151786836,-0.0385802206812267,
3.93926750336755));
#39653=CARTESIAN_POINT('Ctrl Pts',(-23.3405574614409,-1.34045169823594,
3.9265172931166));
#39654=CARTESIAN_POINT('Ctrl Pts',(-23.2743997441982,-2.63537726944501,
3.20454918142005));
#39655=CARTESIAN_POINT('Ctrl Pts',(-23.2082420269555,-3.33065781868451,
2.1038144859638));
#39656=CARTESIAN_POINT('Ctrl Pts',(-23.1708825253153,-3.72328525358264,
1.48222563171916));
#39657=CARTESIAN_POINT('Ctrl Pts',(-23.1335230236751,-3.92469178838456,
0.73985183902043));
#39658=CARTESIAN_POINT('Ctrl Pts',(-23.0961635220349,-3.92699480624753,
-0.00136118811112632));
#39659=CARTESIAN_POINT('Origin',(-27.25,0.,0.));
#39660=CARTESIAN_POINT('',(-21.662836477965,-3.93631159263206,-0.00298228534019229));
#39661=CARTESIAN_POINT('',(-21.8461635220349,-3.93667291872696,-0.00284305540341681));
#39662=CARTESIAN_POINT('',(-27.25,-3.933,-4.81653586104654E-16));
#39663=CARTESIAN_POINT('Ctrl Pts',(-21.662836477965,-3.93631159263206,-0.00298228534019229));
#39664=CARTESIAN_POINT('Ctrl Pts',(-21.7192398820081,-3.92694175997278,
1.1093344945322));
#39665=CARTESIAN_POINT('Ctrl Pts',(-21.7756432860512,-3.43266800109764,
2.22893605216819));
#39666=CARTESIAN_POINT('Ctrl Pts',(-21.8320466900943,-2.59836658334952,
2.96104862423887));
#39667=CARTESIAN_POINT('Ctrl Pts',(-21.898204407337,-1.61978243178991,3.81977155691665));
#39668=CARTESIAN_POINT('Ctrl Pts',(-21.9643621245797,-0.173393518595285,
4.14539317327969));
#39669=CARTESIAN_POINT('Ctrl Pts',(-22.0305198418224,1.07877490261441,3.78887352204631));
#39670=CARTESIAN_POINT('Ctrl Pts',(-22.0966775590651,2.33094332382414,3.43235387081292));
#39671=CARTESIAN_POINT('Ctrl Pts',(-22.1628352763078,3.38889125304889,2.39369295198309));
#39672=CARTESIAN_POINT('Ctrl Pts',(-22.2289929935505,3.76838637920517,1.14829523799207));
#39673=CARTESIAN_POINT('Ctrl Pts',(-22.2951507107932,4.14788150536145,-0.0971024759989268));
#39674=CARTESIAN_POINT('Ctrl Pts',(-22.361308428036,3.84892382844929,-1.54923698515106));
#39675=CARTESIAN_POINT('Ctrl Pts',(-22.4274661452787,3.00834897412506,-2.5434532247429));
#39676=CARTESIAN_POINT('Ctrl Pts',(-22.4936238625214,2.16777411980086,-3.53766946433471));
#39677=CARTESIAN_POINT('Ctrl Pts',(-22.5597815797641,0.785582088064504,
-4.07396743436626));
#39678=CARTESIAN_POINT('Ctrl Pts',(-22.6259392970068,-0.505585359235217,
-3.90687871594465));
#39679=CARTESIAN_POINT('Ctrl Pts',(-22.6920970142495,-1.79675280653497,
-3.73978999752304));
#39680=CARTESIAN_POINT('Ctrl Pts',(-22.7582547314922,-2.99689566939817,
-2.86931459064829));
#39681=CARTESIAN_POINT('Ctrl Pts',(-22.8244124487349,-3.55669773285718,
-1.69387694171179));
#39682=CARTESIAN_POINT('Ctrl Pts',(-22.853887125145,-3.80610151161202,-1.17019435732824));
#39683=CARTESIAN_POINT('Ctrl Pts',(-22.883361801555,-3.92840450256694,-0.585980035389735));
#39684=CARTESIAN_POINT('Ctrl Pts',(-22.912836477965,-3.92686657274101,-0.00115429526849065));
#39685=CARTESIAN_POINT('Ctrl Pts',(-23.0961635220349,-3.92699480624753,
-0.00136118811112632));
#39686=CARTESIAN_POINT('Ctrl Pts',(-23.0673653064324,-3.92877006560706,
-0.572718182331229));
#39687=CARTESIAN_POINT('Ctrl Pts',(-23.0385670908299,-3.81223900635808,
-1.14338545542971));
#39688=CARTESIAN_POINT('Ctrl Pts',(-23.0097688752274,-3.57379115692316,
-1.65750826942529));
#39689=CARTESIAN_POINT('Ctrl Pts',(-22.9436111579847,-3.02600841865232,
-2.83859505014238));
#39690=CARTESIAN_POINT('Ctrl Pts',(-22.877453440742,-1.83480741484064,-3.72126733236049));
#39691=CARTESIAN_POINT('Ctrl Pts',(-22.8112957234993,-0.545411590902302,
-3.90151804981405));
#39692=CARTESIAN_POINT('Ctrl Pts',(-22.7451380062565,0.743984233035964,
-4.0817687672676));
#39693=CARTESIAN_POINT('Ctrl Pts',(-22.6789802890138,2.13157487710084,-3.55959791995668));
#39694=CARTESIAN_POINT('Ctrl Pts',(-22.6128225717711,2.98224758587941,-2.57400781526239));
#39695=CARTESIAN_POINT('Ctrl Pts',(-22.5466648545284,3.83292029465795,-1.58841771056812));
#39696=CARTESIAN_POINT('Ctrl Pts',(-22.4805071372857,4.14667506815019,-0.139408348490439));
#39697=CARTESIAN_POINT('Ctrl Pts',(-22.414349420043,3.77990351610863,1.1097956142574));
#39698=CARTESIAN_POINT('Ctrl Pts',(-22.3481917028003,3.41313196406706,2.35899957700527));
#39699=CARTESIAN_POINT('Ctrl Pts',(-22.2820339855575,2.36583408649171,3.40839814042334));
#39700=CARTESIAN_POINT('Ctrl Pts',(-22.2158762683148,1.11736756975067,3.77767211528275));
#39701=CARTESIAN_POINT('Ctrl Pts',(-22.1497185510721,-0.131098946990363,
4.14694609014217));
#39702=CARTESIAN_POINT('Ctrl Pts',(-22.0835608338294,-1.58073410289704,
3.8360954764429));
#39703=CARTESIAN_POINT('Ctrl Pts',(-22.0174031165867,-2.56802680977533,
2.9873994042964));
#39704=CARTESIAN_POINT('Ctrl Pts',(-21.9603232517361,-3.4198478311971,2.25515743591571));
#39705=CARTESIAN_POINT('Ctrl Pts',(-21.9032433868855,-3.92750233438827,
1.12254470519444));
#39706=CARTESIAN_POINT('Ctrl Pts',(-21.8461635220349,-3.93667291872696,
-0.00284305540341681));
#39707=CARTESIAN_POINT('Origin',(-27.25,0.,0.));
#39708=CARTESIAN_POINT('',(-20.412836477965,-3.93619598941234,0.00302311619237688));
#39709=CARTESIAN_POINT('',(-20.5961635220349,-3.9358195614,0.00314458056749582));
#39710=CARTESIAN_POINT('',(-27.25,-3.933,-4.81653586104654E-16));
#39711=CARTESIAN_POINT('Ctrl Pts',(-20.412836477965,-3.93619598941234,0.00302311619237688));
#39712=CARTESIAN_POINT('Ctrl Pts',(-20.4228025279758,-3.93786691095472,
0.199575999993651));
#39713=CARTESIAN_POINT('Ctrl Pts',(-20.4327685779866,-3.92441667643614,
0.395899437378701));
#39714=CARTESIAN_POINT('Ctrl Pts',(-20.4427346279974,-3.89505305236271,
0.589813170295716));
#39715=CARTESIAN_POINT('Ctrl Pts',(-20.5088923452401,-3.7001282489982,1.87707240519113));
#39716=CARTESIAN_POINT('Ctrl Pts',(-20.5750500624828,-2.8039458261767,3.05814284774776));
#39717=CARTESIAN_POINT('Ctrl Pts',(-20.6412077797255,-1.61669656339455,
3.59243790182692));
#39718=CARTESIAN_POINT('Ctrl Pts',(-20.7073654969682,-0.429447300612364,
4.12673295590609));
#39719=CARTESIAN_POINT('Ctrl Pts',(-20.7735232142109,1.04886880213053,4.01425262150776));
#39720=CARTESIAN_POINT('Ctrl Pts',(-20.8396809314536,2.14161312853879,3.30648016238487));
#39721=CARTESIAN_POINT('Ctrl Pts',(-20.9058386486963,3.23435745494705,2.59870770326197));
#39722=CARTESIAN_POINT('Ctrl Pts',(-20.971996365939,3.94153000502067,1.29564311941459));
#39723=CARTESIAN_POINT('Ctrl Pts',(-21.0381540831818,3.93945152310121,-0.00628917402589305));
#39724=CARTESIAN_POINT('Ctrl Pts',(-21.1043118004245,3.93737304118174,-1.30822146746638));
#39725=CARTESIAN_POINT('Ctrl Pts',(-21.1704695176672,3.22604352726911,-2.60902147049994));
#39726=CARTESIAN_POINT('Ctrl Pts',(-21.2366272349099,2.13104491687146,-3.3133012870626));
#39727=CARTESIAN_POINT('Ctrl Pts',(-21.3027849521526,1.03604630647378,-4.01758110362527));
#39728=CARTESIAN_POINT('Ctrl Pts',(-21.3689426693953,-0.44262140040899,
-4.125340733717));
#39729=CARTESIAN_POINT('Ctrl Pts',(-21.435100386638,-1.62815865509478,-3.58725762253205));
#39730=CARTESIAN_POINT('Ctrl Pts',(-21.5012581038807,-2.81369590978054,
-3.04917451134711));
#39731=CARTESIAN_POINT('Ctrl Pts',(-21.5674158211234,-3.70610271226938,
-1.8652486588855));
#39732=CARTESIAN_POINT('Ctrl Pts',(-21.6335735383661,-3.89691641855152,
-0.57737360815846));
#39733=CARTESIAN_POINT('Ctrl Pts',(-21.6433278515658,-3.92505004727135,
-0.387488933620916));
#39734=CARTESIAN_POINT('Ctrl Pts',(-21.6530821647654,-3.93793199629274,
-0.195344544890875));
#39735=CARTESIAN_POINT('Ctrl Pts',(-21.662836477965,-3.93631159263206,-0.00298228534019229));
#39736=CARTESIAN_POINT('Ctrl Pts',(-21.8461635220349,-3.93667291872696,
-0.00284305540341681));
#39737=CARTESIAN_POINT('Ctrl Pts',(-21.8370856696428,-3.93813138768434,
-0.181822175296321));
#39738=CARTESIAN_POINT('Ctrl Pts',(-21.8280078172507,-3.92698170238435,
-0.360618554012682));
#39739=CARTESIAN_POINT('Ctrl Pts',(-21.8189299648586,-3.90260311466682,
-0.537592620771706));
#39740=CARTESIAN_POINT('Ctrl Pts',(-21.7527722476159,-3.72493645483012,
-1.82734704309961));
#39741=CARTESIAN_POINT('Ctrl Pts',(-21.6866145303732,-2.84465287730681,
-3.02031435716174));
#39742=CARTESIAN_POINT('Ctrl Pts',(-21.6204568131305,-1.66466611667486,
-3.57046266140818));
#39743=CARTESIAN_POINT('Ctrl Pts',(-21.5542990958878,-0.48467935604291,
-4.12061096565462));
#39744=CARTESIAN_POINT('Ctrl Pts',(-21.4881413786451,0.995010587697721,
-4.02794026008539));
#39745=CARTESIAN_POINT('Ctrl Pts',(-21.4219836614023,2.09713627883344,-3.33486676263326));
#39746=CARTESIAN_POINT('Ctrl Pts',(-21.3558259441596,3.19926196996916,-2.64179326518112));
#39747=CARTESIAN_POINT('Ctrl Pts',(-21.2896682269169,3.9238234085,-1.34831697584607));
#39748=CARTESIAN_POINT('Ctrl Pts',(-21.2235105096742,3.93918228765327,-0.046473660864169));
#39749=CARTESIAN_POINT('Ctrl Pts',(-21.1573527924315,3.95454116680654,1.25536965411777));
#39750=CARTESIAN_POINT('Ctrl Pts',(-21.0911950751888,3.26069748658226,2.56557999474652));
#39751=CARTESIAN_POINT('Ctrl Pts',(-21.0250373579461,2.17522975866749,3.2844622685491));
#39752=CARTESIAN_POINT('Ctrl Pts',(-20.9588796407034,1.08976203075273,4.00334454235169));
#39753=CARTESIAN_POINT('Ctrl Pts',(-20.8927219234607,-0.387329744852509,
4.13089874932803));
#39754=CARTESIAN_POINT('Ctrl Pts',(-20.8265642062179,-1.57996733742856,
3.60874217826299));
#39755=CARTESIAN_POINT('Ctrl Pts',(-20.7604064889752,-2.77260493000459,
3.08658560719796));
#39756=CARTESIAN_POINT('Ctrl Pts',(-20.6942487717325,-3.68078833955148,
1.91471825809157));
#39757=CARTESIAN_POINT('Ctrl Pts',(-20.6280910544898,-3.88883382668629,
0.62951438818813));
#39758=CARTESIAN_POINT('Ctrl Pts',(-20.6174485436715,-3.92230122005796,
0.422769103446732));
#39759=CARTESIAN_POINT('Ctrl Pts',(-20.6068060328532,-3.93765059158261,
0.213090920066174));
#39760=CARTESIAN_POINT('Ctrl Pts',(-20.5961635220349,-3.9358195614,0.00314458056749582));
#39761=CARTESIAN_POINT('Origin',(-27.25,0.,0.));
#39762=CARTESIAN_POINT('',(-19.162836477965,-3.92683079790197,0.00108863462069703));
#39763=CARTESIAN_POINT('',(-19.3461635220349,-3.9267306052256,0.000876370530420753));
#39764=CARTESIAN_POINT('',(-27.25,-3.933,-4.81653586104654E-16));
#39765=CARTESIAN_POINT('Ctrl Pts',(-19.162836477965,-3.92683079790197,0.00108863462069703));
#39766=CARTESIAN_POINT('Ctrl Pts',(-19.1925228911862,-3.92829091087402,
0.590128976753198));
#39767=CARTESIAN_POINT('Ctrl Pts',(-19.2222093044074,-3.80414942562565,
1.17858470241226));
#39768=CARTESIAN_POINT('Ctrl Pts',(-19.2518957176286,-3.55127120570492,
1.70522452483698));
#39769=CARTESIAN_POINT('Ctrl Pts',(-19.3180534348713,-2.98771892858378,
2.87886878428782));
#39770=CARTESIAN_POINT('Ctrl Pts',(-19.384211152114,-1.78480283323472,3.74550780533721));
#39771=CARTESIAN_POINT('Ctrl Pts',(-19.4503688693567,-0.493108468151834,
3.90847308999452));
#39772=CARTESIAN_POINT('Ctrl Pts',(-19.5165265865994,0.798585896931094,
4.07143837465183));
#39773=CARTESIAN_POINT('Ctrl Pts',(-19.5826843038421,2.17905853174786,3.53072992291702));
#39774=CARTESIAN_POINT('Ctrl Pts',(-19.6488420210848,3.01645465793078,2.53383487094602));
#39775=CARTESIAN_POINT('Ctrl Pts',(-19.7149997383276,3.85385078411367,1.53693981897505));
#39776=CARTESIAN_POINT('Ctrl Pts',(-19.7811574555703,4.14817040166277,0.0838581667679125));
#39777=CARTESIAN_POINT('Ctrl Pts',(-19.847315172813,3.76470076653265,-1.16032150503335));
#39778=CARTESIAN_POINT('Ctrl Pts',(-19.9134728900557,3.38123113140253,-2.40450117683462));
#39779=CARTESIAN_POINT('Ctrl Pts',(-19.9796306072984,2.31997224359321,-3.43977886823002));
#39780=CARTESIAN_POINT('Ctrl Pts',(-20.0457883245411,1.06667186980089,-3.79229864050154));
#39781=CARTESIAN_POINT('Ctrl Pts',(-20.1119460417838,-0.186628503991429,
-4.14481841277306));
#39782=CARTESIAN_POINT('Ctrl Pts',(-20.1781037590265,-1.63197036376675,
-3.81458026592071));
#39783=CARTESIAN_POINT('Ctrl Pts',(-20.2442614762692,-2.60780770170069,
-2.95273717887741));
#39784=CARTESIAN_POINT('Ctrl Pts',(-20.3004531435012,-3.43664414363103,
-2.2207228051708));
#39785=CARTESIAN_POINT('Ctrl Pts',(-20.3566448107331,-3.9267748178169,-1.10520273337645));
#39786=CARTESIAN_POINT('Ctrl Pts',(-20.412836477965,-3.93619598941234,0.00302311619237688));
#39787=CARTESIAN_POINT('Ctrl Pts',(-20.5961635220349,-3.9358195614,0.00314458056749582));
#39788=CARTESIAN_POINT('Ctrl Pts',(-20.5406483156105,-3.92626824213971,
-1.09201187022606));
#39789=CARTESIAN_POINT('Ctrl Pts',(-20.4851331091861,-3.44923046847552,
-2.19446496955116));
#39790=CARTESIAN_POINT('Ctrl Pts',(-20.4296179027617,-2.63779166770679,
-2.9259822306863));
#39791=CARTESIAN_POINT('Ctrl Pts',(-20.363460185519,-1.67079645686973,-3.79773458895681));
#39792=CARTESIAN_POINT('Ctrl Pts',(-20.2973024682763,-0.228898470472945,
-4.14269891479728));
#39793=CARTESIAN_POINT('Ctrl Pts',(-20.2311447510336,1.02793257557226,-3.80298192430529));
#39794=CARTESIAN_POINT('Ctrl Pts',(-20.1649870337908,2.28476362161743,-3.46326493381331));
#39795=CARTESIAN_POINT('Ctrl Pts',(-20.0988293165481,3.35652772731096,-2.43886662698886));
#39796=CARTESIAN_POINT('Ctrl Pts',(-20.0326715993054,3.75266879296217,-1.19866335008759));
#39797=CARTESIAN_POINT('Ctrl Pts',(-19.9665138820627,4.14880985861339,0.0415399268137066));
#39798=CARTESIAN_POINT('Ctrl Pts',(-19.90035616482,3.86932788422227,1.49754817379188));
#39799=CARTESIAN_POINT('Ctrl Pts',(-19.8341984475773,3.04214429070861,2.50293328137695));
#39800=CARTESIAN_POINT('Ctrl Pts',(-19.7680407303346,2.214960697195,3.50831838896196));
#39801=CARTESIAN_POINT('Ctrl Pts',(-19.7018830130919,0.840075484558995,
4.06308035715393));
#39802=CARTESIAN_POINT('Ctrl Pts',(-19.6357252958492,-0.453213982368851,
3.9132996285361));
#39803=CARTESIAN_POINT('Ctrl Pts',(-19.5695675786065,-1.74650344929677,
3.76351889991825));
#39804=CARTESIAN_POINT('Ctrl Pts',(-19.5034098613638,-2.9581971705165,2.90919547449042));
#39805=CARTESIAN_POINT('Ctrl Pts',(-19.437252144121,-3.53369199898883,1.74136089102682));
#39806=CARTESIAN_POINT('Ctrl Pts',(-19.4068892700923,-3.79781352115349,
1.2053869212177));
#39807=CARTESIAN_POINT('Ctrl Pts',(-19.3765263960636,-3.92793108062113,
0.603377411256794));
#39808=CARTESIAN_POINT('Ctrl Pts',(-19.3461635220349,-3.9267306052256,0.000876370530420753));
#39809=CARTESIAN_POINT('Origin',(-27.25,0.,0.));
#39810=CARTESIAN_POINT('',(-17.912836477965,-3.93220475577819,-0.00358799939168875));
#39811=CARTESIAN_POINT('',(-18.0961635220349,-3.93260484470905,-0.00359775545859465));
#39812=CARTESIAN_POINT('',(-27.25,-3.933,-4.81653586104654E-16));
#39813=CARTESIAN_POINT('Ctrl Pts',(-17.912836477965,-3.93220475577819,-0.00358799939168875));
#39814=CARTESIAN_POINT('Ctrl Pts',(-17.9622432543966,-3.92340751667497,
0.973371178801284));
#39815=CARTESIAN_POINT('Ctrl Pts',(-18.0116500308282,-3.55495908794336,
1.95625352284316));
#39816=CARTESIAN_POINT('Ctrl Pts',(-18.0610568072598,-2.89574899554892,
2.67094657590745));
#39817=CARTESIAN_POINT('Ctrl Pts',(-18.1272145245025,-2.01303941508155,
3.62795013564035));
#39818=CARTESIAN_POINT('Ctrl Pts',(-18.1933722417452,-0.608984933822139,
4.10408177595699));
#39819=CARTESIAN_POINT('Ctrl Pts',(-18.2595299589879,0.673766046010135,
3.88141174984286));
#39820=CARTESIAN_POINT('Ctrl Pts',(-18.3256876762306,1.95651702584241,3.65874172372872));
#39821=CARTESIAN_POINT('Ctrl Pts',(-18.3918453934734,3.11796450424755,2.7372700311838));
#39822=CARTESIAN_POINT('Ctrl Pts',(-18.4580031107161,3.62650349280015,1.53876257859445));
#39823=CARTESIAN_POINT('Ctrl Pts',(-18.5241608279588,4.13504248135275,0.340255126005093));
#39824=CARTESIAN_POINT('Ctrl Pts',(-18.5903185452015,3.99067298005282,-1.1352880866287));
#39825=CARTESIAN_POINT('Ctrl Pts',(-18.6564762624442,3.2594742120202,-2.21249761982914));
#39826=CARTESIAN_POINT('Ctrl Pts',(-18.7226339796869,2.52827544398759,-3.28970715302959));
#39827=CARTESIAN_POINT('Ctrl Pts',(-18.7887916969296,1.2102474092223,-3.96858300679668));
#39828=CARTESIAN_POINT('Ctrl Pts',(-18.8549494141723,-0.0913365706719286,
-3.93839757863934));
#39829=CARTESIAN_POINT('Ctrl Pts',(-18.921107131415,-1.39292055056615,-3.908212150482));
#39830=CARTESIAN_POINT('Ctrl Pts',(-18.9872648486577,-2.67806047558931,
-3.16896544040023));
#39831=CARTESIAN_POINT('Ctrl Pts',(-19.0534225659004,-3.35853620865428,
-2.05901733643319));
#39832=CARTESIAN_POINT('Ctrl Pts',(-19.089893869922,-3.73366761243046,-1.44712719821412));
#39833=CARTESIAN_POINT('Ctrl Pts',(-19.1263651739435,-3.92503697310701,
-0.722578089237031));
#39834=CARTESIAN_POINT('Ctrl Pts',(-19.162836477965,-3.92683079790197,0.00108863462069703));
#39835=CARTESIAN_POINT('Ctrl Pts',(-19.3461635220349,-3.9267306052256,0.000876370530420753));
#39836=CARTESIAN_POINT('Ctrl Pts',(-19.3103686788209,-3.92531536276454,
-0.709413118819952));
#39837=CARTESIAN_POINT('Ctrl Pts',(-19.2745738356069,-3.74139311099748,
-1.42038574213652));
#39838=CARTESIAN_POINT('Ctrl Pts',(-19.2387789923929,-3.37936460400123,
-2.0246510241864));
#39839=CARTESIAN_POINT('Ctrl Pts',(-19.1726212751502,-2.7102464448163,-3.1414826144367));
#39840=CARTESIAN_POINT('Ctrl Pts',(-19.1064635579075,-1.43271419072146,
-3.89380005343788));
#39841=CARTESIAN_POINT('Ctrl Pts',(-19.0403058406648,-0.131505879190206,
-3.9372608626117));
#39842=CARTESIAN_POINT('Ctrl Pts',(-18.9741481234221,1.16970243234101,-3.98072167178552));
#39843=CARTESIAN_POINT('Ctrl Pts',(-18.9079904061794,2.4945868013086,-3.31532585113203));
#39844=CARTESIAN_POINT('Ctrl Pts',(-18.8418326889366,3.23673570009262,-2.24563107038117));
#39845=CARTESIAN_POINT('Ctrl Pts',(-18.7756749716939,3.97888459887663,-1.17593628963034));
#39846=CARTESIAN_POINT('Ctrl Pts',(-18.7095172544512,4.13829802747708,0.2980574512179));
#39847=CARTESIAN_POINT('Ctrl Pts',(-18.6433595372085,3.64201102153556,1.50168991989987));
#39848=CARTESIAN_POINT('Ctrl Pts',(-18.5772018199658,3.145724015594,2.70532238858192));
#39849=CARTESIAN_POINT('Ctrl Pts',(-18.5110441027231,1.99373657511054,3.63859358509767));
#39850=CARTESIAN_POINT('Ctrl Pts',(-18.4448863854804,0.71332374381352,3.8743368636487));
#39851=CARTESIAN_POINT('Ctrl Pts',(-18.3787286682377,-0.567089087483427,
4.11008014219972));
#39852=CARTESIAN_POINT('Ctrl Pts',(-18.312570950995,-1.97592730959393,3.64829550278594));
#39853=CARTESIAN_POINT('Ctrl Pts',(-18.2464132337523,-2.86835295895642,
2.70034594068266));
#39854=CARTESIAN_POINT('Ctrl Pts',(-18.1963299965131,-3.54394406726701,
1.98272168174144));
#39855=CARTESIAN_POINT('Ctrl Pts',(-18.146246759274,-3.92358365927177,0.986480569459381));
#39856=CARTESIAN_POINT('Ctrl Pts',(-18.0961635220349,-3.93260484470905,
-0.00359775545859465));
#39857=CARTESIAN_POINT('Origin',(-27.25,0.,0.));
#39858=CARTESIAN_POINT('',(-16.662836477965,-3.93909976961691,0.00107240331368951));
#39859=CARTESIAN_POINT('',(-16.8461635220349,-3.93892856332975,0.00130481274881613));
#39860=CARTESIAN_POINT('',(-27.25,-3.933,-4.81653586104654E-16));
#39861=CARTESIAN_POINT('Ctrl Pts',(-16.662836477965,-3.93909976961691,0.00107240331368951));
#39862=CARTESIAN_POINT('Ctrl Pts',(-16.6658059003643,-3.9393119090298,0.0595225963558853));
#39863=CARTESIAN_POINT('Ctrl Pts',(-16.6687753227636,-3.93812355350836,
0.117963973516891));
#39864=CARTESIAN_POINT('Ctrl Pts',(-16.6717447451629,-3.93550779063421,
0.176341391714401));
#39865=CARTESIAN_POINT('Ctrl Pts',(-16.7379024624056,-3.87722948686605,
1.47697033807084));
#39866=CARTESIAN_POINT('Ctrl Pts',(-16.8040601796483,-3.11041017286938,
2.74585113031923));
#39867=CARTESIAN_POINT('Ctrl Pts',(-16.870217896891,-1.98602996623102,3.4022055831191));
#39868=CARTESIAN_POINT('Ctrl Pts',(-16.9363756141337,-0.861649759592656,
4.05856003591897));
#39869=CARTESIAN_POINT('Ctrl Pts',(-17.0025333313764,0.620291339687363,
4.10238814927032));
#39870=CARTESIAN_POINT('Ctrl Pts',(-17.0686910486192,1.78149552169719,3.51362940031347));
#39871=CARTESIAN_POINT('Ctrl Pts',(-17.1348487658619,2.94269970370699,2.92487065135663));
#39872=CARTESIAN_POINT('Ctrl Pts',(-17.2010064831046,3.78316696844663,1.70352504009155));
#39873=CARTESIAN_POINT('Ctrl Pts',(-17.2671642003473,3.91820786688699,0.408613470702097));
#39874=CARTESIAN_POINT('Ctrl Pts',(-17.33332191759,4.05324876532736,-0.886298098687392));
#39875=CARTESIAN_POINT('Ctrl Pts',(-17.3994796348327,3.48286329746849,-2.25477562620133));
#39876=CARTESIAN_POINT('Ctrl Pts',(-17.4656373520754,2.46812203746625,-3.0704546022939));
#39877=CARTESIAN_POINT('Ctrl Pts',(-17.5317950693181,1.45338077746402,-3.88613357838647));
#39878=CARTESIAN_POINT('Ctrl Pts',(-17.5979527865608,-0.00571627468155991,
-4.14901400305765));
#39879=CARTESIAN_POINT('Ctrl Pts',(-17.6641105038035,-1.241327235511,-3.73877313445908));
#39880=CARTESIAN_POINT('Ctrl Pts',(-17.7302682210463,-2.47693819634043,
-3.32853226586051));
#39881=CARTESIAN_POINT('Ctrl Pts',(-17.796425938289,-3.48906306585369,-2.24517010399219));
#39882=CARTESIAN_POINT('Ctrl Pts',(-17.8625836555317,-3.81444316077267,
-0.98455128348345));
#39883=CARTESIAN_POINT('Ctrl Pts',(-17.8793345963428,-3.89682845062647,
-0.665366279408071));
#39884=CARTESIAN_POINT('Ctrl Pts',(-17.8960855371539,-3.9351873837123,-0.334817570530705));
#39885=CARTESIAN_POINT('Ctrl Pts',(-17.912836477965,-3.93220475577819,-0.00358799939168875));
#39886=CARTESIAN_POINT('Ctrl Pts',(-18.0961635220349,-3.93260484470905,
-0.00359775545859465));
#39887=CARTESIAN_POINT('Ctrl Pts',(-18.0800890420313,-3.93550024191007,
-0.321368632766151));
#39888=CARTESIAN_POINT('Ctrl Pts',(-18.0640145620277,-3.90021738496414,
-0.638504667178511));
#39889=CARTESIAN_POINT('Ctrl Pts',(-18.0479400820241,-3.82428761157383,
-0.945590376684499));
#39890=CARTESIAN_POINT('Ctrl Pts',(-17.9817823647814,-3.51178353821415,
-2.2094626471555));
#39891=CARTESIAN_POINT('Ctrl Pts',(-17.9156246475387,-2.51076231488021,
-3.30309270330469));
#39892=CARTESIAN_POINT('Ctrl Pts',(-17.849466930296,-1.27940038582653,-3.72591620266241));
#39893=CARTESIAN_POINT('Ctrl Pts',(-17.7833092130533,-0.0480384567728447,
-4.14873970202014));
#39894=CARTESIAN_POINT('Ctrl Pts',(-17.7171514958106,1.41366417800062,-3.90075664458642));
#39895=CARTESIAN_POINT('Ctrl Pts',(-17.6509937785679,2.43667303636025,-3.09547111283409));
#39896=CARTESIAN_POINT('Ctrl Pts',(-17.5848360613252,3.45968189471991,-2.29018558108173));
#39897=CARTESIAN_POINT('Ctrl Pts',(-17.5186783440825,4.04399697666572,-0.927597575010803));
#39898=CARTESIAN_POINT('Ctrl Pts',(-17.4525206268397,3.9221719980135,0.368624082927527));
#39899=CARTESIAN_POINT('Ctrl Pts',(-17.386362909597,3.80034701936129,1.66484574086582));
#39900=CARTESIAN_POINT('Ctrl Pts',(-17.3202051923543,2.97238198011102,2.89470105067148));
#39901=CARTESIAN_POINT('Ctrl Pts',(-17.2540474751116,1.81724394790119,3.49527414237165));
#39902=CARTESIAN_POINT('Ctrl Pts',(-17.1878897578689,0.66210591569132,4.09584723407185));
#39903=CARTESIAN_POINT('Ctrl Pts',(-17.1217320406262,-0.82020510947818,
4.06713810766653));
#39904=CARTESIAN_POINT('Ctrl Pts',(-17.0555743233835,-1.9512219992786,3.42228718929996));
#39905=CARTESIAN_POINT('Ctrl Pts',(-16.9894166061408,-3.08223888907898,
2.77743627093341));
#39906=CARTESIAN_POINT('Ctrl Pts',(-16.9232588888981,-3.86196164351034,
1.51644356060562));
#39907=CARTESIAN_POINT('Ctrl Pts',(-16.8571011716554,-3.93350412389534,
0.216476797402691));
#39908=CARTESIAN_POINT('Ctrl Pts',(-16.8534552884485,-3.93744675581616,
0.144836976850907));
#39909=CARTESIAN_POINT('Ctrl Pts',(-16.8498094052417,-3.93923864578278,
0.0730787921851864));
#39910=CARTESIAN_POINT('Ctrl Pts',(-16.8461635220349,-3.93892856332975,
0.00130481274881613));
#39911=CARTESIAN_POINT('Origin',(-27.25,0.,0.));
#39912=CARTESIAN_POINT('',(-15.4128364779651,-3.92904698718966,0.00291690129643835));
#39913=CARTESIAN_POINT('',(-15.5961635220349,-3.92874808319062,0.00278058184941524));
#39914=CARTESIAN_POINT('',(-27.25,-3.933,-4.81653586104654E-16));
#39915=CARTESIAN_POINT('Ctrl Pts',(-15.4128364779651,-3.92904698718966,
0.00291690129643835));
#39916=CARTESIAN_POINT('Ctrl Pts',(-15.4355262635747,-3.93214136813459,
0.452493402373492));
#39917=CARTESIAN_POINT('Ctrl Pts',(-15.4582160491844,-3.86091700943663,
0.901119249181804));
#39918=CARTESIAN_POINT('Ctrl Pts',(-15.4809058347941,-3.71110271172466,
1.32175433405916));
#39919=CARTESIAN_POINT('Ctrl Pts',(-15.5470635520368,-3.27428183922111,
2.5482206165698));
#39920=CARTESIAN_POINT('Ctrl Pts',(-15.6132212692795,-2.16932140142824,
3.53672087259794));
#39921=CARTESIAN_POINT('Ctrl Pts',(-15.6793789865222,-0.901971758706727,
3.83480961757815));
#39922=CARTESIAN_POINT('Ctrl Pts',(-15.7455367037649,0.365377884014899,
4.13289836255838));
#39923=CARTESIAN_POINT('Ctrl Pts',(-15.8116944210077,1.79511673166521,3.74057559649053));
#39924=CARTESIAN_POINT('Ctrl Pts',(-15.8778521382504,2.73284041582605,2.83741098859542));
#39925=CARTESIAN_POINT('Ctrl Pts',(-15.9440098554931,3.67056409998685,1.93424638070035));
#39926=CARTESIAN_POINT('Ctrl Pts',(-16.0101675727358,4.11627262065823,0.520239930978085));
#39927=CARTESIAN_POINT('Ctrl Pts',(-16.0763252899785,3.86596116713799,-0.757404852608853));
#39928=CARTESIAN_POINT('Ctrl Pts',(-16.1424830072212,3.61564971361774,-2.03504963619579));
#39929=CARTESIAN_POINT('Ctrl Pts',(-16.2086407244639,2.66931828590586,-3.1763327536474));
#39930=CARTESIAN_POINT('Ctrl Pts',(-16.2747984417066,1.46011131543732,-3.65887862645186));
#39931=CARTESIAN_POINT('Ctrl Pts',(-16.3409561589493,0.250904344968778,
-4.14142449925632));
#39932=CARTESIAN_POINT('Ctrl Pts',(-16.4071138761921,-1.22117816825643,
-3.96523312741364));
#39933=CARTESIAN_POINT('Ctrl Pts',(-16.4732715934348,-2.28235077809922,
-3.21094889126006));
#39934=CARTESIAN_POINT('Ctrl Pts',(-16.5364598882782,-3.29589372584808,
-2.49051994213288));
#39935=CARTESIAN_POINT('Ctrl Pts',(-16.5996481831216,-3.9345855153387,-1.24272774869351));
#39936=CARTESIAN_POINT('Ctrl Pts',(-16.662836477965,-3.93909976961691,0.00107240331368951));
#39937=CARTESIAN_POINT('Ctrl Pts',(-16.8461635220349,-3.93892856332975,
0.00130481274881613));
#39938=CARTESIAN_POINT('Ctrl Pts',(-16.783651687999,-3.9336119303655,-1.22932240049576));
#39939=CARTESIAN_POINT('Ctrl Pts',(-16.7211398539631,-3.31035574987545,
-2.46459297315745));
#39940=CARTESIAN_POINT('Ctrl Pts',(-16.6586280199272,-2.3149856042573,-3.18750036056419));
#39941=CARTESIAN_POINT('Ctrl Pts',(-16.5924703026845,-1.26156239789562,
-3.95256993925005));
#39942=CARTESIAN_POINT('Ctrl Pts',(-16.5263125854418,0.208646221166482,
-4.14376828054371));
#39943=CARTESIAN_POINT('Ctrl Pts',(-16.4601548681991,1.42271250505289,-3.67358217881151));
#39944=CARTESIAN_POINT('Ctrl Pts',(-16.3939971509564,2.63677878893936,-3.20339607707928));
#39945=CARTESIAN_POINT('Ctrl Pts',(-16.3278394337137,3.59470273765017,-2.07182553232115));
#39946=CARTESIAN_POINT('Ctrl Pts',(-16.261681716471,3.8580339183116,-0.796800590908822));
#39947=CARTESIAN_POINT('Ctrl Pts',(-16.1955239992282,4.121365098973,0.478224350503403));
#39948=CARTESIAN_POINT('Ctrl Pts',(-16.1293662819855,3.69010351158514,1.89670368856975));
#39949=CARTESIAN_POINT('Ctrl Pts',(-16.0632085647428,2.7616414751588,2.80938663398225));
#39950=CARTESIAN_POINT('Ctrl Pts',(-15.9970508475001,1.83317943873238,3.72206957939482));
#39951=CARTESIAN_POINT('Ctrl Pts',(-15.9308931302574,0.407516953267295,
4.12895613215341));
#39952=CARTESIAN_POINT('Ctrl Pts',(-15.8647354130147,-0.862807400563734,
3.84381064648713));
#39953=CARTESIAN_POINT('Ctrl Pts',(-15.798577695772,-2.13313175439469,3.55866516082088));
#39954=CARTESIAN_POINT('Ctrl Pts',(-15.7324199785293,-3.24811797659165,
2.58148763672992));
#39955=CARTESIAN_POINT('Ctrl Pts',(-15.6662622612866,-3.69742681482843,
1.35954104222826));
#39956=CARTESIAN_POINT('Ctrl Pts',(-15.6428960148693,-3.85611821878305,
0.927961682694594));
#39957=CARTESIAN_POINT('Ctrl Pts',(-15.6195297684521,-3.93177089551102,
0.465849045989298));
#39958=CARTESIAN_POINT('Ctrl Pts',(-15.5961635220349,-3.92874808319062,
0.00278058184941524));
#39959=CARTESIAN_POINT('Origin',(-27.25,0.,0.));
#39960=CARTESIAN_POINT('',(-14.1628364779651,-3.92858680232973,-0.00269909542886165));
#39961=CARTESIAN_POINT('',(-14.3461635220349,-3.92887651838583,-0.00284137689771559));
#39962=CARTESIAN_POINT('',(-27.25,-3.933,-4.81653586104654E-16));
#39963=CARTESIAN_POINT('Ctrl Pts',(-14.1628364779651,-3.92858680232973,
-0.00269909542886165));
#39964=CARTESIAN_POINT('Ctrl Pts',(-14.2052466267851,-3.92327502960724,
0.837865115529639));
#39965=CARTESIAN_POINT('Ctrl Pts',(-14.2476567756052,-3.65903126967813,
1.6814769480063));
#39966=CARTESIAN_POINT('Ctrl Pts',(-14.2900669244253,-3.16092681968387,
2.35114004201739));
#39967=CARTESIAN_POINT('Ctrl Pts',(-14.356224641668,-2.38390871725174,3.39578107379964));
#39968=CARTESIAN_POINT('Ctrl Pts',(-14.4223823589108,-1.03780362497608,
4.01712751967761));
#39969=CARTESIAN_POINT('Ctrl Pts',(-14.4885400761535,0.261264013030088,
3.93078350613078));
#39970=CARTESIAN_POINT('Ctrl Pts',(-14.5546977933962,1.56033165103629,3.84443949258394));
#39971=CARTESIAN_POINT('Ctrl Pts',(-14.6208555106389,2.81236183477307,3.05040501961242));
#39972=CARTESIAN_POINT('Ctrl Pts',(-14.6870132278816,3.44428905442718,1.91211682857702));
#39973=CARTESIAN_POINT('Ctrl Pts',(-14.7531709451243,4.07621627408126,0.773828637541696));
#39974=CARTESIAN_POINT('Ctrl Pts',(-14.819328662367,4.08804052965268,-0.708713271557329));
#39975=CARTESIAN_POINT('Ctrl Pts',(-14.8854863796097,3.47434975269838,-1.85693609273422));
#39976=CARTESIAN_POINT('Ctrl Pts',(-14.9516440968524,2.86065897574404,-3.00515891391118));
#39977=CARTESIAN_POINT('Ctrl Pts',(-15.0178018140951,1.62145316626383,-3.81906264716589));
#39978=CARTESIAN_POINT('Ctrl Pts',(-15.0839595313379,0.32392800228367,-3.92611621146278));
#39979=CARTESIAN_POINT('Ctrl Pts',(-15.1501172485806,-0.973597161696452,
-4.03316977575966));
#39980=CARTESIAN_POINT('Ctrl Pts',(-15.2162749658233,-2.32944168017656,
-3.43337317109877));
#39981=CARTESIAN_POINT('Ctrl Pts',(-15.282432683066,-3.1230232858095,-2.40125871427174));
#39982=CARTESIAN_POINT('Ctrl Pts',(-15.325900614699,-3.64443412669937,-1.72312345633623));
#39983=CARTESIAN_POINT('Ctrl Pts',(-15.369368546332,-3.92311893032414,-0.858358782343565));
#39984=CARTESIAN_POINT('Ctrl Pts',(-15.4128364779651,-3.92904698718966,
0.00291690129643835));
#39985=CARTESIAN_POINT('Ctrl Pts',(-15.5961635220349,-3.92874808319062,
0.00278058184941524));
#39986=CARTESIAN_POINT('Ctrl Pts',(-15.5533720512094,-3.92321229524635,
-0.845253814416959));
#39987=CARTESIAN_POINT('Ctrl Pts',(-15.5105805803839,-3.65381503891493,
-1.69649386003438));
#39988=CARTESIAN_POINT('Ctrl Pts',(-15.4677891095584,-3.14735501292257,
-2.36927696125771));
#39989=CARTESIAN_POINT('Ctrl Pts',(-15.4016313923157,-2.36434291850349,
-3.40943270532938));
#39990=CARTESIAN_POINT('Ctrl Pts',(-15.335473675073,-1.01468727538901,-4.0230285285604));
#39991=CARTESIAN_POINT('Ctrl Pts',(-15.2693159578303,0.28386235315941,-3.92921608733526));
#39992=CARTESIAN_POINT('Ctrl Pts',(-15.2031582405876,1.58241198170787,-3.83540364611011));
#39993=CARTESIAN_POINT('Ctrl Pts',(-15.1370005233449,2.82985559569023,-3.03418294042861));
#39994=CARTESIAN_POINT('Ctrl Pts',(-15.0708428061022,3.45522699964562,-1.892279915191));
#39995=CARTESIAN_POINT('Ctrl Pts',(-15.0046850888595,4.08059840360102,-0.750376889953396));
#39996=CARTESIAN_POINT('Ctrl Pts',(-14.9385273716168,4.08389759752955,0.732208454840364));
#39997=CARTESIAN_POINT('Ctrl Pts',(-14.8723696543741,3.46361451060769,1.87688343229494));
#39998=CARTESIAN_POINT('Ctrl Pts',(-14.8062119371313,2.84333142368583,3.02155840974951));
#39999=CARTESIAN_POINT('Ctrl Pts',(-14.7400542198886,1.59946605591359,3.8283230198649));
#40000=CARTESIAN_POINT('Ctrl Pts',(-14.6738965026459,0.301346807181522,
3.92791382266934));
#40001=CARTESIAN_POINT('Ctrl Pts',(-14.6077387854032,-0.996772441550546,
4.02750462547378));
#40002=CARTESIAN_POINT('Ctrl Pts',(-14.5415810681605,-2.34914557124244,
3.41992162096726));
#40003=CARTESIAN_POINT('Ctrl Pts',(-14.4754233509178,-3.13677920051122,
2.38326103139282));
#40004=CARTESIAN_POINT('Ctrl Pts',(-14.4323367412902,-3.64974222475523,
1.70811394348043));
#40005=CARTESIAN_POINT('Ctrl Pts',(-14.3892501316625,-3.92316870128949,
0.850971859025732));
#40006=CARTESIAN_POINT('Ctrl Pts',(-14.3461635220349,-3.92887651838583,
-0.00284137689771559));
#40007=CARTESIAN_POINT('Origin',(-27.25,0.,0.));
#40008=CARTESIAN_POINT('',(-12.9128364779651,-3.93881934497104,-0.00143284320175408));
#40009=CARTESIAN_POINT('',(-13.0961635220349,-3.93900688952732,-0.0012041997225416));
#40010=CARTESIAN_POINT('',(-27.25,-3.933,-4.81653586104654E-16));
#40011=CARTESIAN_POINT('Ctrl Pts',(-12.9128364779651,-3.93881934497104,
-0.00143284320175408));
#40012=CARTESIAN_POINT('Ctrl Pts',(-12.9749669899956,-3.93308493623946,
1.22177796479248));
#40013=CARTESIAN_POINT('Ctrl Pts',(-13.0370975020261,-3.31842665197076,
2.44996177311049));
#40014=CARTESIAN_POINT('Ctrl Pts',(-13.0992280140566,-2.33327606901329,
3.17413620412613));
#40015=CARTESIAN_POINT('Ctrl Pts',(-13.1653857312993,-1.28426952490503,
3.94525051939226));
#40016=CARTESIAN_POINT('Ctrl Pts',(-13.231543448542,0.184815410869772,4.14489965346203));
#40017=CARTESIAN_POINT('Ctrl Pts',(-13.2977011657847,1.40156531041257,3.68170239661253));
#40018=CARTESIAN_POINT('Ctrl Pts',(-13.3638588830274,2.61831520995538,3.21850513976302));
#40019=CARTESIAN_POINT('Ctrl Pts',(-13.4300166002701,3.58273007326619,2.09246149199423));
#40020=CARTESIAN_POINT('Ctrl Pts',(-13.4961743175128,3.85338851730353,0.818971789067029));
#40021=CARTESIAN_POINT('Ctrl Pts',(-13.5623320347555,4.12404696134087,-0.454517913860173));
#40022=CARTESIAN_POINT('Ctrl Pts',(-13.6284897519982,3.70094898610474,-1.87545367194579));
#40023=CARTESIAN_POINT('Ctrl Pts',(-13.6946474692409,2.77775035167917,-2.79346037027924));
#40024=CARTESIAN_POINT('Ctrl Pts',(-13.7608051864837,1.85455171725356,-3.71146706861271));
#40025=CARTESIAN_POINT('Ctrl Pts',(-13.8269629037264,0.431252423638476,
-4.12654470719399));
#40026=CARTESIAN_POINT('Ctrl Pts',(-13.8931206209691,-0.840690602721897,
-3.8487085063784));
#40027=CARTESIAN_POINT('Ctrl Pts',(-13.9592783382118,-2.11263362908223,
-3.57087230556282));
#40028=CARTESIAN_POINT('Ctrl Pts',(-14.0254360554545,-3.23322038818787,
-2.60012226535041));
#40029=CARTESIAN_POINT('Ctrl Pts',(-14.0915937726972,-3.68954821144631,
-1.38077943640092));
#40030=CARTESIAN_POINT('Ctrl Pts',(-14.1153413411198,-3.85334884813117,
-0.943091613000512));
#40031=CARTESIAN_POINT('Ctrl Pts',(-14.1390889095424,-3.93156113016593,
-0.473373136164104));
#40032=CARTESIAN_POINT('Ctrl Pts',(-14.1628364779651,-3.92858680232973,
-0.00269909542886165));
#40033=CARTESIAN_POINT('Ctrl Pts',(-14.3461635220349,-3.92887651838583,
-0.00284137689771559));
#40034=CARTESIAN_POINT('Ctrl Pts',(-14.3230924144198,-3.93193281971971,
-0.460023253573669));
#40035=CARTESIAN_POINT('Ctrl Pts',(-14.3000213068047,-3.85822984188482,
-0.916250695417715));
#40036=CARTESIAN_POINT('Ctrl Pts',(-14.2769501991897,-3.70344093352043,
-1.34307190739762));
#40037=CARTESIAN_POINT('Ctrl Pts',(-14.210792481947,-3.2595749084152,-2.56700608197123));
#40038=CARTESIAN_POINT('Ctrl Pts',(-14.1446347647043,-2.14894872935906,
-3.54913625647613));
#40039=CARTESIAN_POINT('Ctrl Pts',(-14.0784770474615,-0.879906017600263,
-3.83993259012528));
#40040=CARTESIAN_POINT('Ctrl Pts',(-14.0123193302188,0.389136694158539,
-4.13072892377443));
#40041=CARTESIAN_POINT('Ctrl Pts',(-13.9461616129761,1.81659593862004,-3.73019141656785));
#40042=CARTESIAN_POINT('Ctrl Pts',(-13.8800038957334,2.74911074231022,-2.82164969885171));
#40043=CARTESIAN_POINT('Ctrl Pts',(-13.8138461784907,3.68162554600042,-1.91310798113555));
#40044=CARTESIAN_POINT('Ctrl Pts',(-13.747688461248,4.11919590891929,-0.496562052909773));
#40045=CARTESIAN_POINT('Ctrl Pts',(-13.6815307440053,3.86154192858324,0.77962223564303));
#40046=CARTESIAN_POINT('Ctrl Pts',(-13.6153730267626,3.60388794824719,2.0558065241958));
#40047=CARTESIAN_POINT('Ctrl Pts',(-13.5492153095199,2.65100962465633,3.19162917307553));
#40048=CARTESIAN_POINT('Ctrl Pts',(-13.4830575922772,1.43904796254968,3.66721390949546));
#40049=CARTESIAN_POINT('Ctrl Pts',(-13.4168998750344,0.227086300443004,
4.14279864591541));
#40050=CARTESIAN_POINT('Ctrl Pts',(-13.3507421577917,-1.24395870017946,
3.95814546987541));
#40051=CARTESIAN_POINT('Ctrl Pts',(-13.284584440549,-2.30077647205636,3.19777180582781));
#40052=CARTESIAN_POINT('Ctrl Pts',(-13.221777467711,-3.30406872365444,2.47590941312473));
#40053=CARTESIAN_POINT('Ctrl Pts',(-13.1589704948729,-3.9340305853428,1.23516767268343));
#40054=CARTESIAN_POINT('Ctrl Pts',(-13.0961635220349,-3.93900688952732,
-0.0012041997225416));
#40055=CARTESIAN_POINT('Origin',(-27.25,0.,0.));
#40056=CARTESIAN_POINT('',(-11.6628364779651,-3.93283223678505,0.00359684100027402));
#40057=CARTESIAN_POINT('',(-11.8461635220349,-3.93242970906489,0.00359528210897375));
#40058=CARTESIAN_POINT('',(-27.25,-3.933,-4.81653586104654E-16));
#40059=CARTESIAN_POINT('Ctrl Pts',(-11.6628364779651,-3.93283223678505,
0.00359684100027402));
#40060=CARTESIAN_POINT('Ctrl Pts',(-11.6785296359633,-3.93567289122675,
0.313783719918517));
#40061=CARTESIAN_POINT('Ctrl Pts',(-11.6942227939615,-3.90206523256919,
0.623362207654243));
#40062=CARTESIAN_POINT('Ctrl Pts',(-11.7099159519597,-3.82966180971454,
0.923584473553057));
#40063=CARTESIAN_POINT('Ctrl Pts',(-11.7760736692024,-3.52443037209239,
2.18923283952105));
#40064=CARTESIAN_POINT('Ctrl Pts',(-11.8422313864451,-2.52971422453108,
3.28860089028295));
#40065=CARTESIAN_POINT('Ctrl Pts',(-11.9083891036878,-1.30080392122511,
3.71849795147176));
#40066=CARTESIAN_POINT('Ctrl Pts',(-11.9745468209305,-0.0718936179191432,
4.14839501266058));
#40067=CARTESIAN_POINT('Ctrl Pts',(-12.0407045381732,1.39121084113145,3.90882108427631));
#40068=CARTESIAN_POINT('Ctrl Pts',(-12.1068622554159,2.41883334617547,3.10943131456605));
#40069=CARTESIAN_POINT('Ctrl Pts',(-12.1730199726586,3.44645585121948,2.31004154485579));
#40070=CARTESIAN_POINT('Ctrl Pts',(-12.2391776899013,4.03859640225687,0.950835933819561));
#40071=CARTESIAN_POINT('Ctrl Pts',(-12.305335407144,3.92422692730571,-0.346064848811758));
#40072=CARTESIAN_POINT('Ctrl Pts',(-12.3714931243867,3.80985745235456,-1.64296563144304));
#40073=CARTESIAN_POINT('Ctrl Pts',(-12.4376508416295,2.98897795141481,-2.87756158566949));
#40074=CARTESIAN_POINT('Ctrl Pts',(-12.5038085588722,1.83731237732077,-3.48476700580085));
#40075=CARTESIAN_POINT('Ctrl Pts',(-12.5699662761149,0.685646803226695,
-4.09197242593223));
#40076=CARTESIAN_POINT('Ctrl Pts',(-12.6361239933576,-0.796804844021701,
-4.07178731196857));
#40077=CARTESIAN_POINT('Ctrl Pts',(-12.7022817106003,-1.93151107210173,
-3.43345057266342));
#40078=CARTESIAN_POINT('Ctrl Pts',(-12.768439427843,-3.06621730018176,-2.79511383335826));
#40079=CARTESIAN_POINT('Ctrl Pts',(-12.8345971450857,-3.8531781090934,-1.53862546871164));
#40080=CARTESIAN_POINT('Ctrl Pts',(-12.9007548623284,-3.93219443732835,
-0.239091538157064));
#40081=CARTESIAN_POINT('Ctrl Pts',(-12.9047820675406,-3.93700438214174,
-0.159985274569187));
#40082=CARTESIAN_POINT('Ctrl Pts',(-12.9088092727529,-3.93919104061586,
-0.0807195057544253));
#40083=CARTESIAN_POINT('Ctrl Pts',(-12.9128364779651,-3.93881934497104,
-0.00143284320175408));
#40084=CARTESIAN_POINT('Ctrl Pts',(-13.0961635220349,-3.93900688952732,
-0.0012041997225416));
#40085=CARTESIAN_POINT('Ctrl Pts',(-13.0928127776302,-3.9392723747537,-0.0671644895814343));
#40086=CARTESIAN_POINT('Ctrl Pts',(-13.0894620332256,-3.93775902008951,
-0.133112341879996));
#40087=CARTESIAN_POINT('Ctrl Pts',(-13.0861112888209,-3.93442861297152,
-0.198968303873675));
#40088=CARTESIAN_POINT('Ctrl Pts',(-13.0199535715782,-3.86867243887846,
-1.49924059747244));
#40089=CARTESIAN_POINT('Ctrl Pts',(-12.9537958543355,-3.09456954756098,
-2.76369103261481));
#40090=CARTESIAN_POINT('Ctrl Pts',(-12.8876381370927,-1.96643381565171,
-3.41356923837453));
#40091=CARTESIAN_POINT('Ctrl Pts',(-12.82148041985,-0.838298083742433,-4.06344744413424));
#40092=CARTESIAN_POINT('Ctrl Pts',(-12.7553227026073,0.643870488758641,
-4.09875342051129));
#40093=CARTESIAN_POINT('Ctrl Pts',(-12.6891649853646,1.80166997539429,-3.50332730361839));
#40094=CARTESIAN_POINT('Ctrl Pts',(-12.6230072681219,2.95946946202995,-2.90790118672549));
#40095=CARTESIAN_POINT('Ctrl Pts',(-12.5568495508792,3.79289986280018,-1.68174297656263));
#40096=CARTESIAN_POINT('Ctrl Pts',(-12.4906918336365,3.92049256479515,-0.386076347244129));
#40097=CARTESIAN_POINT('Ctrl Pts',(-12.4245341163938,4.04808526679012,0.909590282074408));
#40098=CARTESIAN_POINT('Ctrl Pts',(-12.3583763991511,3.46984027000979,2.27476533054859));
#40099=CARTESIAN_POINT('Ctrl Pts',(-12.2922186819084,2.45042552589917,3.08459586308112));
#40100=CARTESIAN_POINT('Ctrl Pts',(-12.2260609646657,1.43101078178864,3.89442639561358));
#40101=CARTESIAN_POINT('Ctrl Pts',(-12.1599032474229,-0.0295737096520995,
4.14891241220449));
#40102=CARTESIAN_POINT('Ctrl Pts',(-12.0937455301802,-1.26280525057983,
3.73157336731082));
#40103=CARTESIAN_POINT('Ctrl Pts',(-12.0275878129375,-2.4960367915077,3.31423432241709));
#40104=CARTESIAN_POINT('Ctrl Pts',(-11.9614300956948,-3.5019153819225,2.22507021603861));
#40105=CARTESIAN_POINT('Ctrl Pts',(-11.8952723784521,-3.82004131683789,
0.962601285147102));
#40106=CARTESIAN_POINT('Ctrl Pts',(-11.8789027596464,-3.89875624993747,
0.650224498067916));
#40107=CARTESIAN_POINT('Ctrl Pts',(-11.8625331408406,-3.93536475652441,
0.327237433006823));
#40108=CARTESIAN_POINT('Ctrl Pts',(-11.8461635220349,-3.93242970906489,
0.00359528210897375));
#40109=CARTESIAN_POINT('Origin',(-27.25,0.,0.));
#40110=CARTESIAN_POINT('',(-10.4128364779651,-3.92668394074156,-0.000755260177356665));
#40111=CARTESIAN_POINT('',(-10.5961635220349,-3.92677159154525,-0.000969419521030996));
#40112=CARTESIAN_POINT('',(-27.25,-3.933,-4.81653586104654E-16));
#40113=CARTESIAN_POINT('Ctrl Pts',(-10.4128364779651,-3.92668394074156,
-0.000755260177356665));
#40114=CARTESIAN_POINT('Ctrl Pts',(-10.4482499991737,-3.9254780780401,0.701988440301541));
#40115=CARTESIAN_POINT('Ctrl Pts',(-10.4836635203823,-3.74567922430472,
1.40530796224216));
#40116=CARTESIAN_POINT('Ctrl Pts',(-10.5190770415909,-3.39095092494106,
2.00518569743945));
#40117=CARTESIAN_POINT('Ctrl Pts',(-10.5852347588336,-2.72826577739384,
3.12584640077951));
#40118=CARTESIAN_POINT('Ctrl Pts',(-10.6513924760763,-1.45508055671478,
3.88549745165729));
#40119=CARTESIAN_POINT('Ctrl Pts',(-10.717550193319,-0.154143623967885,
3.93643971118121));
#40120=CARTESIAN_POINT('Ctrl Pts',(-10.7837079105617,1.14679330877898,3.98738197070513));
#40121=CARTESIAN_POINT('Ctrl Pts',(-10.8498656278044,2.47548195359371,3.32961543887524));
#40122=CARTESIAN_POINT('Ctrl Pts',(-10.9160233450471,3.22376953148229,2.26420579110221));
#40123=CARTESIAN_POINT('Ctrl Pts',(-10.9821810622898,3.97205710937091,1.19879614332912));
#40124=CARTESIAN_POINT('Ctrl Pts',(-11.0483387795326,4.13994362033332,-0.274256620387207));
#40125=CARTESIAN_POINT('Ctrl Pts',(-11.1144964967753,3.65058589377732,-1.48072296150509));
#40126=CARTESIAN_POINT('Ctrl Pts',(-11.180654214018,3.16122816722133,-2.68718930262293));
#40127=CARTESIAN_POINT('Ctrl Pts',(-11.2468119312607,2.01462620314707,-3.6270692211423));
#40128=CARTESIAN_POINT('Ctrl Pts',(-11.3129696485034,0.735590064147372,
-3.87017119958562));
#40129=CARTESIAN_POINT('Ctrl Pts',(-11.3791273657461,-0.543446074852362,
-4.11327317802895));
#40130=CARTESIAN_POINT('Ctrl Pts',(-11.4452850829888,-1.9549163887775,-3.65959721639607));
#40131=CARTESIAN_POINT('Ctrl Pts',(-11.5114428002315,-2.85277818189858,
-2.71679489499259));
#40132=CARTESIAN_POINT('Ctrl Pts',(-11.561907359476,-3.53765972770696,-1.99763308610216));
#40133=CARTESIAN_POINT('Ctrl Pts',(-11.6123719187205,-3.92369753143239,
-0.993872510282313));
#40134=CARTESIAN_POINT('Ctrl Pts',(-11.6628364779651,-3.93283223678505,
0.00359684100027402));
#40135=CARTESIAN_POINT('Ctrl Pts',(-11.8461635220349,-3.93242970906489,
0.00359528210897375));
#40136=CARTESIAN_POINT('Ctrl Pts',(-11.7963754235979,-3.92350277963752,
-0.980760398892982));
#40137=CARTESIAN_POINT('Ctrl Pts',(-11.746587325161,-3.54877084267473,-1.97117607336868));
#40138=CARTESIAN_POINT('Ctrl Pts',(-11.696799226724,-2.88034263954507,-2.68755338092733));
#40139=CARTESIAN_POINT('Ctrl Pts',(-11.6306415094813,-1.9921447479208,-3.63946536070601));
#40140=CARTESIAN_POINT('Ctrl Pts',(-11.5644837922386,-0.585375685256206,
-4.1075155648589));
#40141=CARTESIAN_POINT('Ctrl Pts',(-11.4983260749959,0.696073657831846,
-3.87747319260726));
#40142=CARTESIAN_POINT('Ctrl Pts',(-11.4321683577532,1.9775230009199,-3.64743082035563));
#40143=CARTESIAN_POINT('Ctrl Pts',(-11.3660106405104,3.13365262443137,-2.71929587169946));
#40144=CARTESIAN_POINT('Ctrl Pts',(-11.2998529232677,3.63529157009874,-1.51788408545725));
#40145=CARTESIAN_POINT('Ctrl Pts',(-11.233695206025,4.13693051576613,-0.316472299215008));
#40146=CARTESIAN_POINT('Ctrl Pts',(-11.1675374887823,3.98407878358935,1.15821632461326));
#40147=CARTESIAN_POINT('Ctrl Pts',(-11.1013797715396,3.24669799027985,2.23120349955538));
#40148=CARTESIAN_POINT('Ctrl Pts',(-11.0352220542969,2.50931719697037,3.30419067449748));
#40149=CARTESIAN_POINT('Ctrl Pts',(-10.9690643370542,1.18740734252809,3.97547640055349));
#40150=CARTESIAN_POINT('Ctrl Pts',(-10.9029066198114,-0.113981507558553,
3.93780714515707));
#40151=CARTESIAN_POINT('Ctrl Pts',(-10.8367489025687,-1.41537035764512,
3.90013788976065));
#40152=CARTESIAN_POINT('Ctrl Pts',(-10.770591185326,-2.69623820337613,3.15351365291197));
#40153=CARTESIAN_POINT('Ctrl Pts',(-10.7044334680833,-3.37032027689551,
2.03967108320493));
#40154=CARTESIAN_POINT('Ctrl Pts',(-10.6683434860672,-3.73804169965065,
1.43205401319522));
#40155=CARTESIAN_POINT('Ctrl Pts',(-10.6322535040511,-3.92519224964437,
0.715157955617078));
#40156=CARTESIAN_POINT('Ctrl Pts',(-10.5961635220349,-3.92677159154525,
-0.000969419521030996));
#40157=CARTESIAN_POINT('Origin',(-27.25,0.,0.));
#40158=CARTESIAN_POINT('',(-9.16283647796508,-3.93560336451511,-0.00320692409599477));
#40159=CARTESIAN_POINT('',(-9.34616352203492,-3.93598498577306,-0.00309328146845306));
#40160=CARTESIAN_POINT('',(-27.25,-3.933,-4.81653586104654E-16));
#40161=CARTESIAN_POINT('Ctrl Pts',(-9.16283647796508,-3.93560336451511,
-0.00320692409599477));
#40162=CARTESIAN_POINT('Ctrl Pts',(-9.21797036238408,-3.92600068327744,
1.08458219431681));
#40163=CARTESIAN_POINT('Ctrl Pts',(-9.27310424680308,-3.45624748136882,
2.17965170096766));
#40164=CARTESIAN_POINT('Ctrl Pts',(-9.32823813122209,-2.65457303229532,
2.91076620029585));
#40165=CARTESIAN_POINT('Ctrl Pts',(-9.3943958484648,-1.69260650152374,3.78806455916005));
#40166=CARTESIAN_POINT('Ctrl Pts',(-9.46055356570752,-0.252715911624579,
4.14131434950024));
#40167=CARTESIAN_POINT('Ctrl Pts',(-9.52671128295023,1.00604782497662,3.80882995556827));
#40168=CARTESIAN_POINT('Ctrl Pts',(-9.59286900019294,2.26481156157778,3.4763455616363));
#40169=CARTESIAN_POINT('Ctrl Pts',(-9.65902671743565,3.34244844488098,2.4581269834322));
#40170=CARTESIAN_POINT('Ctrl Pts',(-9.72518443467836,3.74571435190455,1.22022204967401));
#40171=CARTESIAN_POINT('Ctrl Pts',(-9.79134215192107,4.14898025892809,-0.0176828840841227));
#40172=CARTESIAN_POINT('Ctrl Pts',(-9.85749986916378,3.87787518967209,-1.47527417339632));
#40173=CARTESIAN_POINT('Ctrl Pts',(-9.92365758640649,3.05648638000691,-2.48539913603562));
#40174=CARTESIAN_POINT('Ctrl Pts',(-9.9898153036492,2.2350975703417,-3.49552409867495));
#40175=CARTESIAN_POINT('Ctrl Pts',(-10.0559730208919,0.863425020267273,
-4.05818273464135));
#40176=CARTESIAN_POINT('Ctrl Pts',(-10.1221307381346,-0.430704370021922,
-3.91584111044081));
#40177=CARTESIAN_POINT('Ctrl Pts',(-10.1882884553773,-1.72483376031112,
-3.77349948624028));
#40178=CARTESIAN_POINT('Ctrl Pts',(-10.25444617262,-2.94141999081508,-2.92615760187282));
#40179=CARTESIAN_POINT('Ctrl Pts',(-10.3206038898627,-3.52362056885937,
-1.7616514817879));
#40180=CARTESIAN_POINT('Ctrl Pts',(-10.3513480858969,-3.794175380128,-1.22049308136327));
#40181=CARTESIAN_POINT('Ctrl Pts',(-10.382092281931,-3.92773080866145,-0.610841163863507));
#40182=CARTESIAN_POINT('Ctrl Pts',(-10.4128364779651,-3.92668394074156,
-0.000755260177356665));
#40183=CARTESIAN_POINT('Ctrl Pts',(-10.5961635220349,-3.92677159154525,
-0.000969419521030996));
#40184=CARTESIAN_POINT('Ctrl Pts',(-10.5660957868083,-3.92808739253641,
-0.59759837584792));
#40185=CARTESIAN_POINT('Ctrl Pts',(-10.5360280515818,-3.80059642103898,
-1.19369378224975));
#40186=CARTESIAN_POINT('Ctrl Pts',(-10.5059603163552,-3.54140705662186,
-1.72561668855637));
#40187=CARTESIAN_POINT('Ctrl Pts',(-10.4398025991125,-2.97111546152114,
-2.89600098804493));
#40188=CARTESIAN_POINT('Ctrl Pts',(-10.3736448818698,-1.76323597001208,
-3.7557086844566));
#40189=CARTESIAN_POINT('Ctrl Pts',(-10.3074871646271,-0.470625921786567,
-3.9112438096158));
#40190=CARTESIAN_POINT('Ctrl Pts',(-10.2413294473844,0.821984126439017,
-4.06677893477501));
#40191=CARTESIAN_POINT('Ctrl Pts',(-10.1751717301416,2.19932473138106,-3.51814148868164));
#40192=CARTESIAN_POINT('Ctrl Pts',(-10.1090140128989,3.03097467299996,-2.51644777973797));
#40193=CARTESIAN_POINT('Ctrl Pts',(-10.0428562956562,3.86262461461886,-1.51475407079431));
#40194=CARTESIAN_POINT('Ctrl Pts',(-9.97669857841352,4.14858389291461,-0.0600040990003427));
#40195=CARTESIAN_POINT('Ctrl Pts',(-9.91054086117081,3.75796636653772,1.18194995007685));
#40196=CARTESIAN_POINT('Ctrl Pts',(-9.8443831439281,3.36734884016083,2.42390399915404));
#40197=CARTESIAN_POINT('Ctrl Pts',(-9.77822542668539,2.30015450911129,3.45306212551446));
#40198=CARTESIAN_POINT('Ctrl Pts',(-9.71206770944267,1.04484784600073,3.79836937056193));
#40199=CARTESIAN_POINT('Ctrl Pts',(-9.64590999219997,-0.210458817109762,
4.14367661560937));
#40200=CARTESIAN_POINT('Ctrl Pts',(-9.57975227495726,-1.65387781228124,
3.80513297934396));
#40201=CARTESIAN_POINT('Ctrl Pts',(-9.51359455771455,-2.62474324416494,
2.93769293812779));
#40202=CARTESIAN_POINT('Ctrl Pts',(-9.457784212488,-3.44376084604448,2.20592451894252));
#40203=CARTESIAN_POINT('Ctrl Pts',(-9.40197386726146,-3.92648420156164,
1.09776529091601));
#40204=CARTESIAN_POINT('Ctrl Pts',(-9.34616352203492,-3.93598498577306,
-0.00309328146845306));
#40205=CARTESIAN_POINT('Origin',(-27.25,0.,0.));
#40206=CARTESIAN_POINT('',(-7.91283647796508,-3.93687099541924,0.00275879756119139));
#40207=CARTESIAN_POINT('',(-8.09616352203492,-3.93651676133011,0.00290543094219859));
#40208=CARTESIAN_POINT('',(-27.25,-3.933,-4.81653586104654E-16));
#40209=CARTESIAN_POINT('Ctrl Pts',(-7.91283647796508,-3.93687099541924,
0.00275879756119139));
#40210=CARTESIAN_POINT('Ctrl Pts',(-7.92153300835178,-3.93823823749687,
0.174197263911898));
#40211=CARTESIAN_POINT('Ctrl Pts',(-7.93022953873848,-3.92800924152857,
0.345471489671227));
#40212=CARTESIAN_POINT('Ctrl Pts',(-7.93892606912519,-3.90562996449843,
0.515143122817789));
#40213=CARTESIAN_POINT('Ctrl Pts',(-8.0050837863679,-3.73538254213334,1.80589787565366));
#40214=CARTESIAN_POINT('Ctrl Pts',(-8.07124150361061,-2.86197325404654,
3.00390728327072));
#40215=CARTESIAN_POINT('Ctrl Pts',(-8.13739922085332,-1.68516941052714,
3.56083163241368));
#40216=CARTESIAN_POINT('Ctrl Pts',(-8.20355693809603,-0.508365567007741,
4.11775598155664));
#40217=CARTESIAN_POINT('Ctrl Pts',(-8.26971465533874,0.971832831944265,
4.03359527222549));
#40218=CARTESIAN_POINT('Ctrl Pts',(-8.33587237258145,2.07792562607827,3.34687062030512));
#40219=CARTESIAN_POINT('Ctrl Pts',(-8.40203008982416,3.18401842021227,2.66014596838474));
#40220=CARTESIAN_POINT('Ctrl Pts',(-8.46818780706687,3.91600560952826,1.37085737387514));
#40221=CARTESIAN_POINT('Ctrl Pts',(-8.53434552430958,3.93885005413059,0.0691238573130398));
#40222=CARTESIAN_POINT('Ctrl Pts',(-8.60050324155228,3.96169449873291,-1.23260965924906));
#40223=CARTESIAN_POINT('Ctrl Pts',(-8.666660958795,3.27539619862157,-2.54678809786367));
#40224=CARTESIAN_POINT('Ctrl Pts',(-8.73281867603771,2.1940800769382,-3.27190013181289));
#40225=CARTESIAN_POINT('Ctrl Pts',(-8.79897639328041,1.11276395525483,-3.99701216576211));
#40226=CARTESIAN_POINT('Ctrl Pts',(-8.86513411052312,-0.363569988000565,
-4.13305779504593));
#40227=CARTESIAN_POINT('Ctrl Pts',(-8.93129182776583,-1.55919038881141,
-3.61776770785694));
#40228=CARTESIAN_POINT('Ctrl Pts',(-8.99744954500854,-2.75481078962223,
-3.10247762066796));
#40229=CARTESIAN_POINT('Ctrl Pts',(-9.06360726225126,-3.66971764798851,
-1.93585181700621));
#40230=CARTESIAN_POINT('Ctrl Pts',(-9.12976497949396,-3.88514984134968,
-0.651865451481312));
#40231=CARTESIAN_POINT('Ctrl Pts',(-9.14078881231767,-3.92104721785293,
-0.437915339062323));
#40232=CARTESIAN_POINT('Ctrl Pts',(-9.15181264514137,-3.93752338799502,
-0.220706661602113));
#40233=CARTESIAN_POINT('Ctrl Pts',(-9.16283647796508,-3.93560336451511,
-0.00320692409599477));
#40234=CARTESIAN_POINT('Ctrl Pts',(-9.34616352203492,-3.93598498577306,
-0.00309328146845306));
#40235=CARTESIAN_POINT('Ctrl Pts',(-9.33581615001875,-3.93774645397904,
-0.207195104157573));
#40236=CARTESIAN_POINT('Ctrl Pts',(-9.32546877800259,-3.92324134568439,
-0.411045973741836));
#40237=CARTESIAN_POINT('Ctrl Pts',(-9.31512140598642,-3.89159701236423,
-0.612200612441036));
#40238=CARTESIAN_POINT('Ctrl Pts',(-9.24896368874371,-3.68927348008389,
-1.89831767562679));
#40239=CARTESIAN_POINT('Ctrl Pts',(-9.182805971501,-2.78631454692713,-3.0742153558314));
#40240=CARTESIAN_POINT('Ctrl Pts',(-9.11664825425829,-1.59601266230262,
-3.60167467690866));
#40241=CARTESIAN_POINT('Ctrl Pts',(-9.05049053701558,-0.405710777678086,
-4.12913399798593));
#40242=CARTESIAN_POINT('Ctrl Pts',(-8.98433281977287,1.0719340584143,-4.00815495993591));
#40243=CARTESIAN_POINT('Ctrl Pts',(-8.91817510253016,2.16059047448068,-3.29411075984077));
#40244=CARTESIAN_POINT('Ctrl Pts',(-8.85201738528746,3.249246890547,-2.58006655974566));
#40245=CARTESIAN_POINT('Ctrl Pts',(-8.78585966804475,3.94891488658736,-1.27295719760559));
#40246=CARTESIAN_POINT('Ctrl Pts',(-8.71970195080204,3.93935010902385,0.0289415799351118));
#40247=CARTESIAN_POINT('Ctrl Pts',(-8.65354423355933,3.92978533146034,1.33084035747585));
#40248=CARTESIAN_POINT('Ctrl Pts',(-8.58738651631661,3.21098778029283,2.62752855041718));
#40249=CARTESIAN_POINT('Ctrl Pts',(-8.5212287990739,2.1119575790511,3.32550027526747));
#40250=CARTESIAN_POINT('Ctrl Pts',(-8.45507108183119,1.01292737780934,4.02347200011778));
#40251=CARTESIAN_POINT('Ctrl Pts',(-8.38891336458848,-0.466335473506701,
4.12272725687701));
#40252=CARTESIAN_POINT('Ctrl Pts',(-8.32275564734577,-1.64875902323899,
3.57783601913271));
#40253=CARTESIAN_POINT('Ctrl Pts',(-8.25659793010306,-2.83118257297127,
3.0329447813884));
#40254=CARTESIAN_POINT('Ctrl Pts',(-8.19044021286035,-3.71676682111984,
1.84390704914054));
#40255=CARTESIAN_POINT('Ctrl Pts',(-8.12428249561764,-3.90017186834352,
0.554956118893427));
#40256=CARTESIAN_POINT('Ctrl Pts',(-8.1149095044234,-3.92615604621803,0.372342113717156));
#40257=CARTESIAN_POINT('Ctrl Pts',(-8.10553651322916,-3.93804592913002,
0.187722628912043));
#40258=CARTESIAN_POINT('Ctrl Pts',(-8.09616352203492,-3.93651676133011,
0.00290543094219859));
#40259=CARTESIAN_POINT('Origin',(-27.25,0.,0.));
#40260=CARTESIAN_POINT('',(-6.66283647796508,-3.92707662061414,0.0014756693134238));
#40261=CARTESIAN_POINT('',(-6.84616352203492,-3.92693618395205,0.00127148827395828));
#40262=CARTESIAN_POINT('',(-27.25,-3.933,-4.81653586104654E-16));
#40263=CARTESIAN_POINT('Ctrl Pts',(-6.66283647796508,-3.92707662061414,
0.0014756693134238));
#40264=CARTESIAN_POINT('Ctrl Pts',(-6.69125337156219,-3.92897796572974,
0.565237947566541));
#40265=CARTESIAN_POINT('Ctrl Pts',(-6.7196702651593,-3.81563262730524,1.12827119920084));
#40266=CARTESIAN_POINT('Ctrl Pts',(-6.74808715875641,-3.58326313671216,
1.63693101554719));
#40267=CARTESIAN_POINT('Ctrl Pts',(-6.81424487599912,-3.04228088606765,
2.82114814989274));
#40268=CARTESIAN_POINT('Ctrl Pts',(-6.88040259324183,-1.85617505344194,
3.71065547367904));
#40269=CARTESIAN_POINT('Ctrl Pts',(-6.94656031048454,-0.567836978435915,
3.8983174604557));
#40270=CARTESIAN_POINT('Ctrl Pts',(-7.01271802772725,0.720501096570151,
4.08597944723238));
#40271=CARTESIAN_POINT('Ctrl Pts',(-7.07887574496995,2.11107141395647,3.57179609699945));
#40272=CARTESIAN_POINT('Ctrl Pts',(-7.14503346221267,2.96739739495242,2.59111376766883));
#40273=CARTESIAN_POINT('Ctrl Pts',(-7.21119117945538,3.82372337594836,1.61043143833821));
#40274=CARTESIAN_POINT('Ctrl Pts',(-7.27734889669809,4.14580502055382,0.1632501299099));
#40275=CARTESIAN_POINT('Ctrl Pts',(-7.3435066139408,3.78622265449433,-1.0880422175491));
#40276=CARTESIAN_POINT('Ctrl Pts',(-7.40966433118351,3.42664028843486,-2.33933456500806));
#40277=CARTESIAN_POINT('Ctrl Pts',(-7.47582204842623,2.38539391171046,-3.39473795149777));
#40278=CARTESIAN_POINT('Ctrl Pts',(-7.54197976566894,1.13907138415888,-3.77118472609928));
#40279=CARTESIAN_POINT('Ctrl Pts',(-7.60813748291165,-0.1072511433927,-4.14763150070078));
#40280=CARTESIAN_POINT('Ctrl Pts',(-7.67429520015435,-1.5586498217715,-3.84512166341409));
#40281=CARTESIAN_POINT('Ctrl Pts',(-7.74045291739706,-2.5508063826392,-3.00211669574342));
#40282=CARTESIAN_POINT('Ctrl Pts',(-7.79791410425306,-3.41254248706492,
-2.26992598562329));
#40283=CARTESIAN_POINT('Ctrl Pts',(-7.85537529110907,-3.92783712225298,
-1.12999844138859));
#40284=CARTESIAN_POINT('Ctrl Pts',(-7.91283647796508,-3.93687099541924,
0.00275879756119139));
#40285=CARTESIAN_POINT('Ctrl Pts',(-8.09616352203492,-3.93651676133011,
0.00290543094219859));
#40286=CARTESIAN_POINT('Ctrl Pts',(-8.03937879598645,-3.92725254963928,
-1.1167791754208));
#40287=CARTESIAN_POINT('Ctrl Pts',(-7.98259406993798,-3.42546314938591,
-2.24372053308702));
#40288=CARTESIAN_POINT('Ctrl Pts',(-7.92580934388951,-2.58129701731398,
-2.97594062523454));
#40289=CARTESIAN_POINT('Ctrl Pts',(-7.8596516266468,-1.59779127276193,-3.82902231086908));
#40290=CARTESIAN_POINT('Ctrl Pts',(-7.79349390940409,-0.149553937359015,
-4.1463215538918));
#40291=CARTESIAN_POINT('Ctrl Pts',(-7.72733619216138,1.10054369575526,-3.78260762837605));
#40292=CARTESIAN_POINT('Ctrl Pts',(-7.66117847491867,2.35064132886953,-3.4188937028603));
#40293=CARTESIAN_POINT('Ctrl Pts',(-7.59502075767596,3.40259925969511,-2.3741666088061));
#40294=CARTESIAN_POINT('Ctrl Pts',(-7.52886304043325,3.77492685345232,-1.12660736177254));
#40295=CARTESIAN_POINT('Ctrl Pts',(-7.46270532319054,4.14725444720951,0.120951885260985));
#40296=CARTESIAN_POINT('Ctrl Pts',(-7.39654760594783,3.83995170389831,1.57134328527392));
#40297=CARTESIAN_POINT('Ctrl Pts',(-7.33038988870512,2.99367386134789,2.56070961032244));
#40298=CARTESIAN_POINT('Ctrl Pts',(-7.26423217146242,2.14739601879745,3.55007593537099));
#40299=CARTESIAN_POINT('Ctrl Pts',(-7.19807445421971,0.762143077007797,
4.07841718545519));
#40300=CARTESIAN_POINT('Ctrl Pts',(-7.131916736977,-0.528042196028415,3.90390680418073));
#40301=CARTESIAN_POINT('Ctrl Pts',(-7.06575901973429,-1.81822746906463,
3.72939642290628));
#40302=CARTESIAN_POINT('Ctrl Pts',(-6.99960130249158,-3.01334507334736,
2.85203441027317));
#40303=CARTESIAN_POINT('Ctrl Pts',(-6.93344358524887,-3.56637890009438,
1.67339727425315));
#40304=CARTESIAN_POINT('Ctrl Pts',(-6.90435023084422,-3.80957969041612,
1.15508271713341));
#40305=CARTESIAN_POINT('Ctrl Pts',(-6.87525687643957,-3.92861002670579,
0.578505562252523));
#40306=CARTESIAN_POINT('Ctrl Pts',(-6.84616352203492,-3.92693618395205,
0.00127148827395828));
#40307=CARTESIAN_POINT('Origin',(-27.25,0.,0.));
#40308=CARTESIAN_POINT('',(-5.41283647796509,-3.93146821322483,-0.00353098110087657));
#40309=CARTESIAN_POINT('',(-5.59616352203493,-3.9318578232019,-0.00356758979283532));
#40310=CARTESIAN_POINT('',(-27.25,-3.933,-4.81653586104654E-16));
#40311=CARTESIAN_POINT('Ctrl Pts',(-5.41283647796509,-3.93146821322483,
-0.00353098110087657));
#40312=CARTESIAN_POINT('Ctrl Pts',(-5.46097373477261,-3.9231618876001,0.948778731502717));
#40313=CARTESIAN_POINT('Ctrl Pts',(-5.50911099158013,-3.57517179997445,
1.90652852351159));
#40314=CARTESIAN_POINT('Ctrl Pts',(-5.55724824838764,-2.94634760568305,
2.61502459708094));
#40315=CARTESIAN_POINT('Ctrl Pts',(-5.62340596563035,-2.0821194381401,3.58875027260494));
#40316=CARTESIAN_POINT('Ctrl Pts',(-5.68956368287305,-0.687436696378754,
4.09167211074258));
#40317=CARTESIAN_POINT('Ctrl Pts',(-5.75572140011577,0.599341746962865,
3.89359824929388));
#40318=CARTESIAN_POINT('Ctrl Pts',(-5.82187911735848,1.88612019030448,3.69552438784518));
#40319=CARTESIAN_POINT('Ctrl Pts',(-5.88803683460119,3.06499433522633,2.79645482681015));
#40320=CARTESIAN_POINT('Ctrl Pts',(-5.95419455184391,3.59638285089867,1.60790181487245));
#40321=CARTESIAN_POINT('Ctrl Pts',(-6.02035226908662,4.127771366571,0.419348802934788));
#40322=CARTESIAN_POINT('Ctrl Pts',(-6.08650998632932,4.01167425299381,-1.0586876599056));
#40323=CARTESIAN_POINT('Ctrl Pts',(-6.15266770357203,3.30123020634185,-2.1496969510498));
#40324=CARTESIAN_POINT('Ctrl Pts',(-6.21882542081474,2.59078615968987,-3.24070624219403));
#40325=CARTESIAN_POINT('Ctrl Pts',(-6.28498313805745,1.28599517996311,-3.94468836164213));
#40326=CARTESIAN_POINT('Ctrl Pts',(-6.35114085530016,-0.0159281307202408,
-3.93942434261913));
#40327=CARTESIAN_POINT('Ctrl Pts',(-6.41729857254287,-1.31785144140355,
-3.93416032359614));
#40328=CARTESIAN_POINT('Ctrl Pts',(-6.48345628978557,-2.61690708304341,
-3.21965016610209));
#40329=CARTESIAN_POINT('Ctrl Pts',(-6.54961400702828,-3.31850556953169,
-2.12293161490267));
#40330=CARTESIAN_POINT('Ctrl Pts',(-6.58735483067388,-3.71874466259825,
-1.49728938970574));
#40331=CARTESIAN_POINT('Ctrl Pts',(-6.62509565431948,-3.92455142093134,
-0.747263901705643));
#40332=CARTESIAN_POINT('Ctrl Pts',(-6.66283647796508,-3.92707662061414,
0.0014756693134238));
#40333=CARTESIAN_POINT('Ctrl Pts',(-6.84616352203492,-3.92693618395205,
0.00127148827395828));
#40334=CARTESIAN_POINT('Ctrl Pts',(-6.80909915919686,-3.92480374111665,
-0.734113399383333));
#40335=CARTESIAN_POINT('Ctrl Pts',(-6.77203479635879,-3.72676527488361,
-1.47056448382967));
#40336=CARTESIAN_POINT('Ctrl Pts',(-6.73497043352073,-3.33998801353544,
-2.08897031236778));
#40337=CARTESIAN_POINT('Ctrl Pts',(-6.66881271627802,-2.64961325101818,
-3.19278850356176));
#40338=CARTESIAN_POINT('Ctrl Pts',(-6.60265499903531,-1.35791367677233,
-3.92051262654278));
#40339=CARTESIAN_POINT('Ctrl Pts',(-6.5364972817926,-0.0561118385083373,
-3.93905678533495));
#40340=CARTESIAN_POINT('Ctrl Pts',(-6.47033956454989,1.24568999975573,-3.95760094412711));
#40341=CARTESIAN_POINT('Ctrl Pts',(-6.40418184730719,2.55759410203788,-3.26696513873041));
#40342=CARTESIAN_POINT('Ctrl Pts',(-6.33802413006447,3.27913012587421,-2.18325960758356));
#40343=CARTESIAN_POINT('Ctrl Pts',(-6.27186641282177,4.00066614971047,-1.09955407643679));
#40344=CARTESIAN_POINT('Ctrl Pts',(-6.20570869557906,4.13183409510091,0.377221180460019));
#40345=CARTESIAN_POINT('Ctrl Pts',(-6.13955097833635,3.61259721016315,1.57113280585333));
#40346=CARTESIAN_POINT('Ctrl Pts',(-6.07339326109364,3.09336032522536,2.76504443124672));
#40347=CARTESIAN_POINT('Ctrl Pts',(-6.00723554385092,1.92371860995926,3.6760924251366));
#40348=CARTESIAN_POINT('Ctrl Pts',(-5.94107782660821,0.639027628913517,
3.8872819020486));
#40349=CARTESIAN_POINT('Ctrl Pts',(-5.8749201093655,-0.645663352132228,
4.09847137896061));
#40350=CARTESIAN_POINT('Ctrl Pts',(-5.80876239212279,-2.04540359895766,
3.60980233889474));
#40351=CARTESIAN_POINT('Ctrl Pts',(-5.74260467488008,-2.91951937334548,
2.64494300982427));
#40352=CARTESIAN_POINT('Ctrl Pts',(-5.69379095726503,-3.56447573448,1.93303255114411));
#40353=CARTESIAN_POINT('Ctrl Pts',(-5.64497723964998,-3.92327908267579,
0.961881335847518));
#40354=CARTESIAN_POINT('Ctrl Pts',(-5.59616352203493,-3.9318578232019,-0.00356758979283532));
#40355=CARTESIAN_POINT('Origin',(-27.25,0.,0.));
#40356=CARTESIAN_POINT('',(-4.16283647796509,-3.93933553009238,0.000621493119071417));
#40357=CARTESIAN_POINT('',(-4.34616352203494,-3.93922419965025,0.000863830554008869));
#40358=CARTESIAN_POINT('',(-27.25,-3.933,-4.81653586104654E-16));
#40359=CARTESIAN_POINT('Ctrl Pts',(-4.16283647796509,-3.93933553009238,
0.000621493119071417));
#40360=CARTESIAN_POINT('Ctrl Pts',(-4.1645363807403,-3.93940906456347,0.0340770639088575));
#40361=CARTESIAN_POINT('Ctrl Pts',(-4.16623628351551,-3.93901973837612,
0.0675308795071106));
#40362=CARTESIAN_POINT('Ctrl Pts',(-4.16793618629071,-3.93816230537414,
0.100972693060727));
#40363=CARTESIAN_POINT('Ctrl Pts',(-4.23409390353343,-3.90479227331878,
1.40247891884733));
#40364=CARTESIAN_POINT('Ctrl Pts',(-4.30025162077614,-3.16240332696561,
2.68580622394492));
#40365=CARTESIAN_POINT('Ctrl Pts',(-4.36640933801885,-2.05079357198834,
3.36356412049544));
#40366=CARTESIAN_POINT('Ctrl Pts',(-4.43256705526156,-0.939183817011137,
4.04132201704592));
#40367=CARTESIAN_POINT('Ctrl Pts',(-4.49872477250427,0.541646746590158,
4.11351050504943));
#40368=CARTESIAN_POINT('Ctrl Pts',(-4.56488248974698,1.71390860469547,3.54708826403145));
#40369=CARTESIAN_POINT('Ctrl Pts',(-4.63104020698969,2.88617046280078,2.98066602301347));
#40370=CARTESIAN_POINT('Ctrl Pts',(-4.69719792423241,3.74986361541014,1.77563305297397));
#40371=CARTESIAN_POINT('Ctrl Pts',(-4.76335564147512,3.90966791844257,0.483543814157597));
#40372=CARTESIAN_POINT('Ctrl Pts',(-4.82951335871783,4.069472221475,-0.808545424658813));
#40373=CARTESIAN_POINT('Ctrl Pts',(-4.89567107596053,3.52538767493053,-2.18769093225205));
#40374=CARTESIAN_POINT('Ctrl Pts',(-4.96182879320324,2.52644668226425,-3.02264536789066));
#40375=CARTESIAN_POINT('Ctrl Pts',(-5.02798651044595,1.527505689598,-3.85759980352923));
#40376=CARTESIAN_POINT('Ctrl Pts',(-5.09414422768866,0.0737082508099615,
-4.14836316721312));
#40377=CARTESIAN_POINT('Ctrl Pts',(-5.16030194493137,-1.16952943056686,
-3.76185044461622));
#40378=CARTESIAN_POINT('Ctrl Pts',(-5.22645966217409,-2.41276711194375,
-3.3753377220193));
#40379=CARTESIAN_POINT('Ctrl Pts',(-5.2926173794168,-3.44544503590944,-2.3115489131415));
#40380=CARTESIAN_POINT('Ctrl Pts',(-5.35877509665951,-3.79489720122999,
-1.05738975224741));
#40381=CARTESIAN_POINT('Ctrl Pts',(-5.37679555709471,-3.89008320796671,
-0.715773891237398));
#40382=CARTESIAN_POINT('Ctrl Pts',(-5.3948160175299,-3.93457773425301,-0.360033628658111));
#40383=CARTESIAN_POINT('Ctrl Pts',(-5.41283647796509,-3.93146821322483,
-0.00353098110087657));
#40384=CARTESIAN_POINT('Ctrl Pts',(-5.59616352203493,-3.9318578232019,-0.00356758979283532));
#40385=CARTESIAN_POINT('Ctrl Pts',(-5.57881952240727,-3.93490593508029,
-0.34660120052666));
#40386=CARTESIAN_POINT('Ctrl Pts',(-5.56147552277961,-3.89373988480933,
-0.688914924782032));
#40387=CARTESIAN_POINT('Ctrl Pts',(-5.54413152315195,-3.80548566654496,
-1.01862443430826));
#40388=CARTESIAN_POINT('Ctrl Pts',(-5.47797380590924,-3.46884488340641,
-2.27628293129547));
#40389=CARTESIAN_POINT('Ctrl Pts',(-5.41181608866654,-2.44707201517901,
-3.35055030719482));
#40390=CARTESIAN_POINT('Ctrl Pts',(-5.34565837142382,-1.20784172112326,
-3.74972469298905));
#40391=CARTESIAN_POINT('Ctrl Pts',(-5.27950065418112,0.0313885729323832,
-4.14889907878324));
#40392=CARTESIAN_POINT('Ctrl Pts',(-5.21334293693841,1.48807629281634,-3.87298047447244));
#40393=CARTESIAN_POINT('Ctrl Pts',(-5.1471852196957,2.49548232805611,-3.04825931428975));
#40394=CARTESIAN_POINT('Ctrl Pts',(-5.08102750245299,3.50288836329594,-2.22353815410701));
#40395=CARTESIAN_POINT('Ctrl Pts',(-5.01486978521028,4.06101271389155,-0.850014438052321));
#40396=CARTESIAN_POINT('Ctrl Pts',(-4.94871206796757,3.91439682990473,0.443637638205326));
#40397=CARTESIAN_POINT('Ctrl Pts',(-4.88255435072487,3.76778094591791,1.73728971446297));
#40398=CARTESIAN_POINT('Ctrl Pts',(-4.81639663348215,2.91642482734867,2.95107015092358));
#40399=CARTESIAN_POINT('Ctrl Pts',(-4.75023891623944,1.7500018493998,3.52942069236006));
#40400=CARTESIAN_POINT('Ctrl Pts',(-4.68408119899673,0.583578871450859,
4.10777123379658));
#40401=CARTESIAN_POINT('Ctrl Pts',(-4.61792348175402,-0.897910965877739,
4.05069188020889));
#40402=CARTESIAN_POINT('Ctrl Pts',(-4.5517657645113,-2.01637639847237,3.384308366267));
#40403=CARTESIAN_POINT('Ctrl Pts',(-4.48560804726859,-3.13484183106693,
2.71792485232515));
#40404=CARTESIAN_POINT('Ctrl Pts',(-4.41945033002589,-3.89028285892757,
1.44223717802918));
#40405=CARTESIAN_POINT('Ctrl Pts',(-4.35329261278318,-3.93692731033631,
0.141139100778367));
#40406=CARTESIAN_POINT('Ctrl Pts',(-4.35091624920043,-3.93860276378731,
0.0944040830477024));
#40407=CARTESIAN_POINT('Ctrl Pts',(-4.34853988561769,-3.93936371164798,
0.0476362802326757));
#40408=CARTESIAN_POINT('Ctrl Pts',(-4.34616352203494,-3.93922419965025,
0.000863830554008869));
#40409=CARTESIAN_POINT('Origin',(-27.25,0.,0.));
#40410=CARTESIAN_POINT('',(-2.91283647796509,-3.92964797513088,0.00314259250936713));
#40411=CARTESIAN_POINT('',(-3.09616352203493,-3.9293213278247,0.00302737416568081));
#40412=CARTESIAN_POINT('',(-27.25,-3.933,-4.81653586104654E-16));
#40413=CARTESIAN_POINT('Ctrl Pts',(-2.91283647796509,-3.92964797513088,
0.00314259250936713));
#40414=CARTESIAN_POINT('Ctrl Pts',(-2.93425674395071,-3.93282742473341,
0.427401276174971));
#40415=CARTESIAN_POINT('Ctrl Pts',(-2.95567700993633,-3.86952908002031,
0.850736746834505));
#40416=CARTESIAN_POINT('Ctrl Pts',(-2.97709727592195,-3.7357245118254,1.25047143256818));
#40417=CARTESIAN_POINT('Ctrl Pts',(-3.04325499316466,-3.32246144616761,
2.48507488374048));
#40418=CARTESIAN_POINT('Ctrl Pts',(-3.10941271040737,-2.23662642002933,
3.49454606427628));
#40419=CARTESIAN_POINT('Ctrl Pts',(-3.17557042765008,-0.97521532047094,
3.81684074856203));
#40420=CARTESIAN_POINT('Ctrl Pts',(-3.24172814489279,0.286195779087454,
4.13913543284778));
#40421=CARTESIAN_POINT('Ctrl Pts',(-3.3078858621355,1.72318295206596,3.77425362088349));
#40422=CARTESIAN_POINT('Ctrl Pts',(-3.37404357937821,2.67802389252845,2.88920509315637));
#40423=CARTESIAN_POINT('Ctrl Pts',(-3.44020129662092,3.63286483299093,2.00415656542924));
#40424=CARTESIAN_POINT('Ctrl Pts',(-3.50635901386363,4.10555954093739,0.598941321939292));
#40425=CARTESIAN_POINT('Ctrl Pts',(-3.57251673110634,3.87975154828102,-0.683260987411258));
#40426=CARTESIAN_POINT('Ctrl Pts',(-3.63867444834905,3.65394355562464,-1.96546329676181));
#40427=CARTESIAN_POINT('Ctrl Pts',(-3.70483216559175,2.72963286236543,-3.12465267197295));
#40428=CARTESIAN_POINT('Ctrl Pts',(-3.77098988283446,1.52988472539395,-3.63025765599397));
#40429=CARTESIAN_POINT('Ctrl Pts',(-3.83714760007717,0.330136588422467,
-4.13586264001499));
#40430=CARTESIAN_POINT('Ctrl Pts',(-3.90330531731989,-1.14504899226128,
-3.98788323284587));
#40431=CARTESIAN_POINT('Ctrl Pts',(-3.9694630345626,-2.22046622372429,-3.25405095602352));
#40432=CARTESIAN_POINT('Ctrl Pts',(-4.0339208490301,-3.26825093078253,-2.53907428026934));
#40433=CARTESIAN_POINT('Ctrl Pts',(-4.09837866349759,-3.93654721104028,
-1.26796457328689));
#40434=CARTESIAN_POINT('Ctrl Pts',(-4.16283647796509,-3.93933553009238,
0.000621493119071417));
#40435=CARTESIAN_POINT('Ctrl Pts',(-4.34616352203494,-3.93922419965025,
0.000863830554008869));
#40436=CARTESIAN_POINT('Ctrl Pts',(-4.28238216837498,-3.93547971200863,
-1.2545038985929));
#40437=CARTESIAN_POINT('Ctrl Pts',(-4.21860081471501,-3.28306189041179,
-2.51321913568449));
#40438=CARTESIAN_POINT('Ctrl Pts',(-4.15481946105504,-2.25354393302045,
-3.23123144326866));
#40439=CARTESIAN_POINT('Ctrl Pts',(-4.08866174381234,-1.1856682293391,-3.9759954298592));
#40440=CARTESIAN_POINT('Ctrl Pts',(-4.02250402656963,0.287931052980419,
-4.13901492283474));
#40441=CARTESIAN_POINT('Ctrl Pts',(-3.95634630932692,1.49277422283225,-3.64567442693553));
#40442=CARTESIAN_POINT('Ctrl Pts',(-3.89018859208421,2.69761739268421,-3.15233393103625));
#40443=CARTESIAN_POINT('Ctrl Pts',(-3.8240308748415,3.63370445006837,-2.00263344626206));
#40444=CARTESIAN_POINT('Ctrl Pts',(-3.75787315759879,3.87257991587189,-0.722801261257757));
#40445=CARTESIAN_POINT('Ctrl Pts',(-3.69171544035608,4.11145538167539,0.557030923746436));
#40446=CARTESIAN_POINT('Ctrl Pts',(-3.62555772311337,3.65311925589831,1.96699480898077));
#40447=CARTESIAN_POINT('Ctrl Pts',(-3.55940000587066,2.70735609581649,2.86173721461466));
#40448=CARTESIAN_POINT('Ctrl Pts',(-3.49324228862795,1.76159293573465,3.75647962024858));
#40449=CARTESIAN_POINT('Ctrl Pts',(-3.42708457138524,0.328402741348056,
4.13600054628211));
#40450=CARTESIAN_POINT('Ctrl Pts',(-3.36092685414253,-0.936230363935897,
3.82658982223686));
#40451=CARTESIAN_POINT('Ctrl Pts',(-3.29476913689982,-2.20086346921985,
3.51717909819162));
#40452=CARTESIAN_POINT('Ctrl Pts',(-3.22861141965711,-3.29693948540113,
2.51883672406761));
#40453=CARTESIAN_POINT('Ctrl Pts',(-3.16245370241439,-3.722774613227,1.28851304686882));
#40454=CARTESIAN_POINT('Ctrl Pts',(-3.14035697562124,-3.86500386282424,
0.877584023086522));
#40455=CARTESIAN_POINT('Ctrl Pts',(-3.11826024882808,-3.93246338668909,
0.440775977735576));
#40456=CARTESIAN_POINT('Ctrl Pts',(-3.09616352203493,-3.9293213278247,0.00302737416568081));
#40457=CARTESIAN_POINT('Origin',(-27.25,0.,0.));
#40458=CARTESIAN_POINT('',(-1.66283647796509,-3.92810494057017,-0.00240077655339843));
#40459=CARTESIAN_POINT('',(-1.84616352203496,-3.92834846924785,-0.00256498101517192));
#40460=CARTESIAN_POINT('',(-27.25,-3.933,-4.81653586104654E-16));
#40461=CARTESIAN_POINT('Ctrl Pts',(-1.66283647796509,-3.92810494057017,
-0.00240077655339843));
#40462=CARTESIAN_POINT('Ctrl Pts',(-1.70397710716111,-3.92354275555459,
0.813259782426832));
#40463=CARTESIAN_POINT('Ctrl Pts',(-1.74511773635714,-3.67602106528321,
1.63145161923944));
#40464=CARTESIAN_POINT('Ctrl Pts',(-1.78625836555316,-3.20534629633937,
2.29019815317242));
#40465=CARTESIAN_POINT('Ctrl Pts',(-1.85241608279587,-2.44846024754571,
3.34951999093285));
#40466=CARTESIAN_POINT('Ctrl Pts',(-1.91857380003859,-1.11451276938518,
3.99652515830297));
#40467=CARTESIAN_POINT('Ctrl Pts',(-1.9847315172813,0.185965708862303,3.93506573455426));
#40468=CARTESIAN_POINT('Ctrl Pts',(-2.05088923452401,1.48644418710979,3.87360631080555));
#40469=CARTESIAN_POINT('Ctrl Pts',(-2.11704695176672,2.75345366544434,3.10368229593785));
#40470=CARTESIAN_POINT('Ctrl Pts',(-2.18320466900943,3.40705712250568,1.97769894516902));
#40471=CARTESIAN_POINT('Ctrl Pts',(-2.24936238625214,4.06066057956705,0.851715594400124));
#40472=CARTESIAN_POINT('Ctrl Pts',(-2.31552010349485,4.10085801535535,-0.630327092269794));
#40473=CARTESIAN_POINT('Ctrl Pts',(-2.38167782073757,3.50925872819166,-1.79008694485165));
#40474=CARTESIAN_POINT('Ctrl Pts',(-2.44783553798027,2.91765944102804,-2.94984679743337));
#40475=CARTESIAN_POINT('Ctrl Pts',(-2.51399325522299,1.69426343091233,-3.78732381592697));
#40476=CARTESIAN_POINT('Ctrl Pts',(-2.58015097246569,0.399025891082152,
-3.91919609647393));
#40477=CARTESIAN_POINT('Ctrl Pts',(-2.6463086897084,-0.896211648748102,
-4.0510683770209));
#40478=CARTESIAN_POINT('Ctrl Pts',(-2.71246640695111,-2.26329071829293,
-3.47733591962131));
#40479=CARTESIAN_POINT('Ctrl Pts',(-2.77862412419382,-3.07648470047672,
-2.4606018300171));
#40480=CARTESIAN_POINT('Ctrl Pts',(-2.82336157545091,-3.62638617315059,
-1.77306160537151));
#40481=CARTESIAN_POINT('Ctrl Pts',(-2.868099026708,-3.92300751269621,-0.882945945963138));
#40482=CARTESIAN_POINT('Ctrl Pts',(-2.91283647796509,-3.92964797513088,
0.00314259250936713));
#40483=CARTESIAN_POINT('Ctrl Pts',(-3.09616352203493,-3.9293213278247,0.00302737416568081));
#40484=CARTESIAN_POINT('Ctrl Pts',(-3.05210253158537,-3.92305604578036,
-0.869845663626177));
#40485=CARTESIAN_POINT('Ctrl Pts',(-3.00804154113582,-3.63607483546347,
-1.74645841465561));
#40486=CARTESIAN_POINT('Ctrl Pts',(-2.96398055068627,-3.10142389777848,
-2.42909178207749));
#40487=CARTESIAN_POINT('Ctrl Pts',(-2.89782283344356,-2.29864381503363,
-3.45406795355147));
#40488=CARTESIAN_POINT('Ctrl Pts',(-2.83166511620085,-0.937489410073432,
-4.04171531622592));
#40489=CARTESIAN_POINT('Ctrl Pts',(-2.76550739895814,0.359026369870962,
-3.92306223857118));
#40490=CARTESIAN_POINT('Ctrl Pts',(-2.69934968171543,1.65554214981543,-3.80440916091644));
#40491=CARTESIAN_POINT('Ctrl Pts',(-2.63319196447272,2.88741930474417,-2.97945564293242));
#40492=CARTESIAN_POINT('Ctrl Pts',(-2.56703424723,3.49081711581239,-1.82579060500368));
#40493=CARTESIAN_POINT('Ctrl Pts',(-2.50087652998729,4.09421492688058,-0.672125567075004));
#40494=CARTESIAN_POINT('Ctrl Pts',(-2.43471881274459,4.06913339408844,0.8102509907982));
#40495=CARTESIAN_POINT('Ctrl Pts',(-2.36856109550188,3.42705147522404,1.94284242960063));
#40496=CARTESIAN_POINT('Ctrl Pts',(-2.30240337825917,2.78496955635964,3.07543386840307));
#40497=CARTESIAN_POINT('Ctrl Pts',(-2.23624566101646,1.52588725142289,3.85824018813459));
#40498=CARTESIAN_POINT('Ctrl Pts',(-2.17008794377375,0.226099966689285,
3.93296294841805));
#40499=CARTESIAN_POINT('Ctrl Pts',(-2.10393022653105,-1.07368731804432,
4.00768570870152));
#40500=CARTESIAN_POINT('Ctrl Pts',(-2.03777250928834,-2.41417958257486,
3.37432490953694));
#40501=CARTESIAN_POINT('Ctrl Pts',(-1.97161479204563,-3.18182539675517,
2.32277727332773));
#40502=CARTESIAN_POINT('Ctrl Pts',(-1.92979770204207,-3.66704035640476,
1.65811313467455));
#40503=CARTESIAN_POINT('Ctrl Pts',(-1.88798061203852,-3.92338745106363,
0.826371887481848));
#40504=CARTESIAN_POINT('Ctrl Pts',(-1.84616352203496,-3.92834846924785,
-0.00256498101517192));
#40505=CARTESIAN_POINT('Origin',(-27.25,0.,0.));
#40506=CARTESIAN_POINT('',(-0.41283647796511,-3.93929521061115,-0.00160796147817999));
#40507=CARTESIAN_POINT('',(-0.596163522034944,-3.93875600852084,-0.00157175874070594));
#40508=CARTESIAN_POINT('',(-27.25,-3.933,-4.81653586104654E-16));
#40509=CARTESIAN_POINT('Ctrl Pts',(-0.41283647796511,-3.93929521061115,
-0.00160796147817999));
#40510=CARTESIAN_POINT('Ctrl Pts',(-0.473697470371537,-3.93274620403603,
1.19707520163202));
#40511=CARTESIAN_POINT('Ctrl Pts',(-0.534558462777964,-3.34481231109049,
2.40115562852338));
#40512=CARTESIAN_POINT('Ctrl Pts',(-0.59541945518439,-2.39319605116334,
3.12878034020633));
#40513=CARTESIAN_POINT('Ctrl Pts',(-0.661577172427097,-1.35876074279041,
3.91973014287904));
#40514=CARTESIAN_POINT('Ctrl Pts',(-0.727734889669808,0.105414000682263,
4.14768369252194));
#40515=CARTESIAN_POINT('Ctrl Pts',(-0.793892606912517,1.33061187712945,
3.70791565939382));
#40516=CARTESIAN_POINT('Ctrl Pts',(-0.860050324155229,2.55580975357671,
3.26814762626567));
#40517=CARTESIAN_POINT('Ctrl Pts',(-0.926208041397931,3.54203076299841,
2.16065801036661));
#40518=CARTESIAN_POINT('Ctrl Pts',(-0.992365758640646,3.83711969094379,
0.892555614996963));
#40519=CARTESIAN_POINT('Ctrl Pts',(-1.05852347588335,4.13220861888915,-0.375546780372539));
#40520=CARTESIAN_POINT('Ctrl Pts',(-1.12468119312606,3.73616546535818,-1.80426195521246));
#40521=CARTESIAN_POINT('Ctrl Pts',(-1.19083891036877,2.83065587439165,-2.73975879600272));
#40522=CARTESIAN_POINT('Ctrl Pts',(-1.25699662761148,1.92514628342501,-3.67525563679308));
#40523=CARTESIAN_POINT('Ctrl Pts',(-1.32315434485419,0.510170255022601,
-4.1175341435337));
#40524=CARTESIAN_POINT('Ctrl Pts',(-1.38931206209691,-0.76683039427974,
-3.86410473867316));
#40525=CARTESIAN_POINT('Ctrl Pts',(-1.45546977933961,-2.04383104358194,
-3.61067533381264));
#40526=CARTESIAN_POINT('Ctrl Pts',(-1.52162749658232,-3.18285631378417,
-2.66153801735112));
#40527=CARTESIAN_POINT('Ctrl Pts',(-1.58778521382502,-3.66245663917197,
-1.45115010504507));
#40528=CARTESIAN_POINT('Ctrl Pts',(-1.61280230187171,-3.84381422022983,
-0.993450198899252));
#40529=CARTESIAN_POINT('Ctrl Pts',(-1.6378193899184,-3.93087914666402,-0.498393483008929));
#40530=CARTESIAN_POINT('Ctrl Pts',(-1.66283647796509,-3.92810494057017,
-0.00240077655339843));
#40531=CARTESIAN_POINT('Ctrl Pts',(-1.84616352203496,-3.92834846924785,
-0.00256498101517192));
#40532=CARTESIAN_POINT('Ctrl Pts',(-1.8218228947958,-3.93123614733207,-0.485067310066915));
#40533=CARTESIAN_POINT('Ctrl Pts',(-1.79748226755664,-3.84895176851133,
-0.966619488238375));
#40534=CARTESIAN_POINT('Ctrl Pts',(-1.77314164031748,-3.67705446577845,
-1.41371880629667));
#40535=CARTESIAN_POINT('Ctrl Pts',(-1.70698392307477,-3.20983835679131,
-2.62893277645775));
#40536=CARTESIAN_POINT('Ctrl Pts',(-1.64082620583206,-2.08060677498703,
-3.589626243526));
#40537=CARTESIAN_POINT('Ctrl Pts',(-1.57466848858935,-0.806233729792193,
-3.85607466381471));
#40538=CARTESIAN_POINT('Ctrl Pts',(-1.50851077134664,0.468139315402641,
-4.12252308410342));
#40539=CARTESIAN_POINT('Ctrl Pts',(-1.44235305410394,1.88765382398794,-3.69472645761258));
#40540=CARTESIAN_POINT('Ctrl Pts',(-1.37619533686123,2.80261298269254,-2.76850354687877));
#40541=CARTESIAN_POINT('Ctrl Pts',(-1.31003761961852,3.71757214139709,-1.84228063614501));
#40542=CARTESIAN_POINT('Ctrl Pts',(-1.2438799023758,4.12797595022095,-0.41763144116817));
#40543=CARTESIAN_POINT('Ctrl Pts',(-1.17772218513309,3.84592575036428,0.853392939764376));
#40544=CARTESIAN_POINT('Ctrl Pts',(-1.11156446789038,3.5638755505076,2.124417320697));
#40545=CARTESIAN_POINT('Ctrl Pts',(-1.04540675064768,2.58937134197042,3.24181688758541));
#40546=CARTESIAN_POINT('Ctrl Pts',(-0.979249033404965,1.36855410729865,
3.69410247152038));
#40547=CARTESIAN_POINT('Ctrl Pts',(-0.913091316162255,0.147736872626877,
4.14638805545535));
#40548=CARTESIAN_POINT('Ctrl Pts',(-0.846933598919547,-1.3193933881794,
3.93355965643683));
#40549=CARTESIAN_POINT('Ctrl Pts',(-0.780775881676838,-2.36151226423397,
3.15311740810728));
#40550=CARTESIAN_POINT('Ctrl Pts',(-0.719238428462872,-3.33085256573394,
2.42717899389947));
#40551=CARTESIAN_POINT('Ctrl Pts',(-0.657700975248911,-3.93247174430637,
1.21013937735618));
#40552=CARTESIAN_POINT('Ctrl Pts',(-0.596163522034944,-3.93875600852084,
-0.00157175874070594));
#40553=CARTESIAN_POINT('Origin',(-56.8777734492732,0.,0.));
#40554=CARTESIAN_POINT('',(-0.00277344927320074,-3.2279083752853,-0.00131758399470729));
#40555=CARTESIAN_POINT('',(-8.88178419700125E-15,-3.22275,1.66140794472856E-12));
#40556=CARTESIAN_POINT('',(-56.8777734492732,-3.22275,1.66140794472856E-12));
#40557=CARTESIAN_POINT('',(0.,-3.22243683749934,-0.044926504729961));
#40558=CARTESIAN_POINT('Ctrl Pts',(-0.00277344927320076,-3.2279083752853,
-0.00131758399470763));
#40559=CARTESIAN_POINT('Ctrl Pts',(-0.00184896618213632,-3.22798989038041,
-0.01623752199351));
#40560=CARTESIAN_POINT('Ctrl Pts',(-0.000924483091071884,-3.2279614830524,
-0.0311564395318102));
#40561=CARTESIAN_POINT('Ctrl Pts',(-7.44426764155703E-15,-3.22782252806242,
-0.046072952734026));
#40562=CARTESIAN_POINT('Origin',(0.,0.,0.));
#40563=CARTESIAN_POINT('Origin',(-56.8777734492732,0.,0.));
#40564=CARTESIAN_POINT('',(-1.2527734492732,-3.21873892632151,-0.0019672267056687));
#40565=CARTESIAN_POINT('',(-1.00622655072698,-3.22746654626507,-0.00128791901194192));
#40566=CARTESIAN_POINT('',(-56.8777734492732,-3.22275,1.66140794472856E-12));
#40567=CARTESIAN_POINT('Ctrl Pts',(-1.2527734492732,-3.21873892632151,-0.00196722670566859));
#40568=CARTESIAN_POINT('Ctrl Pts',(-1.2277563612265,-3.22101214592218,-0.40838993067981));
#40569=CARTESIAN_POINT('Ctrl Pts',(-1.13658155593709,-2.96100577144116,
-1.88680273286147));
#40570=CARTESIAN_POINT('Ctrl Pts',(-0.979249033404971,-0.741409307439854,
-3.73636822239283));
#40571=CARTESIAN_POINT('Ctrl Pts',(-0.780775881676852,2.73693851524025,
-2.64914239661277));
#40572=CARTESIAN_POINT('Ctrl Pts',(-0.58230272994871,3.7105068394527,0.862979517739233));
#40573=CARTESIAN_POINT('Ctrl Pts',(-0.383829578220586,1.28614089123481,
3.58545256094235));
#40574=CARTESIAN_POINT('Ctrl Pts',(-0.190653151328746,-2.21709352745839,
3.04004312499088));
#40575=CARTESIAN_POINT('Ctrl Pts',(-0.0636344416796209,-3.22254203637332,
0.980898577691776));
#40576=CARTESIAN_POINT('Ctrl Pts',(-0.00277344927320076,-3.2279083752853,
-0.00131758399470763));
#40577=CARTESIAN_POINT('',(-8.88178419700125E-15,-1.09131022003147,3.03235215074946));
#40578=CARTESIAN_POINT('Origin',(0.,0.,0.));
#40579=CARTESIAN_POINT('Ctrl Pts',(-1.00622655072698,-3.22746654626507,
-0.00128791901194189));
#40580=CARTESIAN_POINT('Ctrl Pts',(-1.0016062866982,-3.22785316632397,-0.0758347258874285));
#40581=CARTESIAN_POINT('Ctrl Pts',(-0.930828305426712,-3.19164983838238,
-1.21744274340176));
#40582=CARTESIAN_POINT('Ctrl Pts',(-0.793892606912507,-1.8372343102454,
-3.33679471955611));
#40583=CARTESIAN_POINT('Ctrl Pts',(-0.59541945518438,1.80537864589007,-3.35297192389334));
#40584=CARTESIAN_POINT('Ctrl Pts',(-0.396946303456254,3.79975239553181,
-0.301770123854898));
#40585=CARTESIAN_POINT('Ctrl Pts',(-0.198473151728127,2.30693671058513,
3.02973452897375));
#40586=CARTESIAN_POINT('Ctrl Pts',(-0.0661577172427008,-0.082916802787829,
3.39526186154233));
#40587=CARTESIAN_POINT('Ctrl Pts',(8.88178419700125E-15,-1.09131022003164,
3.0323521507494));
#40588=CARTESIAN_POINT('Origin',(-56.8777734492732,0.,0.));
#40589=CARTESIAN_POINT('',(-2.50277344927319,-3.2200033083786,0.00257508009463239));
#40590=CARTESIAN_POINT('',(-2.25622655072698,-3.21893847680358,-0.00210177792008243));
#40591=CARTESIAN_POINT('',(-56.8777734492732,-3.22275,1.66140794472856E-12));
#40592=CARTESIAN_POINT('Ctrl Pts',(-2.50277344927319,-3.2200033083786,0.00257508009463239));
#40593=CARTESIAN_POINT('Ctrl Pts',(-2.45803599801609,-3.21456202937765,
-0.723497088062683));
#40594=CARTESIAN_POINT('Ctrl Pts',(-2.34714082951628,-2.61207673716788,
-2.53146408727085));
#40595=CARTESIAN_POINT('Ctrl Pts',(-2.17008794377376,0.385834726766185,
-3.78962036336862));
#40596=CARTESIAN_POINT('Ctrl Pts',(-1.97161479204564,3.39323327108378,-1.73090254387995));
#40597=CARTESIAN_POINT('Ctrl Pts',(-1.77314164031749,3.29441840747864,1.91231108576612));
#40598=CARTESIAN_POINT('Ctrl Pts',(-1.57466848858938,0.179807578872998,
3.80496754565549));
#40599=CARTESIAN_POINT('Ctrl Pts',(-1.40121242490793,-2.68602209988967,
2.41495284019006));
#40600=CARTESIAN_POINT('Ctrl Pts',(-1.29391407846921,-3.21500061415274,
0.666395363289895));
#40601=CARTESIAN_POINT('Ctrl Pts',(-1.2527734492732,-3.21873892632151,-0.00196722670566859));
#40602=CARTESIAN_POINT('Ctrl Pts',(-2.25622655072698,-3.21893847680358,
-0.00210177792008253));
#40603=CARTESIAN_POINT('Ctrl Pts',(-2.23188592348779,-3.22130467679004,
-0.397470295833488));
#40604=CARTESIAN_POINT('Ctrl Pts',(-2.14138757900589,-2.97061933829329,
-1.86455399408909));
#40605=CARTESIAN_POINT('Ctrl Pts',(-1.98473151728128,-0.779568879692582,
-3.72858958741861));
#40606=CARTESIAN_POINT('Ctrl Pts',(-1.78625836555316,2.7099356073734,-2.67696366978096));
#40607=CARTESIAN_POINT('Ctrl Pts',(-1.58778521382502,3.71880583993438,0.825163098419798));
#40608=CARTESIAN_POINT('Ctrl Pts',(-1.3893120620969,1.32324257672849,3.57199715958687));
#40609=CARTESIAN_POINT('Ctrl Pts',(-1.19545917439755,-2.19935562265448,
3.06099349809352));
#40610=CARTESIAN_POINT('Ctrl Pts',(-1.06776400394091,-3.22231714059518,
0.99160352870076));
#40611=CARTESIAN_POINT('Ctrl Pts',(-1.00622655072698,-3.22746654626507,
-0.00128791901194189));
#40612=CARTESIAN_POINT('Origin',(-56.8777734492732,0.,0.));
#40613=CARTESIAN_POINT('',(-3.75277344927319,-3.22794141357874,0.00050925933183513));
#40614=CARTESIAN_POINT('',(-3.50622655072697,-3.2197356494399,0.0024806687263787));
#40615=CARTESIAN_POINT('',(-56.8777734492732,-3.22275,1.66140794472856E-12));
#40616=CARTESIAN_POINT('Ctrl Pts',(-3.75277344927319,-3.22794141357874,
0.000509259331835047));
#40617=CARTESIAN_POINT('Ctrl Pts',(-3.68831563480568,-3.22565662964174,
-1.03898622643229));
#40618=CARTESIAN_POINT('Ctrl Pts',(-3.55770010309546,-2.1159939982431,-3.14958145779129));
#40619=CARTESIAN_POINT('Ctrl Pts',(-3.36092685414253,1.47930384451711,-3.51023441585637));
#40620=CARTESIAN_POINT('Ctrl Pts',(-3.16245370241441,3.75147950180274,-0.66067106043193));
#40621=CARTESIAN_POINT('Ctrl Pts',(-2.96398055068628,2.58948341482026,2.79368243000086));
#40622=CARTESIAN_POINT('Ctrl Pts',(-2.76550739895815,-0.942973039578199,
3.69064876067085));
#40623=CARTESIAN_POINT('Ctrl Pts',(-2.61177169848712,-3.0105454903401,1.76848309786626));
#40624=CARTESIAN_POINT('Ctrl Pts',(-2.5241937152588,-3.22260858964133,0.350218017491745));
#40625=CARTESIAN_POINT('Ctrl Pts',(-2.50277344927319,-3.2200033083786,0.00257508009463239));
#40626=CARTESIAN_POINT('Ctrl Pts',(-3.50622655072697,-3.2197356494399,0.00248066872637863));
#40627=CARTESIAN_POINT('Ctrl Pts',(-3.46216556027738,-3.21460179800166,
-0.712762550837853));
#40628=CARTESIAN_POINT('Ctrl Pts',(-3.35194685258509,-2.6263582225274,-2.50961126578718));
#40629=CARTESIAN_POINT('Ctrl Pts',(-3.17557042765007,0.347156461294124,
-3.7933583964979));
#40630=CARTESIAN_POINT('Ctrl Pts',(-2.97709727592195,3.37540367795816,-1.76542632168304));
#40631=CARTESIAN_POINT('Ctrl Pts',(-2.77862412419381,3.31374730129506,1.87860804283756));
#40632=CARTESIAN_POINT('Ctrl Pts',(-2.58015097246569,0.218623351459381,
3.80293227389407));
#40633=CARTESIAN_POINT('Ctrl Pts',(-2.40601844797674,-2.67249830937439,
2.43692429754177));
#40634=CARTESIAN_POINT('Ctrl Pts',(-2.29804364073051,-3.21487335568621,
0.677139588199134));
#40635=CARTESIAN_POINT('Ctrl Pts',(-2.25622655072698,-3.21893847680358,
-0.00210177792008253));
#40636=CARTESIAN_POINT('Origin',(-56.8777734492732,0.,0.));
#40637=CARTESIAN_POINT('',(-5.00277344927319,-3.2214948345208,-0.00289333062281008));
#40638=CARTESIAN_POINT('',(-4.75622655072696,-3.22785018800479,0.000707833695615633));
#40639=CARTESIAN_POINT('',(-56.8777734492732,-3.22275,1.66140794472856E-12));
#40640=CARTESIAN_POINT('Ctrl Pts',(-5.00277344927319,-3.2214948345208,-0.00289333062280996));
#40641=CARTESIAN_POINT('Ctrl Pts',(-4.98475298883799,-3.22404281542441,
-0.295016114100004));
#40642=CARTESIAN_POINT('Ctrl Pts',(-4.90057481116007,-3.05373173874959,
-1.65667814746345));
#40643=CARTESIAN_POINT('Ctrl Pts',(-4.75023891623944,-1.13086255544314,
-3.6374764880366));
#40644=CARTESIAN_POINT('Ctrl Pts',(-4.55176576451131,2.44291753292778,-2.92271094241356));
#40645=CARTESIAN_POINT('Ctrl Pts',(-4.35329261278319,3.78040683298627,0.467556932945782));
#40646=CARTESIAN_POINT('Ctrl Pts',(-4.15481946105505,1.65724351676092,3.42981475460483));
#40647=CARTESIAN_POINT('Ctrl Pts',(-3.95634630932692,-1.98299042591341,
3.25235827122354));
#40648=CARTESIAN_POINT('Ctrl Pts',(-3.8223309720663,-3.21526690679691,1.12218908818911));
#40649=CARTESIAN_POINT('Ctrl Pts',(-3.75447335204839,-3.22800166865545,
0.0279231776543737));
#40650=CARTESIAN_POINT('Ctrl Pts',(-3.75277344927319,-3.22794141357874,
0.000509259331835047));
#40651=CARTESIAN_POINT('Ctrl Pts',(-4.75622655072696,-3.22785018800479,
0.000707833695615589));
#40652=CARTESIAN_POINT('Ctrl Pts',(-4.69244519706697,-3.22478190741881,
-1.02795637914702));
#40653=CARTESIAN_POINT('Ctrl Pts',(-4.56250612616426,-2.1356649716347,-3.12919892137489));
#40654=CARTESIAN_POINT('Ctrl Pts',(-4.36640933801884,1.44342026140034,-3.52514147306206));
#40655=CARTESIAN_POINT('Ctrl Pts',(-4.16793618629072,3.74454502431787,-0.698904068557403));
#40656=CARTESIAN_POINT('Ctrl Pts',(-3.96946303456259,2.61784574945316,2.7671227133945));
#40657=CARTESIAN_POINT('Ctrl Pts',(-3.77098988283447,-0.905276827937616,
3.70007547035483));
#40658=CARTESIAN_POINT('Ctrl Pts',(-3.61657772155592,-3.00153291000458,
1.7907359329079));
#40659=CARTESIAN_POINT('Ctrl Pts',(-3.52832327752009,-3.22231029225817,
0.361177417303153));
#40660=CARTESIAN_POINT('Ctrl Pts',(-3.50622655072697,-3.2197356494399,0.00248066872637863));
#40661=CARTESIAN_POINT('Origin',(-56.8777734492732,0.,0.));
#40662=CARTESIAN_POINT('',(-6.25277344927318,-3.21789630792886,0.0012091821211443));
#40663=CARTESIAN_POINT('',(-6.00622655072697,-3.22181408586928,-0.00292332824735064));
#40664=CARTESIAN_POINT('',(-56.8777734492732,-3.22275,1.66140794472856E-12));
#40665=CARTESIAN_POINT('Ctrl Pts',(-6.25277344927318,-3.21789630792886,
0.00120918212114421));
#40666=CARTESIAN_POINT('Ctrl Pts',(-6.21503262562757,-3.21582712733459,
-0.612317502979839));
#40667=CARTESIAN_POINT('Ctrl Pts',(-6.11113408473924,-2.75156807830961,
-2.30422559493896));
#40668=CARTESIAN_POINT('Ctrl Pts',(-5.94107782660823,-0.0154015163207855,
-3.80917945408937));
#40669=CARTESIAN_POINT('Ctrl Pts',(-5.74260467488009,3.19208523418617,-2.07862386640746));
#40670=CARTESIAN_POINT('Ctrl Pts',(-5.54413152315197,3.47747956887825,1.55474151163881));
#40671=CARTESIAN_POINT('Ctrl Pts',(-5.34565837142383,0.57952636479995,3.76486845887453));
#40672=CARTESIAN_POINT('Ctrl Pts',(-5.16520568013092,-2.53764694845794,
2.64081745748553));
#40673=CARTESIAN_POINT('Ctrl Pts',(-5.0509107060807,-3.21468852612825,0.777441306115686));
#40674=CARTESIAN_POINT('Ctrl Pts',(-5.00277344927319,-3.2214948345208,-0.00289333062280996));
#40675=CARTESIAN_POINT('Ctrl Pts',(-6.00622655072697,-3.22181408586928,
-0.00292332824735106));
#40676=CARTESIAN_POINT('Ctrl Pts',(-5.98888255109927,-3.22431174733808,
-0.284009412405685));
#40677=CARTESIAN_POINT('Ctrl Pts',(-5.90538083422887,-3.06191100119738,
-1.63444269098198));
#40678=CARTESIAN_POINT('Ctrl Pts',(-5.75572140011576,-1.16790816827868,
-3.62575163696693));
#40679=CARTESIAN_POINT('Ctrl Pts',(-5.55724824838763,2.41297691887338,-2.94747804273184));
#40680=CARTESIAN_POINT('Ctrl Pts',(-5.35877509665951,3.78497939857008,0.428970131116378));
#40681=CARTESIAN_POINT('Ctrl Pts',(-5.16030194493137,1.69214344806,3.41273130701552));
#40682=CARTESIAN_POINT('Ctrl Pts',(-4.96182879320323,-1.94971114633403,
3.27241667179486));
#40683=CARTESIAN_POINT('Ctrl Pts',(-4.8271369951351,-3.20998195595637,1.14424004540375));
#40684=CARTESIAN_POINT('Ctrl Pts',(-4.75860291430968,-3.22796450590223,
0.0390337711987965));
#40685=CARTESIAN_POINT('Ctrl Pts',(-4.75622655072696,-3.22785018800479,
0.000707833695615589));
#40686=CARTESIAN_POINT('Origin',(-56.8777734492732,0.,0.));
#40687=CARTESIAN_POINT('',(-7.50277344927318,-3.22592194266142,0.00226059365463134));
#40688=CARTESIAN_POINT('',(-7.25622655072695,-3.21778123234973,0.00104187359324354));
#40689=CARTESIAN_POINT('',(-56.8777734492732,-3.22275,1.66140794472856E-12));
#40690=CARTESIAN_POINT('Ctrl Pts',(-7.50277344927318,-3.22592194266142,
0.00226059365463134));
#40691=CARTESIAN_POINT('Ctrl Pts',(-7.44531226241716,-3.21851947260152,
-0.925935031015119));
#40692=CARTESIAN_POINT('Ctrl Pts',(-7.32169335831845,-2.31013732855039,
-2.93544523349847));
#40693=CARTESIAN_POINT('Ctrl Pts',(-7.131916736977,1.10141150988432,-3.6465021604372));
#40694=CARTESIAN_POINT('Ctrl Pts',(-6.93344358524887,3.6610429062145,-1.05206946493042));
#40695=CARTESIAN_POINT('Ctrl Pts',(-6.73497043352074,2.86928957276539,2.50544660046798));
#40696=CARTESIAN_POINT('Ctrl Pts',(-6.5364972817926,-0.549063204013273,
3.76943164391853));
#40697=CARTESIAN_POINT('Ctrl Pts',(-6.3757649537101,-2.91035052847904,1.99860958833013));
#40698=CARTESIAN_POINT('Ctrl Pts',(-6.28119034287028,-3.2194542941915,0.463163131330338));
#40699=CARTESIAN_POINT('Ctrl Pts',(-6.25277344927318,-3.21789630792886,
0.00120918212114421));
#40700=CARTESIAN_POINT('Ctrl Pts',(-7.25622655072695,-3.21778123234973,
0.0010418735932435));
#40701=CARTESIAN_POINT('Ctrl Pts',(-7.21916218788886,-3.21603388168955,
-0.601541814863301));
#40702=CARTESIAN_POINT('Ctrl Pts',(-7.11594010780805,-2.76410687756682,
-2.28213517941486));
#40703=CARTESIAN_POINT('Ctrl Pts',(-6.94656031048453,-0.0542566740194617,
-3.80882404895191));
#40704=CARTESIAN_POINT('Ctrl Pts',(-6.74808715875641,3.17071582455421,-2.11107687744781));
#40705=CARTESIAN_POINT('Ctrl Pts',(-6.54961400702828,3.49315785049429,1.51918815623972));
#40706=CARTESIAN_POINT('Ctrl Pts',(-6.35114085530014,0.617900155701453,
3.75876094213507));
#40707=CARTESIAN_POINT('Ctrl Pts',(-6.17001170319971,-2.52230457329154,
2.66247123123546));
#40708=CARTESIAN_POINT('Ctrl Pts',(-6.05504026834198,-3.21478455725691,
0.788177746023009));
#40709=CARTESIAN_POINT('Ctrl Pts',(-6.00622655072697,-3.22181408586928,
-0.00292332824735106));
#40710=CARTESIAN_POINT('Origin',(-56.8777734492732,0.,0.));
#40711=CARTESIAN_POINT('',(-8.75277344927317,-3.22488322984771,-0.00262779420977039));
#40712=CARTESIAN_POINT('',(-8.50622655072697,-3.22563167876346,0.00238074690490087));
#40713=CARTESIAN_POINT('',(-56.8777734492732,-3.22275,1.66140794472856E-12));
#40714=CARTESIAN_POINT('Ctrl Pts',(-8.75277344927317,-3.22488322984771,
-0.0026277942097702));
#40715=CARTESIAN_POINT('Ctrl Pts',(-8.74174961644946,-3.22645652139871,
-0.180849833123689));
#40716=CARTESIAN_POINT('Ctrl Pts',(-8.66456806638304,-3.13193301652771,
-1.42697228178268));
#40717=CARTESIAN_POINT('Ctrl Pts',(-8.52122879907392,-1.50764057830064,
-3.49815740166747));
#40718=CARTESIAN_POINT('Ctrl Pts',(-8.32275564734576,2.12153960142961,-3.1637248678963));
#40719=CARTESIAN_POINT('Ctrl Pts',(-8.12428249561765,3.80862415267616,0.0668384906429997));
#40720=CARTESIAN_POINT('Ctrl Pts',(-7.92580934388952,2.00922543843686,3.23621668893135));
#40721=CARTESIAN_POINT('Ctrl Pts',(-7.72733619216139,-1.62945449308302,
3.44310374156095));
#40722=CARTESIAN_POINT('Ctrl Pts',(-7.58632422728927,-3.15489729953755,
1.35073438181086));
#40723=CARTESIAN_POINT('Ctrl Pts',(-7.51146997965987,-3.22704227813193,
0.142739443751509));
#40724=CARTESIAN_POINT('Ctrl Pts',(-7.50277344927318,-3.22592194266142,
0.00226059365463134));
#40725=CARTESIAN_POINT('Ctrl Pts',(-8.50622655072697,-3.22563167876345,
0.00238074690490067));
#40726=CARTESIAN_POINT('Ctrl Pts',(-8.44944182467846,-3.2180404664003,-0.915102997096774));
#40727=CARTESIAN_POINT('Ctrl Pts',(-8.32649938138723,-2.32782638712261,
-2.91438608798932));
#40728=CARTESIAN_POINT('Ctrl Pts',(-8.13739922085333,1.06415762040292,-3.65754739976015));
#40729=CARTESIAN_POINT('Ctrl Pts',(-7.93892606912516,3.65012056591666,-1.08935957187082));
#40730=CARTESIAN_POINT('Ctrl Pts',(-7.74045291739707,2.89469728902442,2.47604766260028));
#40731=CARTESIAN_POINT('Ctrl Pts',(-7.54197976566891,-0.510584113075111,
3.77483619327098));
#40732=CARTESIAN_POINT('Ctrl Pts',(-7.38057097677889,-2.89982523894728,
2.02084194588588));
#40733=CARTESIAN_POINT('Ctrl Pts',(-7.28531990513157,-3.21915280029623,
0.474034782800556));
#40734=CARTESIAN_POINT('Ctrl Pts',(-7.25622655072695,-3.21778123234973,
0.0010418735932435));
#40735=CARTESIAN_POINT('Origin',(-56.8777734492732,0.,0.));
#40736=CARTESIAN_POINT('',(-10.0027734492732,-3.21757454106912,-0.000618869751645723));
#40737=CARTESIAN_POINT('',(-9.75622655072694,-3.22519593513859,-0.00253467400071289));
#40738=CARTESIAN_POINT('',(-56.8777734492732,-3.22275,1.66140794472856E-12));
#40739=CARTESIAN_POINT('Ctrl Pts',(-10.0027734492732,-3.21757454106912,
-0.000618869751645747));
#40740=CARTESIAN_POINT('Ctrl Pts',(-9.97202925323905,-3.21843235789835,
-0.500530984194887));
#40741=CARTESIAN_POINT('Ctrl Pts',(-9.87512733996222,-2.87350040501786,
-2.07507144870353));
#40742=CARTESIAN_POINT('Ctrl Pts',(-9.71206770944269,-0.416464461400303,
-3.78637592858529));
#40743=CARTESIAN_POINT('Ctrl Pts',(-9.51359455771457,2.95543310591665,-2.40322709635013));
#40744=CARTESIAN_POINT('Ctrl Pts',(-9.31512140598641,3.62187388543242,1.17987917949349));
#40745=CARTESIAN_POINT('Ctrl Pts',(-9.11664825425831,0.972785963491132,
3.6829027667608));
#40746=CARTESIAN_POINT('Ctrl Pts',(-8.92919893535388,-2.37020743770456,
2.86276287115722));
#40747=CARTESIAN_POINT('Ctrl Pts',(-8.80790733369217,-3.21701467125132,
0.888720383101256));
#40748=CARTESIAN_POINT('Ctrl Pts',(-8.75277344927317,-3.22488322984771,
-0.0026277942097702));
#40749=CARTESIAN_POINT('Ctrl Pts',(-9.75622655072694,-3.22519593513859,
-0.0025346740007132));
#40750=CARTESIAN_POINT('Ctrl Pts',(-9.74587917871075,-3.22663930449054,
-0.169778291868378));
#40751=CARTESIAN_POINT('Ctrl Pts',(-9.66937408945183,-3.1387605467685,-1.40480258922794));
#40752=CARTESIAN_POINT('Ctrl Pts',(-9.52671128295022,-1.54324543714212,
-3.48259643704148));
#40753=CARTESIAN_POINT('Ctrl Pts',(-9.3282381312221,2.0891572291558,-3.18520117016493));
#40754=CARTESIAN_POINT('Ctrl Pts',(-9.12976497949396,3.80910767480012,0.0279847160571414));
#40755=CARTESIAN_POINT('Ctrl Pts',(-8.93129182776584,2.0421322300825,3.21555288829343));
#40756=CARTESIAN_POINT('Ctrl Pts',(-8.73281867603769,-1.59424790270054,
3.45954593079627));
#40757=CARTESIAN_POINT('Ctrl Pts',(-8.59113025035809,-3.14837458608671,
1.37288362723526));
#40758=CARTESIAN_POINT('Ctrl Pts',(-8.51559954192117,-3.22688469822105,
0.153822299092808));
#40759=CARTESIAN_POINT('Ctrl Pts',(-8.50622655072697,-3.22563167876345,
0.00238074690490067));
#40760=CARTESIAN_POINT('Origin',(-56.8777734492732,0.,0.));
#40761=CARTESIAN_POINT('',(-11.2527734492732,-3.22261253269744,0.00294729705999707));
#40762=CARTESIAN_POINT('',(-11.0062265507269,-3.2176463632475,-0.000794354628363692));
#40763=CARTESIAN_POINT('',(-56.8777734492732,-3.22275,1.66140794472856E-12));
#40764=CARTESIAN_POINT('Ctrl Pts',(-11.2527734492732,-3.22261253269744,
0.00294729705999697));
#40765=CARTESIAN_POINT('Ctrl Pts',(-11.2023088900286,-3.21512743946722,
-0.814391719427845));
#40766=CARTESIAN_POINT('Ctrl Pts',(-11.0856866135414,-2.48411033802337,
-2.71515413077375));
#40767=CARTESIAN_POINT('Ctrl Pts',(-10.9029066198115,0.711270052496804,
-3.74221595216));
#40768=CARTESIAN_POINT('Ctrl Pts',(-10.7044334680833,3.52989055571641,-1.43176743392344));
#40769=CARTESIAN_POINT('Ctrl Pts',(-10.5059603163552,3.11718555708669,2.18934682562397));
#40770=CARTESIAN_POINT('Ctrl Pts',(-10.3074871646271,-0.14904734152245,
3.80629350026567));
#40771=CARTESIAN_POINT('Ctrl Pts',(-10.1397582089331,-2.79402367672853,
2.22815779781535));
#40772=CARTESIAN_POINT('Ctrl Pts',(-10.0381869704818,-3.21658644190266,
0.57521821662457));
#40773=CARTESIAN_POINT('Ctrl Pts',(-10.0027734492732,-3.21757454106912,
-0.000618869751645747));
#40774=CARTESIAN_POINT('Ctrl Pts',(-11.0062265507269,-3.2176463632475,-0.000794354628363692));
#40775=CARTESIAN_POINT('Ctrl Pts',(-10.9761588155003,-3.21872454724075,
-0.489679676012747));
#40776=CARTESIAN_POINT('Ctrl Pts',(-10.879933363031,-2.88439762842973,-2.05285499893439));
#40777=CARTESIAN_POINT('Ctrl Pts',(-10.717550193319,-0.45506613045934,-3.78193062330111));
#40778=CARTESIAN_POINT('Ctrl Pts',(-10.5190770415909,2.93076486464135,-2.43324921262453));
#40779=CARTESIAN_POINT('Ctrl Pts',(-10.3206038898627,3.63372082507465,1.1428724285645));
#40780=CARTESIAN_POINT('Ctrl Pts',(-10.1221307381346,1.01030318175698,3.67278802866238));
#40781=CARTESIAN_POINT('Ctrl Pts',(-9.93400495842269,-2.35297576150677,
2.88395492681478));
#40782=CARTESIAN_POINT('Ctrl Pts',(-9.81203689595346,-3.21741087225541,
0.899522779380902));
#40783=CARTESIAN_POINT('Ctrl Pts',(-9.75622655072694,-3.22519593513859,
-0.0025346740007132));
#40784=CARTESIAN_POINT('Origin',(-56.8777734492732,0.,0.));
#40785=CARTESIAN_POINT('',(-12.5027734492732,-3.22751844495433,-0.00117408986154981));
#40786=CARTESIAN_POINT('',(-12.2562265507269,-3.22228269638671,0.00294601968564429));
#40787=CARTESIAN_POINT('',(-56.8777734492732,-3.22275,1.66140794472856E-12));
#40788=CARTESIAN_POINT('Ctrl Pts',(-12.5027734492732,-3.22751844495433,
-0.00117408986154978));
#40789=CARTESIAN_POINT('Ctrl Pts',(-12.4987462440609,-3.22782301707217,
-0.0661425850922179));
#40790=CARTESIAN_POINT('Ctrl Pts',(-12.428561321606,-3.19659648953803,-1.19809562747136));
#40791=CARTESIAN_POINT('Ctrl Pts',(-12.2922186819084,-1.86765162909789,
-3.31993414279675));
#40792=CARTESIAN_POINT('Ctrl Pts',(-12.0937455301802,1.77656732297672,-3.36955395669975));
#40793=CARTESIAN_POINT('Ctrl Pts',(-11.8952723784521,3.7944844943374,-0.334623284325299));
#40794=CARTESIAN_POINT('Ctrl Pts',(-11.696799226724,2.33886209856671,3.00662757987545));
#40795=CARTESIAN_POINT('Ctrl Pts',(-11.4983260749959,-1.2577968605525,3.59555731114996));
#40796=CARTESIAN_POINT('Ctrl Pts',(-11.3503174825123,-3.08130730766144,
1.58019933119097));
#40797=CARTESIAN_POINT('Ctrl Pts',(-11.2684666072713,-3.22494020091553,
0.2571183532596));
#40798=CARTESIAN_POINT('Ctrl Pts',(-11.2527734492732,-3.22261253269744,
0.00294729705999697));
#40799=CARTESIAN_POINT('Ctrl Pts',(-12.2562265507269,-3.22228269638671,
0.00294601968564401));
#40800=CARTESIAN_POINT('Ctrl Pts',(-12.2064384522899,-3.21496785738077,
-0.803647489328101));
#40801=CARTESIAN_POINT('Ctrl Pts',(-12.0904926366102,-2.49989067661973,
-2.69359488486215));
#40802=CARTESIAN_POINT('Ctrl Pts',(-11.9083891036878,0.673060134005079,
-3.74927652735391));
#40803=CARTESIAN_POINT('Ctrl Pts',(-11.7099159519597,3.51510189157322,-1.46769994018271));
#40804=CARTESIAN_POINT('Ctrl Pts',(-11.5114428002315,3.1393559572694,2.15743565283212));
#40805=CARTESIAN_POINT('Ctrl Pts',(-11.3129696485034,-0.110213061344868,
3.80761572426406));
#40806=CARTESIAN_POINT('Ctrl Pts',(-11.1445642320019,-2.78188136687003,
2.25028698315051));
#40807=CARTESIAN_POINT('Ctrl Pts',(-11.0423165327431,-3.2163522304958,0.58600948422847));
#40808=CARTESIAN_POINT('Ctrl Pts',(-11.0062265507269,-3.2176463632475,-0.000794354628363692));
#40809=CARTESIAN_POINT('Origin',(-56.8777734492732,0.,0.));
#40810=CARTESIAN_POINT('',(-13.7527734492732,-3.21913376994867,-0.00221167296974806));
#40811=CARTESIAN_POINT('',(-13.5062265507269,-3.22767212133845,-0.000986736498302387));
#40812=CARTESIAN_POINT('',(-56.8777734492732,-3.22275,1.66140794472856E-12));
#40813=CARTESIAN_POINT('Ctrl Pts',(-13.7527734492732,-3.21913376994867,
-0.00221167296974831));
#40814=CARTESIAN_POINT('Ctrl Pts',(-13.7290258808505,-3.22157097183896,
-0.387887941665459));
#40815=CARTESIAN_POINT('Ctrl Pts',(-13.6391205951852,-2.97894141443826,
-1.84504509362306));
#40816=CARTESIAN_POINT('Ctrl Pts',(-13.4830575922771,-0.812895766645905,
-3.72146285655909));
#40817=CARTESIAN_POINT('Ctrl Pts',(-13.284584440549,2.68591262275001,-2.70110323814768));
#40818=CARTESIAN_POINT('Ctrl Pts',(-13.0861112888209,3.72598813738973,0.791895018427709));
#40819=CARTESIAN_POINT('Ctrl Pts',(-12.8876381370928,1.35522688587594,3.55997828757123));
#40820=CARTESIAN_POINT('Ctrl Pts',(-12.6931921905769,-2.18285564035938,
3.07915168903474));
#40821=CARTESIAN_POINT('Ctrl Pts',(-12.5649039613036,-3.22281959782984,
1.00114033461412));
#40822=CARTESIAN_POINT('Ctrl Pts',(-12.5027734492732,-3.22751844495433,
-0.00117408986154978));
#40823=CARTESIAN_POINT('Ctrl Pts',(-13.5062265507269,-3.22767212133845,
-0.0009867364983027));
#40824=CARTESIAN_POINT('Ctrl Pts',(-13.5028758063222,-3.22788966329458,
-0.0550354332043843));
#40825=CARTESIAN_POINT('Ctrl Pts',(-13.4333673446748,-3.20216558835672,
-1.1760201796722));
#40826=CARTESIAN_POINT('Ctrl Pts',(-13.2977011657847,-1.9014197600839,-3.30071012336989));
#40827=CARTESIAN_POINT('Ctrl Pts',(-13.0992280140566,1.74210332689385,-3.38750061564265));
#40828=CARTESIAN_POINT('Ctrl Pts',(-12.9007548623284,3.79087359697976,-0.373311926243645));
#40829=CARTESIAN_POINT('Ctrl Pts',(-12.7022817106003,2.36940978052417,2.98261323582365));
#40830=CARTESIAN_POINT('Ctrl Pts',(-12.5038085588722,-1.22105449849256,
3.60820042878236));
#40831=CARTESIAN_POINT('Ctrl Pts',(-12.3551235055811,-3.07345562513412,
1.60242275642856));
#40832=CARTESIAN_POINT('Ctrl Pts',(-12.2725961695326,-3.22468771143873,
0.268142496116896));
#40833=CARTESIAN_POINT('Ctrl Pts',(-12.2562265507269,-3.22228269638671,
0.00294601968564401));
#40834=CARTESIAN_POINT('Origin',(-56.8777734492732,0.,0.));
#40835=CARTESIAN_POINT('',(-15.0027734492732,-3.21951085124981,0.00239014585722026));
#40836=CARTESIAN_POINT('',(-14.7562265507269,-3.21937116695345,-0.0023282602058064));
#40837=CARTESIAN_POINT('',(-56.8777734492732,-3.22275,1.66140794472856E-12));
#40838=CARTESIAN_POINT('Ctrl Pts',(-15.0027734492732,-3.21951085124981,
0.00239014585722008));
#40839=CARTESIAN_POINT('Ctrl Pts',(-14.9593055176401,-3.21465332639279,
-0.703350054867812));
#40840=CARTESIAN_POINT('Ctrl Pts',(-14.8496798687644,-2.63873730532825,
-2.49042930614228));
#40841=CARTESIAN_POINT('Ctrl Pts',(-14.6738965026459,0.313218324198597,
-3.79631131515394));
#40842=CARTESIAN_POINT('Ctrl Pts',(-14.4754233509178,3.35948111786941,-1.79554224090064));
#40843=CARTESIAN_POINT('Ctrl Pts',(-14.2769501991897,3.33041428366469,1.84889859628423));
#40844=CARTESIAN_POINT('Ctrl Pts',(-14.0784770474615,0.252626126046346,
3.80082430015101));
#40845=CARTESIAN_POINT('Ctrl Pts',(-13.903751464156,-2.66048884593533,2.45616432920152));
#40846=CARTESIAN_POINT('Ctrl Pts',(-13.7951835980932,-3.21478123612154,
0.686557284789165));
#40847=CARTESIAN_POINT('Ctrl Pts',(-13.7527734492732,-3.21913376994867,
-0.00221167296974831));
#40848=CARTESIAN_POINT('Ctrl Pts',(-14.7562265507269,-3.21937116695345,
-0.00232826020580643));
#40849=CARTESIAN_POINT('Ctrl Pts',(-14.7331554431118,-3.22187553896581,
-0.376948878832709));
#40850=CARTESIAN_POINT('Ctrl Pts',(-14.643926618254,-2.98830157339018,-1.82279076916866));
#40851=CARTESIAN_POINT('Ctrl Pts',(-14.4885400761535,-0.850814645052164,
-3.71297708884916));
#40852=CARTESIAN_POINT('Ctrl Pts',(-14.2900669244253,2.6582198935355,-2.72836057370837));
#40853=CARTESIAN_POINT('Ctrl Pts',(-14.0915937726972,3.73387198132893,0.753846436352181));
#40854=CARTESIAN_POINT('Ctrl Pts',(-13.8931206209691,1.39147028998462,3.54596881749461));
#40855=CARTESIAN_POINT('Ctrl Pts',(-13.6979982136457,-2.1636578828704,3.09971074376555));
#40856=CARTESIAN_POINT('Ctrl Pts',(-13.5690335235649,-3.22359447467857,
1.01211203080251));
#40857=CARTESIAN_POINT('Ctrl Pts',(-13.5062265507269,-3.22767212133845,
-0.0009867364983027));
#40858=CARTESIAN_POINT('Origin',(-56.8777734492732,0.,0.));
#40859=CARTESIAN_POINT('',(-16.2527734492731,-3.22774822845993,0.000878740854861755));
#40860=CARTESIAN_POINT('',(-16.0062265507269,-3.21926592552825,0.00227844397724913));
#40861=CARTESIAN_POINT('',(-56.8777734492732,-3.22275,1.66140794472856E-12));
#40862=CARTESIAN_POINT('Ctrl Pts',(-16.2527734492731,-3.22774822845993,
0.000878740854861754));
#40863=CARTESIAN_POINT('Ctrl Pts',(-16.1895851544297,-3.22404919134472,
-1.01830685280946));
#40864=CARTESIAN_POINT('Ctrl Pts',(-16.0602391423435,-2.15275090221681,
-3.11126884796112));
#40865=CARTESIAN_POINT('Ctrl Pts',(-15.8647354130147,1.41183724821851,-3.53790911481943));
#40866=CARTESIAN_POINT('Ctrl Pts',(-15.6662622612865,3.73814511142124,-0.732363602411441));
#40867=CARTESIAN_POINT('Ctrl Pts',(-15.4677891095585,2.64248749510294,2.7436007651268));
#40868=CARTESIAN_POINT('Ctrl Pts',(-15.2693159578303,-0.872150850636688,
3.70802349155361));
#40869=CARTESIAN_POINT('Ctrl Pts',(-15.1143107377352,-2.99351493580881,
1.81024609645543));
#40870=CARTESIAN_POINT('Ctrl Pts',(-15.0254632348828,-3.22204642617731,
0.370778823417696));
#40871=CARTESIAN_POINT('Ctrl Pts',(-15.0027734492732,-3.21951085124981,
0.00239014585722008));
#40872=CARTESIAN_POINT('Ctrl Pts',(-16.0062265507269,-3.21926592552825,
0.00227844397724927));
#40873=CARTESIAN_POINT('Ctrl Pts',(-15.9634350799014,-3.21472983079245,
-0.692611678211759));
#40874=CARTESIAN_POINT('Ctrl Pts',(-15.8544858918332,-2.65269578681809,
-2.46852391928997));
#40875=CARTESIAN_POINT('Ctrl Pts',(-15.6793789865222,0.274477321913715,
-3.79930870321287));
#40876=CARTESIAN_POINT('Ctrl Pts',(-15.4809058347941,3.34099059953505,-1.82971752912093));
#40877=CARTESIAN_POINT('Ctrl Pts',(-15.282432683066,3.34910080337457,1.81483008333833));
#40878=CARTESIAN_POINT('Ctrl Pts',(-15.0839595313379,0.291383706511294,
3.79804949390259));
#40879=CARTESIAN_POINT('Ctrl Pts',(-14.9085574872248,-2.64662678665883,
2.47808446093996));
#40880=CARTESIAN_POINT('Ctrl Pts',(-14.7993131603545,-3.2146941093514,0.697297116369363));
#40881=CARTESIAN_POINT('Ctrl Pts',(-14.7562265507269,-3.21937116695345,
-0.00232826020580643));
#40882=CARTESIAN_POINT('Origin',(-56.8777734492732,0.,0.));
#40883=CARTESIAN_POINT('',(-17.5027734492731,-3.22209836681519,-0.00294005213236294));
#40884=CARTESIAN_POINT('',(-17.2562265507269,-3.22760793986041,0.00106918008988845));
#40885=CARTESIAN_POINT('',(-56.8777734492732,-3.22275,1.66140794472856E-12));
#40886=CARTESIAN_POINT('Ctrl Pts',(-17.5027734492732,-3.22209836681519,
-0.00294005213236352));
#40887=CARTESIAN_POINT('Ctrl Pts',(-17.486022508462,-3.22454236991077,-0.274353756782468));
#40888=CARTESIAN_POINT('Ctrl Pts',(-17.4031138504082,-3.06897092992912,
-1.61495252967173));
#40889=CARTESIAN_POINT('Ctrl Pts',(-17.2540474751116,-1.2002865876007,-3.61516215788525));
#40890=CARTESIAN_POINT('Ctrl Pts',(-17.0555743233835,2.38652121163826,-2.96893951211207));
#40891=CARTESIAN_POINT('Ctrl Pts',(-16.8571011716553,3.78866443554566,0.395103929379446));
#40892=CARTESIAN_POINT('Ctrl Pts',(-16.6586280199273,1.72259587914657,3.39746210535554));
#40893=CARTESIAN_POINT('Ctrl Pts',(-16.4601548681991,-1.92036802451838,
3.28972217224905));
#40894=CARTESIAN_POINT('Ctrl Pts',(-16.3248700113144,-3.20525340772958,
1.1635806507222));
#40895=CARTESIAN_POINT('Ctrl Pts',(-16.2557428716724,-3.22792205818097,
0.04877356913509));
#40896=CARTESIAN_POINT('Ctrl Pts',(-16.2527734492731,-3.22774822845993,
0.000878740854861754));
#40897=CARTESIAN_POINT('Ctrl Pts',(-17.2562265507269,-3.22760793986041,
0.00106918008988849));
#40898=CARTESIAN_POINT('Ctrl Pts',(-17.193714716691,-3.22325142349043,-1.00732234075576));
#40899=CARTESIAN_POINT('Ctrl Pts',(-17.0650451654124,-2.17205757669084,
-3.09074945429766));
#40900=CARTESIAN_POINT('Ctrl Pts',(-16.870217896891,1.37567491389401,-3.55212653967123));
#40901=CARTESIAN_POINT('Ctrl Pts',(-16.6717447451629,3.73047995257294,-0.770456842402849));
#40902=CARTESIAN_POINT('Ctrl Pts',(-16.4732715934348,2.67033633643725,2.7165029491714));
#40903=CARTESIAN_POINT('Ctrl Pts',(-16.2747984417066,-0.834281340932724,
3.71672692926525));
#40904=CARTESIAN_POINT('Ctrl Pts',(-16.119116760804,-2.98423536114668,1.83250028631888));
#40905=CARTESIAN_POINT('Ctrl Pts',(-16.0295927971441,-3.22174285621849,
0.381722606907516));
#40906=CARTESIAN_POINT('Ctrl Pts',(-16.0062265507269,-3.21926592552825,
0.00227844397724927));
#40907=CARTESIAN_POINT('Origin',(-56.8777734492732,0.,0.));
#40908=CARTESIAN_POINT('',(-18.7527734492731,-3.21769487768588,0.000892040993440023));
#40909=CARTESIAN_POINT('',(-18.5062265507269,-3.22242620475109,-0.00294804637601787));
#40910=CARTESIAN_POINT('',(-56.8777734492732,-3.22275,1.66140794472856E-12));
#40911=CARTESIAN_POINT('Ctrl Pts',(-18.7527734492731,-3.21769487768588,
0.000892040993440008));
#40912=CARTESIAN_POINT('Ctrl Pts',(-18.7163021452516,-3.21622499493547,
-0.592089635668959));
#40913=CARTESIAN_POINT('Ctrl Pts',(-18.6136731239874,-2.77496559282729,
-2.26275470710555));
#40914=CARTESIAN_POINT('Ctrl Pts',(-18.4448863854804,-0.088316809298266,
-3.80818663688835));
#40915=CARTESIAN_POINT('Ctrl Pts',(-18.2464132337523,3.15170977273075,-2.13934822519688));
#40916=CARTESIAN_POINT('Ctrl Pts',(-18.0479400820241,3.50660436488545,1.48788815048238));
#40917=CARTESIAN_POINT('Ctrl Pts',(-17.849466930296,0.651490054412623,3.7530848683691));
#40918=CARTESIAN_POINT('Ctrl Pts',(-17.667744719379,-2.50870676080208,2.68142439262922));
#40919=CARTESIAN_POINT('Ctrl Pts',(-17.5521802257047,-3.2148897977024,0.797592668823855));
#40920=CARTESIAN_POINT('Ctrl Pts',(-17.5027734492732,-3.22209836681519,
-0.00294005213236352));
#40921=CARTESIAN_POINT('Ctrl Pts',(-18.5062265507269,-3.22242620475109,
-0.00294804637601842));
#40922=CARTESIAN_POINT('Ctrl Pts',(-18.4901520707233,-3.22479872987954,
-0.263333526885802));
#40923=CARTESIAN_POINT('Ctrl Pts',(-18.407919873477,-3.07689763924138,-1.59272602597641));
#40924=CARTESIAN_POINT('Ctrl Pts',(-18.2595299589879,-1.23710096689095,
-3.6027303007957));
#40925=CARTESIAN_POINT('Ctrl Pts',(-18.0610568072598,2.35611197454017,-2.99312892906109));
#40926=CARTESIAN_POINT('Ctrl Pts',(-17.8625836555317,3.79249750493022,0.356436667098387));
#40927=CARTESIAN_POINT('Ctrl Pts',(-17.6641105038036,1.75716239414189,3.37971370727872));
#40928=CARTESIAN_POINT('Ctrl Pts',(-17.4656373520754,-1.88671087539651,
3.30913984219684));
#40929=CARTESIAN_POINT('Ctrl Pts',(-17.3296760343832,-3.19975019779073,
1.18565042945036));
#40930=CARTESIAN_POINT('Ctrl Pts',(-17.2598724339337,-3.22786202534867,
0.0598816876481213));
#40931=CARTESIAN_POINT('Ctrl Pts',(-17.2562265507269,-3.22760793986041,
0.00106918008988849));
#40932=CARTESIAN_POINT('Origin',(-56.8777734492732,0.,0.));
#40933=CARTESIAN_POINT('',(-20.0027734492731,-3.22536883419238,0.00247717968785189));
#40934=CARTESIAN_POINT('',(-19.7562265507269,-3.21761277853822,0.000718109111264298));
#40935=CARTESIAN_POINT('',(-56.8777734492732,-3.22275,1.66140794472856E-12));
#40936=CARTESIAN_POINT('Ctrl Pts',(-20.0027734492731,-3.22536883419238,
0.00247717968785173));
#40937=CARTESIAN_POINT('Ctrl Pts',(-19.9465817820412,-3.2176490068956,-0.905617113904481));
#40938=CARTESIAN_POINT('Ctrl Pts',(-19.8242323975665,-2.34317999425177,
-2.89587764470511));
#40939=CARTESIAN_POINT('Ctrl Pts',(-19.6357252958492,1.03140566167082,-3.66691800852612));
#40940=CARTESIAN_POINT('Ctrl Pts',(-19.437252144121,3.64023257295061,-1.12195906120018));
#40941=CARTESIAN_POINT('Ctrl Pts',(-19.2387789923929,2.9167249089872,2.45006145340748));
#40942=CARTESIAN_POINT('Ctrl Pts',(-19.0403058406648,-0.476805360925414,
3.77925150895946));
#40943=CARTESIAN_POINT('Ctrl Pts',(-18.8783039929582,-2.89047297318496,
2.04032844964183));
#40944=CARTESIAN_POINT('Ctrl Pts',(-18.7824598624943,-3.21889131274313,
0.483559155818458));
#40945=CARTESIAN_POINT('Ctrl Pts',(-18.7527734492731,-3.21769487768588,
0.000892040993440008));
#40946=CARTESIAN_POINT('Ctrl Pts',(-19.7562265507269,-3.21761277853822,
0.000718109111264124));
#40947=CARTESIAN_POINT('Ctrl Pts',(-19.7204317075129,-3.21645311094604,
-0.581302092212425));
#40948=CARTESIAN_POINT('Ctrl Pts',(-19.6184791470562,-2.78719884611832,
-2.24063383593941));
#40949=CARTESIAN_POINT('Ctrl Pts',(-19.4503688693567,-0.12715804379987,
-3.80708750286241));
#40950=CARTESIAN_POINT('Ctrl Pts',(-19.2518957176286,3.12972303941186,-2.17138622062695));
#40951=CARTESIAN_POINT('Ctrl Pts',(-19.0534225659005,3.52159918511936,1.4520411846503));
#40952=CARTESIAN_POINT('Ctrl Pts',(-18.8549494141723,0.689739899217004,
3.74624389141739));
#40953=CARTESIAN_POINT('Ctrl Pts',(-18.6725507424478,-2.49302790386833,
2.70300609504122));
#40954=CARTESIAN_POINT('Ctrl Pts',(-18.556309787966,-3.21503413117626,0.808334669522118));
#40955=CARTESIAN_POINT('Ctrl Pts',(-18.5062265507269,-3.22242620475109,
-0.00294804637601842));
#40956=CARTESIAN_POINT('Origin',(-56.8777734492732,0.,0.));
#40957=CARTESIAN_POINT('',(-21.2527734492731,-3.22546356093439,-0.00244372236887117));
#40958=CARTESIAN_POINT('',(-21.0062265507269,-3.22506038431272,0.00257670913582225));
#40959=CARTESIAN_POINT('',(-56.8777734492732,-3.22275,1.66140794472856E-12));
#40960=CARTESIAN_POINT('Ctrl Pts',(-21.2527734492731,-3.22546356093439,
-0.00244372236887114));
#40961=CARTESIAN_POINT('Ctrl Pts',(-21.2430191360735,-3.22679134021169,
-0.160067793553129));
#40962=CARTESIAN_POINT('Ctrl Pts',(-21.1671071056311,-3.1446431200358,-1.38537302685204));
#40963=CARTESIAN_POINT('Ctrl Pts',(-21.0250373579461,-1.57432862205077,
-3.46865603800252));
#40964=CARTESIAN_POINT('Ctrl Pts',(-20.8265642062179,2.06058850407911,-3.20375722192501));
#40965=CARTESIAN_POINT('Ctrl Pts',(-20.6280910544898,3.80920573593449,-0.00608124192798155));
#40966=CARTESIAN_POINT('Ctrl Pts',(-20.4296179027617,2.07080731049629,3.19716161664916));
#40967=CARTESIAN_POINT('Ctrl Pts',(-20.2311447510336,-1.56324548898088,
3.47366504737583));
#40968=CARTESIAN_POINT('Ctrl Pts',(-20.0888632665374,-3.14255397345149,
1.39230915019779));
#40969=CARTESIAN_POINT('Ctrl Pts',(-20.0127394992839,-3.22673800846152,
0.163535101444709));
#40970=CARTESIAN_POINT('Ctrl Pts',(-20.0027734492731,-3.22536883419238,
0.00247717968785173));
#40971=CARTESIAN_POINT('Ctrl Pts',(-21.0062265507269,-3.22506038431272,
0.00257670913582222));
#40972=CARTESIAN_POINT('Ctrl Pts',(-20.9507113443025,-3.21723391237169,
-0.894808353614492));
#40973=CARTESIAN_POINT('Ctrl Pts',(-20.8290384206354,-2.36051683312814,
-2.87471529474172));
#40974=CARTESIAN_POINT('Ctrl Pts',(-20.6412077797255,0.993947162456761,
-3.67724808257454));
#40975=CARTESIAN_POINT('Ctrl Pts',(-20.4427346279974,3.62859839939353,-1.15903325166825));
#40976=CARTESIAN_POINT('Ctrl Pts',(-20.2442614762692,2.94156519346794,2.42018152937583));
#40977=CARTESIAN_POINT('Ctrl Pts',(-20.0457883245411,-0.438229862995021,
3.78391847292371));
#40978=CARTESIAN_POINT('Ctrl Pts',(-19.883110016027,-2.87966204308117,2.06254890030518));
#40979=CARTESIAN_POINT('Ctrl Pts',(-19.7865894247556,-3.21859646327756,
0.494415090804314));
#40980=CARTESIAN_POINT('Ctrl Pts',(-19.7562265507269,-3.21761277853822,
0.000718109111264124));
#40981=CARTESIAN_POINT('Origin',(-56.8777734492732,0.,0.));
#40982=CARTESIAN_POINT('',(-22.5027734492731,-3.21772419204198,-0.000945844158032132));
#40983=CARTESIAN_POINT('',(-22.2562265507269,-3.22575963611168,-0.00232963559445576));
#40984=CARTESIAN_POINT('',(-56.8777734492732,-3.22275,1.66140794472856E-12));
#40985=CARTESIAN_POINT('Ctrl Pts',(-22.5027734492731,-3.21772419204198,
-0.000945844158032338));
#40986=CARTESIAN_POINT('Ctrl Pts',(-22.4732987728631,-3.21898439121486,
-0.480159460729692));
#40987=CARTESIAN_POINT('Ctrl Pts',(-22.3776663792103,-2.89382542886802,
-2.03337186564838));
#40988=CARTESIAN_POINT('Ctrl Pts',(-22.2158762683149,-0.488869742173803,
-3.77770984795902));
#40989=CARTESIAN_POINT('Ctrl Pts',(-22.0174031165867,2.90888721456023,-2.45936180606832));
#40990=CARTESIAN_POINT('Ctrl Pts',(-21.8189299648586,3.64379633223308,1.11033040550302));
#40991=CARTESIAN_POINT('Ctrl Pts',(-21.6204568131305,1.04310854511736,3.66360613102486));
#40992=CARTESIAN_POINT('Ctrl Pts',(-21.431737974602,-2.33771495359402,2.9024904986763));
#40993=CARTESIAN_POINT('Ctrl Pts',(-21.3091768533162,-3.21778580141147,
0.909002731313567));
#40994=CARTESIAN_POINT('Ctrl Pts',(-21.2527734492731,-3.22546356093439,
-0.00244372236887114));
#40995=CARTESIAN_POINT('Ctrl Pts',(-22.2562265507269,-3.22575963611168,
-0.00232963559445581));
#40996=CARTESIAN_POINT('Ctrl Pts',(-22.2471486983348,-3.22695472404273,
-0.148987392685038));
#40997=CARTESIAN_POINT('Ctrl Pts',(-22.1719131286999,-3.15123563559383,
-1.36321886650731));
#40998=CARTESIAN_POINT('Ctrl Pts',(-22.0305198418224,-1.60962907726382,
-3.45241635035243));
#40999=CARTESIAN_POINT('Ctrl Pts',(-21.8320466900942,2.02780095034114,-3.22460970170803));
#41000=CARTESIAN_POINT('Ctrl Pts',(-21.6335735383662,3.80894540192439,-0.0449371529252134));
#41001=CARTESIAN_POINT('Ctrl Pts',(-21.435100386638,2.1033125106639,3.17587167641245));
#41002=CARTESIAN_POINT('Ctrl Pts',(-21.2366272349099,-1.52773060133581,
3.48943027331057));
#41003=CARTESIAN_POINT('Ctrl Pts',(-21.0936692896062,-3.13579716094896,
1.41447418339441));
#41004=CARTESIAN_POINT('Ctrl Pts',(-21.0168690615452,-3.22656075362891,
0.174609398079968));
#41005=CARTESIAN_POINT('Ctrl Pts',(-21.0062265507269,-3.22506038431272,
0.00257670913582222));
#41006=CARTESIAN_POINT('Origin',(-56.8777734492732,0.,0.));
#41007=CARTESIAN_POINT('',(-23.7527734492731,-3.22199650686841,0.00293511691597435));
#41008=CARTESIAN_POINT('',(-23.5062265507269,-3.21782926820092,-0.00111537477188062));
#41009=CARTESIAN_POINT('',(-56.8777734492732,-3.22275,1.66140794472856E-12));
#41010=CARTESIAN_POINT('Ctrl Pts',(-23.7527734492731,-3.22199650686841,
0.00293511691597463));
#41011=CARTESIAN_POINT('Ctrl Pts',(-23.7035784096527,-3.21484998616783,
-0.794231051178209));
#41012=CARTESIAN_POINT('Ctrl Pts',(-23.5882256527895,-2.51357736811805,
-2.67466106277306));
#41013=CARTESIAN_POINT('Ctrl Pts',(-23.4067151786836,0.639503469586358,
-3.7551458869885));
#41014=CARTESIAN_POINT('Ctrl Pts',(-23.2082420269555,3.50183579684358,-1.4990768399667));
#41015=CARTESIAN_POINT('Ctrl Pts',(-23.0097688752274,3.15852445469445,2.12927419307066));
#41016=CARTESIAN_POINT('Ctrl Pts',(-22.8112957234992,-0.0761571601507046,
3.80844921288671));
#41017=CARTESIAN_POINT('Ctrl Pts',(-22.6422972481812,-2.77110315051519,
2.26967547266405));
#41018=CARTESIAN_POINT('Ctrl Pts',(-22.5394564901058,-3.21615579695349,
0.595464865147483));
#41019=CARTESIAN_POINT('Ctrl Pts',(-22.5027734492731,-3.21772419204198,
-0.000945844158032338));
#41020=CARTESIAN_POINT('Ctrl Pts',(-23.5062265507269,-3.21782926820092,
-0.00111537477188048));
#41021=CARTESIAN_POINT('Ctrl Pts',(-23.4774283351244,-3.21928393819887,
-0.469292530410071));
#41022=CARTESIAN_POINT('Ctrl Pts',(-23.3824724022791,-2.90443597318009,
-2.01114266715587));
#41023=CARTESIAN_POINT('Ctrl Pts',(-23.2213587521912,-0.527379242599795,
-3.77252641568339));
#41024=CARTESIAN_POINT('Ctrl Pts',(-23.022885600463,2.88364878803355,-2.48890620350118));
#41025=CARTESIAN_POINT('Ctrl Pts',(-22.8244124487349,3.65493269060604,1.0731036528189));
#41026=CARTESIAN_POINT('Ctrl Pts',(-22.6259392970067,1.08042526501054,3.65277506415067));
#41027=CARTESIAN_POINT('Ctrl Pts',(-22.4365439976708,-2.32013180474122,
2.9235810681689));
#41028=CARTESIAN_POINT('Ctrl Pts',(-22.3133064155775,-3.21824514318517,
0.91982734519994));
#41029=CARTESIAN_POINT('Ctrl Pts',(-22.2562265507269,-3.22575963611168,
-0.00232963559445581));
#41030=CARTESIAN_POINT('Origin',(-56.8777734492732,0.,0.));
#41031=CARTESIAN_POINT('',(-25.0027734492731,-3.22778696626011,-0.000818109748633706));
#41032=CARTESIAN_POINT('',(-24.7562265507269,-3.22167406644033,0.00291166086733255));
#41033=CARTESIAN_POINT('',(-56.8777734492732,-3.22275,1.66140794472856E-12));
#41034=CARTESIAN_POINT('Ctrl Pts',(-25.0027734492731,-3.22778696626011,
-0.000818109748633739));
#41035=CARTESIAN_POINT('Ctrl Pts',(-25.000015763685,-3.22793832383972,-0.0452963360147774));
#41036=CARTESIAN_POINT('Ctrl Pts',(-24.9311003608541,-3.2069519157609,-1.15667469946367));
#41037=CARTESIAN_POINT('Ctrl Pts',(-24.7960272407805,-1.93086202407817,
-3.28357384021623));
#41038=CARTESIAN_POINT('Ctrl Pts',(-24.5975540890524,1.71173930615894,-3.40294488170616));
#41039=CARTESIAN_POINT('Ctrl Pts',(-24.3990809373243,3.78738359192001,-0.407198781720557));
#41040=CARTESIAN_POINT('Ctrl Pts',(-24.2006077855962,2.3959886047388,2.9613044298318));
#41041=CARTESIAN_POINT('Ctrl Pts',(-24.002134633868,-1.18873758023125,3.6189761377392));
#41042=CARTESIAN_POINT('Ctrl Pts',(-23.8528565217603,-3.06646226142991,
1.62191059947188));
#41043=CARTESIAN_POINT('Ctrl Pts',(-23.7697361268954,-3.22446066032168,
0.277801705602104));
#41044=CARTESIAN_POINT('Ctrl Pts',(-23.7527734492731,-3.22199650686841,
0.00293511691597463));
#41045=CARTESIAN_POINT('Ctrl Pts',(-24.7562265507269,-3.22167406644033,
0.00291166086733272));
#41046=CARTESIAN_POINT('Ctrl Pts',(-24.7077079719139,-3.21473953966774,
-0.783493160315694));
#41047=CARTESIAN_POINT('Ctrl Pts',(-24.5930316758583,-2.52902034751673,
-2.65302825184713));
#41048=CARTESIAN_POINT('Ctrl Pts',(-24.41219766256,0.601165393915808,-3.76147372604303));
#41049=CARTESIAN_POINT('Ctrl Pts',(-24.2137245108318,3.48636199609287,-1.53471966650373));
#41050=CARTESIAN_POINT('Ctrl Pts',(-24.0152513591037,3.18007992525289,2.09694446553971));
#41051=CARTESIAN_POINT('Ctrl Pts',(-23.8167782073755,-0.0373046849413855,
3.80902780024449));
#41052=CARTESIAN_POINT('Ctrl Pts',(-23.64710327125,-2.7586563104495,2.29177527391161));
#41053=CARTESIAN_POINT('Ctrl Pts',(-23.5435860523671,-3.21594214620264,
0.606243964965262));
#41054=CARTESIAN_POINT('Ctrl Pts',(-23.5062265507269,-3.21782926820092,
-0.00111537477188048));
#41055=CARTESIAN_POINT('Origin',(-56.8777734492732,0.,0.));
#41056=CARTESIAN_POINT('',(-26.2527734492731,-3.21959007219934,-0.00242327538640936));
#41057=CARTESIAN_POINT('',(-26.0062265507269,-3.22789335144083,-0.000621618279896263));
#41058=CARTESIAN_POINT('',(-56.8777734492732,-3.22275,1.66140794472856E-12));
#41059=CARTESIAN_POINT('Ctrl Pts',(-26.2527734492731,-3.21959007219934,
-0.00242327538640976));
#41060=CARTESIAN_POINT('Ctrl Pts',(-26.2302954004745,-3.2221409144289,-0.367351620292292));
#41061=CARTESIAN_POINT('Ctrl Pts',(-26.1416596344333,-2.99639014349327,
-1.80328044297311));
#41062=CARTESIAN_POINT('Ctrl Pts',(-25.9868661511494,-0.883985791987881,
-3.70521989087602));
#41063=CARTESIAN_POINT('Ctrl Pts',(-25.7883929994212,2.63371395382021,-2.75202400600582));
#41064=CARTESIAN_POINT('Ctrl Pts',(-25.5899198476931,3.74046442819159,0.720424306650572));
#41065=CARTESIAN_POINT('Ctrl Pts',(-25.3914466959649,1.42312627862469,3.53338321092794));
#41066=CARTESIAN_POINT('Ctrl Pts',(-25.195731229825,-2.14666794500629,3.11767679330578));
#41067=CARTESIAN_POINT('Ctrl Pts',(-25.0661734809277,-3.22430720940184,
1.02174986004855));
#41068=CARTESIAN_POINT('Ctrl Pts',(-25.0027734492731,-3.22778696626011,
-0.000818109748633739));
#41069=CARTESIAN_POINT('Ctrl Pts',(-26.0062265507269,-3.22789335144083,
-0.000621618279895882));
#41070=CARTESIAN_POINT('Ctrl Pts',(-26.0041453259463,-3.22798218375112,
-0.0341863611775746));
#41071=CARTESIAN_POINT('Ctrl Pts',(-25.9359063839229,-3.21230194639243,
-1.13461799097082));
#41072=CARTESIAN_POINT('Ctrl Pts',(-25.8015097246568,-1.9642559671063,-3.26370692897528));
#41073=CARTESIAN_POINT('Ctrl Pts',(-25.6030365729288,1.67693807707542,-3.4202285169574));
#41074=CARTESIAN_POINT('Ctrl Pts',(-25.4045634212006,3.78303274977641,-0.445811211919431));
#41075=CARTESIAN_POINT('Ctrl Pts',(-25.2060902694725,2.42607098893233,2.93670971994425));
#41076=CARTESIAN_POINT('Ctrl Pts',(-25.0076171177444,-1.15175992694511,
3.63091358933775));
#41077=CARTESIAN_POINT('Ctrl Pts',(-24.8576625448291,-3.05835901460307,
1.64414342660099));
#41078=CARTESIAN_POINT('Ctrl Pts',(-24.7738656891567,-3.2241951435345,0.288812522806601));
#41079=CARTESIAN_POINT('Ctrl Pts',(-24.7562265507269,-3.22167406644033,
0.00291166086733272));
#41080=CARTESIAN_POINT('Origin',(-56.8777734492732,0.,0.));
#41081=CARTESIAN_POINT('',(-27.5027734492731,-3.21906218437362,0.00217345376617098));
#41082=CARTESIAN_POINT('',(-27.2562265507269,-3.21985095291246,-0.00252303240216523));
#41083=CARTESIAN_POINT('',(-56.8777734492732,-3.22275,1.66140794472856E-12));
#41084=CARTESIAN_POINT('Ctrl Pts',(-27.5027734492731,-3.21906218437362,
0.00217345376617089));
#41085=CARTESIAN_POINT('Ctrl Pts',(-27.4605750372641,-3.21481218592836,
-0.683195035194659));
#41086=CARTESIAN_POINT('Ctrl Pts',(-27.3522189080125,-2.66479263286037,
-2.44929786227344));
#41087=CARTESIAN_POINT('Ctrl Pts',(-27.1777050615181,0.240489146638442,
-3.80161153861474));
#41088=CARTESIAN_POINT('Ctrl Pts',(-26.9792319097899,3.32449393969521,-1.85952288641721));
#41089=CARTESIAN_POINT('Ctrl Pts',(-26.7807587580619,3.36519699902431,1.78480656597217));
#41090=CARTESIAN_POINT('Ctrl Pts',(-26.5822856063336,0.325338009741355,
3.79529188595517));
#41091=CARTESIAN_POINT('Ctrl Pts',(-26.4062905034042,-2.634332868274,2.49728024707007));
#41092=CARTESIAN_POINT('Ctrl Pts',(-26.2964531177173,-3.21463323880872,
0.706710744840075));
#41093=CARTESIAN_POINT('Ctrl Pts',(-26.2527734492731,-3.21959007219934,
-0.00242327538640976));
#41094=CARTESIAN_POINT('Ctrl Pts',(-27.2562265507269,-3.21985095291246,
-0.00252303240216523));
#41095=CARTESIAN_POINT('Ctrl Pts',(-27.2344249627358,-3.22244081034009,
-0.356396858653335));
#41096=CARTESIAN_POINT('Ctrl Pts',(-27.1464656575021,-3.00548259499999,
-1.78102692704359));
#41097=CARTESIAN_POINT('Ctrl Pts',(-26.9923486350256,-0.921735281371103,
-3.69600980702566));
#41098=CARTESIAN_POINT('Ctrl Pts',(-26.7938754832976,2.60550451902449,-2.77874623236759));
#41099=CARTESIAN_POINT('Ctrl Pts',(-26.5954023315693,3.74761847355685,0.682231778217214));
#41100=CARTESIAN_POINT('Ctrl Pts',(-26.3969291798413,1.45909486194852,3.51868251002977));
#41101=CARTESIAN_POINT('Ctrl Pts',(-26.2005372528937,-2.12710644928032,
3.13810092564533));
#41102=CARTESIAN_POINT('Ctrl Pts',(-26.070303043189,-3.22515839320196,1.0327655560849));
#41103=CARTESIAN_POINT('Ctrl Pts',(-26.0062265507269,-3.22789335144083,
-0.000621618279895882));
#41104=CARTESIAN_POINT('Origin',(-56.8777734492732,0.,0.));
#41105=CARTESIAN_POINT('',(-28.7527734492731,-3.22746554720106,0.00123150883681248));
#41106=CARTESIAN_POINT('',(-28.5062265507269,-3.21884251806067,0.00204608467250691));
#41107=CARTESIAN_POINT('',(-56.8777734492732,-3.22275,1.66140794472856E-12));
#41108=CARTESIAN_POINT('Ctrl Pts',(-28.7527734492731,-3.22746554720106,
0.00123150883681244));
#41109=CARTESIAN_POINT('Ctrl Pts',(-28.6908546740537,-3.22258522547558,
-0.997710618875136));
#41110=CARTESIAN_POINT('Ctrl Pts',(-28.5627781815916,-2.18882495849549,
-3.07270221306961));
#41111=CARTESIAN_POINT('Ctrl Pts',(-28.3685439718869,1.34385328587831,-3.56428725921659));
#41112=CARTESIAN_POINT('Ctrl Pts',(-28.1700708201588,3.72344069482658,-0.803787728376804));
#41113=CARTESIAN_POINT('Ctrl Pts',(-27.9715976684306,2.69452331250517,2.69251359115343));
#41114=CARTESIAN_POINT('Ctrl Pts',(-27.7731245167025,-0.801009325330438,
3.72403939035468));
#41115=CARTESIAN_POINT('Ctrl Pts',(-27.6168497769833,-2.97598203878223,
1.85201076842463));
#41116=CARTESIAN_POINT('Ctrl Pts',(-27.5267327545069,-3.22147523749922,
0.391310201877));
#41117=CARTESIAN_POINT('Ctrl Pts',(-27.5027734492731,-3.21906218437362,
0.00217345376617089));
#41118=CARTESIAN_POINT('Ctrl Pts',(-28.5062265507269,-3.21884251806067,
0.00204608467250695));
#41119=CARTESIAN_POINT('Ctrl Pts',(-28.4647045995254,-3.21492241651639,
-0.672451064148926));
#41120=CARTESIAN_POINT('Ctrl Pts',(-28.3570249310813,-2.67843067685807,
-2.42734436139883));
#41121=CARTESIAN_POINT('Ctrl Pts',(-28.1831875453944,0.201697865006982,
-3.80386676867179));
#41122=CARTESIAN_POINT('Ctrl Pts',(-27.9847143936663,3.30535260103752,-1.89333795329003));
#41123=CARTESIAN_POINT('Ctrl Pts',(-27.7862412419381,3.38322793010033,1.75038658459866));
#41124=CARTESIAN_POINT('Ctrl Pts',(-27.5877680902101,0.364035370925649,
3.79177566204397));
#41125=CARTESIAN_POINT('Ctrl Pts',(-27.4110965264729,-2.62014813522317,
2.51914926709635));
#41126=CARTESIAN_POINT('Ctrl Pts',(-27.3005826799786,-3.21458179312233,
0.717446227746891));
#41127=CARTESIAN_POINT('Ctrl Pts',(-27.2562265507269,-3.21985095291246,
-0.00252303240216523));
#41128=CARTESIAN_POINT('Origin',(-56.8777734492732,0.,0.));
#41129=CARTESIAN_POINT('',(-30.0027734492731,-3.22271626523272,-0.002945234897088));
#41130=CARTESIAN_POINT('',(-29.7562265507269,-3.22728206048765,0.00141062354910213));
#41131=CARTESIAN_POINT('',(-56.8777734492732,-3.22275,1.66140794472856E-12));
#41132=CARTESIAN_POINT('Ctrl Pts',(-30.0027734492731,-3.22271626523272,
-0.00294523489708803));
#41133=CARTESIAN_POINT('Ctrl Pts',(-29.987292028086,-3.22501767013846,-0.253666310298777));
#41134=CARTESIAN_POINT('Ctrl Pts',(-29.9056528896563,-3.08373759365553,
-1.57324436536649));
#41135=CARTESIAN_POINT('Ctrl Pts',(-29.7578560339838,-1.26927074168613,
-3.59152295057115));
#41136=CARTESIAN_POINT('Ctrl Pts',(-29.5593828822556,2.32925028389996,-3.01408003130834));
#41137=CARTESIAN_POINT('Ctrl Pts',(-29.3609097305275,3.79553357470212,0.322506129381382));
#41138=CARTESIAN_POINT('Ctrl Pts',(-29.1624365787994,1.78731695127927,3.36386436050109));
#41139=CARTESIAN_POINT('Ctrl Pts',(-28.9639634270713,-1.85704185655309,
3.32588046435669));
#41140=CARTESIAN_POINT('Ctrl Pts',(-28.8274090505625,-3.19482911305915,
1.20500740939856));
#41141=CARTESIAN_POINT('Ctrl Pts',(-28.7570123912965,-3.22779965266062,
0.0696188073427509));
#41142=CARTESIAN_POINT('Ctrl Pts',(-28.7527734492731,-3.22746554720106,
0.00123150883681244));
#41143=CARTESIAN_POINT('Ctrl Pts',(-29.7562265507269,-3.22728206048765,
0.00141062354910211));
#41144=CARTESIAN_POINT('Ctrl Pts',(-29.694984236315,-3.22186222518609,-0.986767058927104));
#41145=CARTESIAN_POINT('Ctrl Pts',(-29.5675842046605,-2.20776927460923,
-3.05205235830958));
#41146=CARTESIAN_POINT('Ctrl Pts',(-29.3740264557631,1.30742541749708,-3.57780983287773));
#41147=CARTESIAN_POINT('Ctrl Pts',(-29.1755533040351,3.71504773171258,-0.841727256093824));
#41148=CARTESIAN_POINT('Ctrl Pts',(-28.9770801523069,2.72184832452091,2.66488763756686));
#41149=CARTESIAN_POINT('Ctrl Pts',(-28.7786070005788,-0.762980147188692,
3.732016307246));
#41150=CARTESIAN_POINT('Ctrl Pts',(-28.6216558000521,-2.96643236631015,
1.87426426718019));
#41151=CARTESIAN_POINT('Ctrl Pts',(-28.5308623167682,-3.22116838911703,
0.402238114985581));
#41152=CARTESIAN_POINT('Ctrl Pts',(-28.5062265507269,-3.21884251806067,
0.00204608467250695));
#41153=CARTESIAN_POINT('Origin',(-56.8777734492732,0.,0.));
#41154=CARTESIAN_POINT('',(-31.2527734492731,-3.21755572586831,0.000563448608700447));
#41155=CARTESIAN_POINT('',(-31.0062265507269,-3.22304863623215,-0.00293073635939056));
#41156=CARTESIAN_POINT('',(-56.8777734492732,-3.22275,1.66140794472856E-12));
#41157=CARTESIAN_POINT('Ctrl Pts',(-31.2527734492731,-3.21755572586831,
0.000563448608700487));
#41158=CARTESIAN_POINT('Ctrl Pts',(-31.2175716648756,-3.21666178478838,
-0.571839069851177));
#41159=CARTESIAN_POINT('Ctrl Pts',(-31.1162121632355,-2.7977911693512,-2.22122822227451));
#41160=CARTESIAN_POINT('Ctrl Pts',(-30.9486949443525,-0.16119973612574,
-3.80579820343283));
#41161=CARTESIAN_POINT('Ctrl Pts',(-30.7502217926245,3.11017927930475,-2.19928856014008));
#41162=CARTESIAN_POINT('Ctrl Pts',(-30.5517486408963,3.53444406784637,1.42048951120562));
#41163=CARTESIAN_POINT('Ctrl Pts',(-30.3532754891682,0.723214987379329,
3.73992585517541));
#41164=CARTESIAN_POINT('Ctrl Pts',(-30.1702837586271,-2.4791338182994,2.72189388402554));
#41165=CARTESIAN_POINT('Ctrl Pts',(-30.0534497453287,-3.21518293383258,
0.817755609742787));
#41166=CARTESIAN_POINT('Ctrl Pts',(-30.0027734492731,-3.22271626523272,
-0.00294523489708803));
#41167=CARTESIAN_POINT('Ctrl Pts',(-31.0062265507269,-3.22304863623215,
-0.00293073635939122));
#41168=CARTESIAN_POINT('Ctrl Pts',(-30.9914215903473,-3.22525997788838,
-0.242633256256471));
#41169=CARTESIAN_POINT('Ctrl Pts',(-30.9104589127251,-3.09141502618626,
-1.551028275585));
#41170=CARTESIAN_POINT('Ctrl Pts',(-30.7633385178601,-1.30584039539486,
-3.57838864355298));
#41171=CARTESIAN_POINT('Ctrl Pts',(-30.5648653661319,2.29838356734553,-3.03768289982842));
#41172=CARTESIAN_POINT('Ctrl Pts',(-30.3663922144039,3.79862574454081,0.283772577015008));
#41173=CARTESIAN_POINT('Ctrl Pts',(-30.1679190626757,1.82153737945105,3.34545751696486));
#41174=CARTESIAN_POINT('Ctrl Pts',(-29.9694459109477,-1.82301916741003,
3.34465028632439));
#41175=CARTESIAN_POINT('Ctrl Pts',(-29.8322150736313,-3.18910491711469,
1.2270956905746));
#41176=CARTESIAN_POINT('Ctrl Pts',(-29.7611419535577,-3.22771706484762,
0.080723291995476));
#41177=CARTESIAN_POINT('Ctrl Pts',(-29.7562265507269,-3.22728206048765,
0.00141062354910211));
#41178=CARTESIAN_POINT('Origin',(-56.8777734492732,0.,0.));
#41179=CARTESIAN_POINT('',(-32.5027734492731,-3.22478385912128,0.00265457541594172));
#41180=CARTESIAN_POINT('',(-32.2562265507269,-3.21750741052827,0.00038513969681353));
#41181=CARTESIAN_POINT('',(-56.8777734492732,-3.22275,1.66140794472856E-12));
#41182=CARTESIAN_POINT('Ctrl Pts',(-32.5027734492731,-3.22478385912128,
0.00265457541594166));
#41183=CARTESIAN_POINT('Ctrl Pts',(-32.4478513016652,-3.21689735745027,
-0.885341341109883));
#41184=CARTESIAN_POINT('Ctrl Pts',(-32.3267714368147,-2.37556273920755,
-2.85611887470812));
#41185=CARTESIAN_POINT('Ctrl Pts',(-32.1395338547213,0.961021826073252,
-3.68599001219353));
#41186=CARTESIAN_POINT('Ctrl Pts',(-31.9410607029932,3.61808817488804,-1.19143748426638));
#41187=CARTESIAN_POINT('Ctrl Pts',(-31.7425875512651,2.96309132998079,2.39377841296397));
#41188=CARTESIAN_POINT('Ctrl Pts',(-31.5441143995369,-0.404372779207533,
3.78768636183299));
#41189=CARTESIAN_POINT('Ctrl Pts',(-31.3808430322063,-2.87005783900842,
2.08202372962302));
#41190=CARTESIAN_POINT('Ctrl Pts',(-31.2837293821183,-3.21834184454131,
0.503925827112667));
#41191=CARTESIAN_POINT('Ctrl Pts',(-31.2527734492731,-3.21755572586831,
0.000563448608700487));
#41192=CARTESIAN_POINT('Ctrl Pts',(-32.2562265507269,-3.21750741052827,
0.000385139696813461));
#41193=CARTESIAN_POINT('Ctrl Pts',(-32.2217012271369,-3.21690860986362,
-0.561038684184639));
#41194=CARTESIAN_POINT('Ctrl Pts',(-32.1210181863043,-2.80972226202356,
-2.19908042246798));
#41195=CARTESIAN_POINT('Ctrl Pts',(-31.9541774282289,-0.200012812968363,
-3.80395574332859));
#41196=CARTESIAN_POINT('Ctrl Pts',(-31.7557042765008,3.08758327993605,-2.23089979873894));
#41197=CARTESIAN_POINT('Ctrl Pts',(-31.5572311247726,3.54874993145618,1.38436207205476));
#41198=CARTESIAN_POINT('Ctrl Pts',(-31.3587579730445,0.761326868309329,
3.73235392509128));
#41199=CARTESIAN_POINT('Ctrl Pts',(-31.1750897816959,-2.4631155885873,2.74339848566718));
#41200=CARTESIAN_POINT('Ctrl Pts',(-31.05757930759,-3.21537833604205,0.828505816538859));
#41201=CARTESIAN_POINT('Ctrl Pts',(-31.0062265507269,-3.22304863623215,
-0.00293073635939122));
#41202=CARTESIAN_POINT('Origin',(-56.8777734492732,0.,0.));
#41203=CARTESIAN_POINT('',(-33.7527734492731,-3.22601040418458,-0.00222081755632452));
#41204=CARTESIAN_POINT('',(-33.5062265507269,-3.22446233910715,0.00273246397124949));
#41205=CARTESIAN_POINT('',(-56.8777734492732,-3.22275,1.66140794472856E-12));
#41206=CARTESIAN_POINT('Ctrl Pts',(-33.7527734492731,-3.22601040418458,
-0.00222081755632462));
#41207=CARTESIAN_POINT('Ctrl Pts',(-33.7442886556975,-3.22708935468399,
-0.139269568694677));
#41208=CARTESIAN_POINT('Ctrl Pts',(-33.6696461448792,-3.15691350318655,
-1.34380329108049));
#41209=CARTESIAN_POINT('Ctrl Pts',(-33.5288459168183,-1.64043970914924,
-3.43788348854727));
#41210=CARTESIAN_POINT('Ctrl Pts',(-33.3303727650901,1.99888224657508,-3.24261546972602));
#41211=CARTESIAN_POINT('Ctrl Pts',(-33.131899613362,3.80839132946346,-0.0789987458582374));
#41212=CARTESIAN_POINT('Ctrl Pts',(-32.9334264616339,2.13163027743554,3.15693485528285));
#41213=CARTESIAN_POINT('Ctrl Pts',(-32.7349533099058,-1.49646358995037,
3.50295333170919));
#41214=CARTESIAN_POINT('Ctrl Pts',(-32.5914023057855,-3.12976997368095,
1.43391316872666));
#41215=CARTESIAN_POINT('Ctrl Pts',(-32.5140090189079,-3.22639722171832,
0.184314258988555));
#41216=CARTESIAN_POINT('Ctrl Pts',(-32.5027734492731,-3.22478385912128,
0.00265457541594166));
#41217=CARTESIAN_POINT('Ctrl Pts',(-33.5062265507269,-3.22446233910715,
0.00273246397124952));
#41218=CARTESIAN_POINT('Ctrl Pts',(-33.4519808639265,-3.21654358931584,
-0.874552402068785));
#41219=CARTESIAN_POINT('Ctrl Pts',(-33.3315774598834,-2.392549869961,-2.83485900261666));
#41220=CARTESIAN_POINT('Ctrl Pts',(-33.1450163385977,0.923372444839,-3.6956011352236));
#41221=CARTESIAN_POINT('Ctrl Pts',(-32.9465431868696,3.60574643173899,-1.22828217139039));
#41222=CARTESIAN_POINT('Ctrl Pts',(-32.7480700351414,2.98735507926837,2.36342845310018));
#41223=CARTESIAN_POINT('Ctrl Pts',(-32.5495968834133,-0.365715011353638,
3.79161403007012));
#41224=CARTESIAN_POINT('Ctrl Pts',(-32.3856490552751,-2.85895781632522,
2.10422941420904));
#41225=CARTESIAN_POINT('Ctrl Pts',(-32.2878589443796,-3.21805603676474,
0.514766398334013));
#41226=CARTESIAN_POINT('Ctrl Pts',(-32.2562265507269,-3.21750741052827,
0.000385139696813461));
#41227=CARTESIAN_POINT('Origin',(-56.8777734492732,0.,0.));
#41228=CARTESIAN_POINT('',(-35.0027734492731,-3.21793583222462,-0.00126067022288214));
#41229=CARTESIAN_POINT('',(-34.7562265507269,-3.22628460838897,-0.0020870326190342));
#41230=CARTESIAN_POINT('',(-56.8777734492732,-3.22275,1.66140794472856E-12));
#41231=CARTESIAN_POINT('Ctrl Pts',(-35.0027734492731,-3.21793583222462,
-0.00126067022288179));
#41232=CARTESIAN_POINT('Ctrl Pts',(-34.9745682924871,-3.21954919455613,
-0.459758487032632));
#41233=CARTESIAN_POINT('Ctrl Pts',(-34.8802054184584,-2.91361395473245,
-1.99164958121414));
#41234=CARTESIAN_POINT('Ctrl Pts',(-34.719684827187,-0.56109586298945,-3.76765932015034));
#41235=CARTESIAN_POINT('Ctrl Pts',(-34.521211675459,2.86127528031798,-2.51459521402966));
#41236=CARTESIAN_POINT('Ctrl Pts',(-34.3227385237307,3.66438340819573,1.04037471995407));
#41237=CARTESIAN_POINT('Ctrl Pts',(-34.1242653720026,1.1130488505117,3.64296686459735));
#41238=CARTESIAN_POINT('Ctrl Pts',(-33.9342770138501,-2.30456177240892,
2.9420251518518));
#41239=CARTESIAN_POINT('Ctrl Pts',(-33.8104463729402,-3.21867655106971,
0.929328322994788));
#41240=CARTESIAN_POINT('Ctrl Pts',(-33.7527734492731,-3.22601040418458,
-0.00222081755632462));
#41241=CARTESIAN_POINT('Ctrl Pts',(-34.7562265507269,-3.22628460838897,
-0.0020870326190342));
#41242=CARTESIAN_POINT('Ctrl Pts',(-34.7484182179588,-3.22723246148271,
-0.128181329246406));
#41243=CARTESIAN_POINT('Ctrl Pts',(-34.674452167948,-3.16327403099888,-1.32166548379005));
#41244=CARTESIAN_POINT('Ctrl Pts',(-34.5343284006946,-1.67542282389703,
-3.42097102935977));
#41245=CARTESIAN_POINT('Ctrl Pts',(-34.3358552489665,1.96570152728694,-3.26283648505036));
#41246=CARTESIAN_POINT('Ctrl Pts',(-34.1373820972383,3.80738723472595,-0.117842553434008));
#41247=CARTESIAN_POINT('Ctrl Pts',(-33.9389089455102,2.16372197368752,3.13502657773993));
#41248=CARTESIAN_POINT('Ctrl Pts',(-33.740435793782,-1.46065342046419,3.51803581673643));
#41249=CARTESIAN_POINT('Ctrl Pts',(-33.5962083288543,-3.12277599809849,
1.45609309127958));
#41250=CARTESIAN_POINT('Ctrl Pts',(-33.5181385811692,-3.22620124950064,
0.195379006899928));
#41251=CARTESIAN_POINT('Ctrl Pts',(-33.5062265507269,-3.22446233910715,
0.00273246397124952));
#41252=CARTESIAN_POINT('Origin',(-56.8777734492732,0.,0.));
#41253=CARTESIAN_POINT('',(-36.2527734492731,-3.22139608804363,0.00288158050599253));
#41254=CARTESIAN_POINT('',(-36.0062265507269,-3.21807312213843,-0.0014220418686986));
#41255=CARTESIAN_POINT('',(-56.8777734492732,-3.22275,1.66140794472856E-12));
#41256=CARTESIAN_POINT('Ctrl Pts',(-36.2527734492731,-3.22139608804363,
0.00288158050599251));
#41257=CARTESIAN_POINT('Ctrl Pts',(-36.2048479292767,-3.2146635292965,-0.774081151249586));
#41258=CARTESIAN_POINT('Ctrl Pts',(-36.0907646920376,-2.54241255560425,
-2.63403211011377));
#41259=CARTESIAN_POINT('Ctrl Pts',(-35.9105237375558,0.567502522785501,
-3.76669964382771));
#41260=CARTESIAN_POINT('Ctrl Pts',(-35.7120505858277,3.472497692532,-1.5658368674736));
#41261=CARTESIAN_POINT('Ctrl Pts',(-35.5135774340996,3.19870582288421,2.06842122857658));
#41262=CARTESIAN_POINT('Ctrl Pts',(-35.3151042823714,-0.00323906886257519,
3.80920921302736));
#41263=CARTESIAN_POINT('Ctrl Pts',(-35.1448362874292,-2.74760962933859,
2.31113643119006));
#41264=CARTESIAN_POINT('Ctrl Pts',(-35.0407260097298,-3.21576490894666,
0.61568913948014));
#41265=CARTESIAN_POINT('Ctrl Pts',(-35.0027734492731,-3.21793583222462,
-0.00126067022288179));
#41266=CARTESIAN_POINT('Ctrl Pts',(-36.0062265507269,-3.21807312213843,
-0.0014220418686987));
#41267=CARTESIAN_POINT('Ctrl Pts',(-35.9786978547484,-3.21985374816276,
-0.448875666670094));
#41268=CARTESIAN_POINT('Ctrl Pts',(-35.8850114415272,-2.92394127391821,
-1.96941039752039));
#41269=CARTESIAN_POINT('Ctrl Pts',(-35.7251673110634,-0.599499081901595,
-3.76173966049661));
#41270=CARTESIAN_POINT('Ctrl Pts',(-35.5266941593352,2.83547591786548,-2.54365106525228));
#41271=CARTESIAN_POINT('Ctrl Pts',(-35.3282210076071,3.67480510407022,1.0029416082971));
#41272=CARTESIAN_POINT('Ctrl Pts',(-35.1297478558789,1.15015139627886,3.6314234382941));
#41273=CARTESIAN_POINT('Ctrl Pts',(-34.9390830369189,-2.28662470261192,
2.96300846018566));
#41274=CARTESIAN_POINT('Ctrl Pts',(-34.8145759352015,-3.21920157975339,
0.940178725324924));
#41275=CARTESIAN_POINT('Ctrl Pts',(-34.7562265507269,-3.22628460838897,
-0.0020870326190342));
#41276=CARTESIAN_POINT('Origin',(-56.8777734492732,0.,0.));
#41277=CARTESIAN_POINT('',(-37.5027734492731,-3.22796415037744,-0.00044646271146332));
#41278=CARTESIAN_POINT('',(-37.2562265507269,-3.2210849165079,0.00283661979922523));
#41279=CARTESIAN_POINT('',(-56.8777734492732,-3.22275,1.66140794472856E-12));
#41280=CARTESIAN_POINT('Ctrl Pts',(-37.5027734492731,-3.22796415037744,
-0.000446462711463694));
#41281=CARTESIAN_POINT('Ctrl Pts',(-37.501285283309,-3.22801075358026,-0.0244452988629991));
#41282=CARTESIAN_POINT('Ctrl Pts',(-37.4336394001022,-3.2168973996266,-1.11528905868563));
#41283=CARTESIAN_POINT('Ctrl Pts',(-37.2998357996528,-1.99336480079335,
-3.24601018038109));
#41284=CARTESIAN_POINT('Ctrl Pts',(-37.1013626479246,1.64628397471009,-3.43508870260906));
#41285=CARTESIAN_POINT('Ctrl Pts',(-36.9028894961965,3.77889469710683,-0.479625049760291));
#41286=CARTESIAN_POINT('Ctrl Pts',(-36.7044163444683,2.45223703403194,2.9148960271512));
#41287=CARTESIAN_POINT('Ctrl Pts',(-36.5059431927402,-1.11924265385457,
3.64106868954325));
#41288=CARTESIAN_POINT('Ctrl Pts',(-36.3553955610085,-3.05114365842598,
1.66363885049783));
#41289=CARTESIAN_POINT('Ctrl Pts',(-36.2710056465194,-3.22395734015022,
0.2984597563813));
#41290=CARTESIAN_POINT('Ctrl Pts',(-36.2527734492731,-3.22139608804363,
0.00288158050599251));
#41291=CARTESIAN_POINT('Ctrl Pts',(-37.2562265507269,-3.2210849165079,0.00283661979922505));
#41292=CARTESIAN_POINT('Ctrl Pts',(-37.208977491538,-3.21459943825884,-0.763347069727803));
#41293=CARTESIAN_POINT('Ctrl Pts',(-37.0955707151064,-2.55752111380778,
-2.61233066684471));
#41294=CARTESIAN_POINT('Ctrl Pts',(-36.9160062214322,0.529050339993744,
-3.77229242772965));
#41295=CARTESIAN_POINT('Ctrl Pts',(-36.717533069704,3.45634442597985,-1.60117695198001));
#41296=CARTESIAN_POINT('Ctrl Pts',(-36.5190599179759,3.21963846421469,2.03568479443731));
#41297=CARTESIAN_POINT('Ctrl Pts',(-36.3205867662477,0.0356173628047984,
3.80904395170505));
#41298=CARTESIAN_POINT('Ctrl Pts',(-36.1496423104981,-2.73485489133519,
2.33320322322453));
#41299=CARTESIAN_POINT('Ctrl Pts',(-36.0448555719911,-3.21557449886142,
0.626457157376317));
#41300=CARTESIAN_POINT('Ctrl Pts',(-36.0062265507269,-3.21807312213843,
-0.0014220418686987));
#41301=CARTESIAN_POINT('Origin',(-56.8777734492732,0.,0.));
#41302=CARTESIAN_POINT('',(-38.7527734492731,-3.22008925450213,-0.0026026082531262));
#41303=CARTESIAN_POINT('',(-38.5062265507269,-3.22801732889799,-0.000244327765261954));
#41304=CARTESIAN_POINT('',(-56.8777734492732,-3.22275,1.66140794472856E-12));
#41305=CARTESIAN_POINT('Ctrl Pts',(-38.7527734492731,-3.22008925450213,
-0.00260260825312667));
#41306=CARTESIAN_POINT('Ctrl Pts',(-38.7315649200986,-3.22270124067416,
-0.346785967826072));
#41307=CARTESIAN_POINT('Ctrl Pts',(-38.6441986736814,-3.01333795851248,
-1.76151821125225));
#41308=CARTESIAN_POINT('Ctrl Pts',(-38.4906747100216,-0.954751856070833,
-3.68761904397796));
#41309=CARTESIAN_POINT('Ctrl Pts',(-38.2922015582933,2.58055008692402,-2.80193621787794));
#41310=CARTESIAN_POINT('Ctrl Pts',(-38.0937284065653,3.7535699214344,0.648689575284357));
#41311=CARTESIAN_POINT('Ctrl Pts',(-37.895255254837,1.4905041270395,3.50549322741577));
#41312=CARTESIAN_POINT('Ctrl Pts',(-37.6982702690731,-2.10979678019673,
3.15594586387091));
#41313=CARTESIAN_POINT('Ctrl Pts',(-37.5674430005517,-3.22593896750995,
1.04244391550343));
#41314=CARTESIAN_POINT('Ctrl Pts',(-37.5027734492731,-3.22796415037744,
-0.000446462711463694));
#41315=CARTESIAN_POINT('Ctrl Pts',(-38.5062265507269,-3.22801732889799,
-0.000244327765261728));
#41316=CARTESIAN_POINT('Ctrl Pts',(-38.5054148455703,-3.22803159826031,
-0.0133336695831677));
#41317=CARTESIAN_POINT('Ctrl Pts',(-38.438445423171,-3.22203104550765,-1.09325134200945));
#41318=CARTESIAN_POINT('Ctrl Pts',(-38.3053182835291,-2.02637231772134,
-3.22550765811006));
#41319=CARTESIAN_POINT('Ctrl Pts',(-38.1068451318009,1.6111582665074,-3.45170298009821));
#41320=CARTESIAN_POINT('Ctrl Pts',(-37.9083719800728,3.77380550466478,-0.518147117637242));
#41321=CARTESIAN_POINT('Ctrl Pts',(-37.7098988283447,2.48184309593248,2.88972996484555));
#41322=CARTESIAN_POINT('Ctrl Pts',(-37.5114256766165,-1.082043260835,3.65229610029575));
#41323=CARTESIAN_POINT('Ctrl Pts',(-37.3602015840773,-3.04278554668972,
1.6858795326344));
#41324=CARTESIAN_POINT('Ctrl Pts',(-37.2751352087807,-3.22368034788013,
0.30945659573954));
#41325=CARTESIAN_POINT('Ctrl Pts',(-37.2562265507269,-3.2210849165079,0.00283661979922505));
#41326=CARTESIAN_POINT('Origin',(-56.8777734492732,0.,0.));
#41327=CARTESIAN_POINT('',(-40.0027734492731,-3.21866195397384,0.00192812909354238));
#41328=CARTESIAN_POINT('',(-39.7562265507269,-3.2203708227658,-0.00268402097280518));
#41329=CARTESIAN_POINT('',(-56.8777734492732,-3.22275,1.66140794472856E-12));
#41330=CARTESIAN_POINT('Ctrl Pts',(-40.0027734492731,-3.21866195397384,
0.00192812909354245));
#41331=CARTESIAN_POINT('Ctrl Pts',(-39.9618445568882,-3.21503311819019,
-0.663028774388865));
#41332=CARTESIAN_POINT('Ctrl Pts',(-39.8547579472606,-2.69024800802762,
-2.40807795997689));
#41333=CARTESIAN_POINT('Ctrl Pts',(-39.6815136203903,0.16767183512014,-3.80551855545168));
#41334=CARTESIAN_POINT('Ctrl Pts',(-39.4830404686621,3.28828840795416,-1.92282205788625));
#41335=CARTESIAN_POINT('Ctrl Pts',(-39.284567316934,3.39874644404531,1.72006044349292));
#41336=CARTESIAN_POINT('Ctrl Pts',(-39.0860941652058,0.397930664244868,
3.78836858114853));
#41337=CARTESIAN_POINT('Ctrl Pts',(-38.9088295426523,-2.60756993467388,
2.53829833231303));
#41338=CARTESIAN_POINT('Ctrl Pts',(-38.7977226373413,-3.21455343178135,
0.726856866852839));
#41339=CARTESIAN_POINT('Ctrl Pts',(-38.7527734492731,-3.22008925450213,
-0.00260260825312667));
#41340=CARTESIAN_POINT('Ctrl Pts',(-39.7562265507269,-3.2203708227658,-0.00268402097280518));
#41341=CARTESIAN_POINT('Ctrl Pts',(-39.7356944823599,-3.22299454943295,
-0.335815833202966));
#41342=CARTESIAN_POINT('Ctrl Pts',(-39.6490046967502,-3.02216610517768,
-1.73926753296821));
#41343=CARTESIAN_POINT('Ctrl Pts',(-39.4961571938978,-0.992318122077262,
-3.67768801927938));
#41344=CARTESIAN_POINT('Ctrl Pts',(-39.2976840421697,2.55183428468159,-2.82811354193527));
#41345=CARTESIAN_POINT('Ctrl Pts',(-39.0992108904416,3.7599915464262,0.610367097210888));
#41346=CARTESIAN_POINT('Ctrl Pts',(-38.9007377387134,1.52618470788745,3.4901066831781));
#41347=CARTESIAN_POINT('Ctrl Pts',(-38.7030762921419,-2.08986966660851,
3.17622859575436));
#41348=CARTESIAN_POINT('Ctrl Pts',(-38.571572562813,-3.22686857936123,1.05350811141649));
#41349=CARTESIAN_POINT('Ctrl Pts',(-38.5062265507269,-3.22801732889799,
-0.000244327765261728));
#41350=CARTESIAN_POINT('Origin',(-56.8777734492732,0.,0.));
#41351=CARTESIAN_POINT('',(-41.2527734492731,-3.22710433633706,0.00156176513451752));
#41352=CARTESIAN_POINT('',(-41.0062265507269,-3.21846982119328,0.00178688758337556));
#41353=CARTESIAN_POINT('',(-56.8777734492732,-3.22275,1.66140794472856E-12));
#41354=CARTESIAN_POINT('Ctrl Pts',(-41.2527734492731,-3.22710433633706,
0.00156176513451766));
#41355=CARTESIAN_POINT('Ctrl Pts',(-41.1921241936778,-3.22126058887623,
-0.977189372262004));
#41356=CARTESIAN_POINT('Ctrl Pts',(-41.0653172208397,-2.2242198704757,-3.03389349971977));
#41357=CARTESIAN_POINT('Ctrl Pts',(-40.8723525307591,1.27537683100426,-3.58935917109407));
#41358=CARTESIAN_POINT('Ctrl Pts',(-40.6738793790308,3.70737171949489,-0.874917283901245));
#41359=CARTESIAN_POINT('Ctrl Pts',(-40.4754062273029,2.74557164665491,2.64043967044588));
#41360=CARTESIAN_POINT('Ctrl Pts',(-40.2769330755746,-0.72957424780644,
3.73869051101015));
#41361=CARTESIAN_POINT('Ctrl Pts',(-40.1193888162315,-2.95794074349924,
1.89377317364348));
#41362=CARTESIAN_POINT('Ctrl Pts',(-40.0280022741309,-3.22089879101215,
0.411811716906847));
#41363=CARTESIAN_POINT('Ctrl Pts',(-40.0027734492731,-3.21866195397384,
0.00192812909354245));
#41364=CARTESIAN_POINT('Ctrl Pts',(-41.0062265507269,-3.21846982119328,
0.00178688758337563));
#41365=CARTESIAN_POINT('Ctrl Pts',(-40.9659741191495,-3.21517429251383,
-0.652277557928967));
#41366=CARTESIAN_POINT('Ctrl Pts',(-40.8595639703294,-2.70356885076125,
-2.3860805065197));
#41367=CARTESIAN_POINT('Ctrl Pts',(-40.6869961042666,0.128844490289695,
-3.80703080101488));
#41368=CARTESIAN_POINT('Ctrl Pts',(-40.4885229525384,3.26850326385081,-1.95626451093675));
#41369=CARTESIAN_POINT('Ctrl Pts',(-40.2900498008104,3.41611517854965,1.68530160785441));
#41370=CARTESIAN_POINT('Ctrl Pts',(-40.0915766490822,0.436553624420728,
3.78411222819291));
#41371=CARTESIAN_POINT('Ctrl Pts',(-39.9136355657211,-2.59305936995176,
2.56011184016511));
#41372=CARTESIAN_POINT('Ctrl Pts',(-39.8018521996026,-3.21454046853544,
0.737589916483859));
#41373=CARTESIAN_POINT('Ctrl Pts',(-39.7562265507269,-3.2203708227658,-0.00268402097280518));
#41374=CARTESIAN_POINT('Origin',(-56.8777734492732,0.,0.));
#41375=CARTESIAN_POINT('',(-42.5027734492731,-3.223340812517,-0.00290808097893776));
#41376=CARTESIAN_POINT('',(-42.2562265507269,-3.22688342116564,0.00172679050016274));
#41377=CARTESIAN_POINT('',(-56.8777734492732,-3.22275,1.66140794472856E-12));
#41378=CARTESIAN_POINT('Ctrl Pts',(-42.5027734492731,-3.223340812517,-0.00290808097893728));
#41379=CARTESIAN_POINT('Ctrl Pts',(-42.4885615477101,-3.22546598349143,
-0.232955127105204));
#41380=CARTESIAN_POINT('Ctrl Pts',(-42.4081919289044,-3.09803786246336,
-1.53155634344338));
#41381=CARTESIAN_POINT('Ctrl Pts',(-42.261664592856,-1.33778973609199,-3.56656752945834));
#41382=CARTESIAN_POINT('Ctrl Pts',(-42.0631914411278,2.27112573740255,-3.05811595677589));
#41383=CARTESIAN_POINT('Ctrl Pts',(-41.8647182893997,3.80101173467418,0.249790138013328));
#41384=CARTESIAN_POINT('Ctrl Pts',(-41.6662451376716,1.8513830112441,3.32903383369054));
#41385=CARTESIAN_POINT('Ctrl Pts',(-41.4677719859434,-1.7930351237828,3.36081989476688));
#41386=CARTESIAN_POINT('Ctrl Pts',(-41.3299480898107,-3.18398887201866,
1.24646872161016));
#41387=CARTESIAN_POINT('Ctrl Pts',(-41.2582819109205,-3.22763509402649,
0.0904567243517276));
#41388=CARTESIAN_POINT('Ctrl Pts',(-41.2527734492731,-3.22710433633706,
0.00156176513451766));
#41389=CARTESIAN_POINT('Ctrl Pts',(-42.2562265507269,-3.22688342116564,
0.00172679050016271));
#41390=CARTESIAN_POINT('Ctrl Pts',(-42.1962537559391,-3.22061008171567,
-0.96628254910302));
#41391=CARTESIAN_POINT('Ctrl Pts',(-42.0701232439086,-2.24280389648251,
-3.01311945076458));
#41392=CARTESIAN_POINT('Ctrl Pts',(-41.8778350146354,1.2386967785751,-3.60218193784014));
#41393=CARTESIAN_POINT('Ctrl Pts',(-41.6793618629072,3.69825402795075,-0.912689195345268));
#41394=CARTESIAN_POINT('Ctrl Pts',(-41.4808887111792,2.77236281533892,2.61229570352975));
#41395=CARTESIAN_POINT('Ctrl Pts',(-41.2824155594509,-0.691399338080392,
3.7459379837173));
#41396=CARTESIAN_POINT('Ctrl Pts',(-41.1241948393002,-2.94811754240371,
1.91602372979707));
#41397=CARTESIAN_POINT('Ctrl Pts',(-41.0321318363922,-3.22059072690044,
0.42272360222518));
#41398=CARTESIAN_POINT('Ctrl Pts',(-41.0062265507269,-3.21846982119328,
0.00178688758337563));
#41399=CARTESIAN_POINT('Origin',(-56.8777734492732,0.,0.));
#41400=CARTESIAN_POINT('',(-43.7527734492731,-3.21748022116968,0.000227641132840197));
#41401=CARTESIAN_POINT('',(-43.5062265507269,-3.22367341548636,-0.0028708798850563));
#41402=CARTESIAN_POINT('',(-56.8777734492732,-3.22275,1.66140794472856E-12));
#41403=CARTESIAN_POINT('Ctrl Pts',(-43.7527734492731,-3.21748022116968,
0.000227641132840434));
#41404=CARTESIAN_POINT('Ctrl Pts',(-43.7188411844997,-3.2171325373007,-0.551564014624385));
#41405=CARTESIAN_POINT('Ctrl Pts',(-43.6187512024836,-2.82005117109617,
-2.17965269821368));
#41406=CARTESIAN_POINT('Ctrl Pts',(-43.4525035032247,-0.234023586811988,
-3.80201502903332));
#41407=CARTESIAN_POINT('Ctrl Pts',(-43.2540303514966,3.06750897389918,-2.25842290442415));
#41408=CARTESIAN_POINT('Ctrl Pts',(-43.0555571997685,3.5609884751578,1.35257029391188));
#41409=CARTESIAN_POINT('Ctrl Pts',(-42.8570840480403,0.794674878034206,
3.72539624179777));
#41410=CARTESIAN_POINT('Ctrl Pts',(-42.6728227978752,-2.44892272596741,
2.76221643248652));
#41411=CARTESIAN_POINT('Ctrl Pts',(-42.5547192649528,-3.21557311589762,
0.837935165982687));
#41412=CARTESIAN_POINT('Ctrl Pts',(-42.5027734492731,-3.223340812517,-0.00290808097893728));
#41413=CARTESIAN_POINT('Ctrl Pts',(-43.5062265507269,-3.22367341548636,
-0.00287087988505616));
#41414=CARTESIAN_POINT('Ctrl Pts',(-43.4926911099714,-3.22569286306808,
-0.22191002267826));
#41415=CARTESIAN_POINT('Ctrl Pts',(-43.4129979519732,-3.10546925677265,
-1.50935200779924));
#41416=CARTESIAN_POINT('Ctrl Pts',(-43.2671470767323,-1.3741012622493,-3.55273558594484));
#41417=CARTESIAN_POINT('Ctrl Pts',(-43.0686739250041,2.23981285336136,-3.0811236269373));
#41418=CARTESIAN_POINT('Ctrl Pts',(-42.8702007732761,3.80336187175512,0.211004490552806));
#41419=CARTESIAN_POINT('Ctrl Pts',(-42.6717276215479,1.88524481156147,3.30997529039638));
#41420=CARTESIAN_POINT('Ctrl Pts',(-42.4732544698198,-1.75865936318237,
3.37893499002941));
#41421=CARTESIAN_POINT('Ctrl Pts',(-42.3347541128794,-3.17804089141674,
1.26857508589703));
#41422=CARTESIAN_POINT('Ctrl Pts',(-42.2624114731818,-3.22753038314513,
0.10155643362859));
#41423=CARTESIAN_POINT('Ctrl Pts',(-42.2562265507269,-3.22688342116564,
0.00172679050016271));
#41424=CARTESIAN_POINT('Origin',(-56.8777734492732,0.,0.));
#41425=CARTESIAN_POINT('',(-45.0027734492731,-3.22417653578848,0.00279102537114976));
#41426=CARTESIAN_POINT('',(-44.7562265507269,-3.21746616228897,4.72427012537802E-5));
#41427=CARTESIAN_POINT('',(-56.8777734492732,-3.22275,1.66140794472856E-12));
#41428=CARTESIAN_POINT('Ctrl Pts',(-45.0027734492731,-3.22417653578848,
0.00279102537114981));
#41429=CARTESIAN_POINT('Ctrl Pts',(-44.9491208212893,-3.21625964967102,
-0.865101307677308));
#41430=CARTESIAN_POINT('Ctrl Pts',(-44.8293104760627,-2.40729031540785,
-2.81617952915074));
#41431=CARTESIAN_POINT('Ctrl Pts',(-44.6433424135935,0.890285797212397,
-3.70371118197161));
#41432=CARTESIAN_POINT('Ctrl Pts',(-44.4448692618654,3.5946178274591,-1.26047927182198));
#41433=CARTESIAN_POINT('Ctrl Pts',(-44.2463961101372,3.00837184347797,2.33661810562801));
#41434=CARTESIAN_POINT('Ctrl Pts',(-44.0479229584092,-0.331792003801605,
3.79473311135223));
#41435=CARTESIAN_POINT('Ctrl Pts',(-43.8833820714544,-2.84909864975645,
2.12369000224508));
#41436=CARTESIAN_POINT('Ctrl Pts',(-43.7849989017424,-3.21781041634141,
0.524263861358598));
#41437=CARTESIAN_POINT('Ctrl Pts',(-43.7527734492731,-3.21748022116968,
0.000227641132840434));
#41438=CARTESIAN_POINT('Ctrl Pts',(-44.7562265507269,-3.21746616228897,
4.72427012538842E-5));
#41439=CARTESIAN_POINT('Ctrl Pts',(-44.722970746761,-3.21739546247406,-0.54074993855212));
#41440=CARTESIAN_POINT('Ctrl Pts',(-44.6235572255524,-2.83168351011836,
-2.15748135685122));
#41441=CARTESIAN_POINT('Ctrl Pts',(-44.4579859871011,-0.272794281860559,
-3.79942991807168));
#41442=CARTESIAN_POINT('Ctrl Pts',(-44.2595128353729,3.04431198941514,-2.28959580137133));
#41443=CARTESIAN_POINT('Ctrl Pts',(-44.0610396836448,3.57460013936063,1.31617562135035));
#41444=CARTESIAN_POINT('Ctrl Pts',(-43.8625665319167,0.832634827927634,
3.71709613352627));
#41445=CARTESIAN_POINT('Ctrl Pts',(-43.677628820944,-2.43256230338299,2.78363876634131));
#41446=CARTESIAN_POINT('Ctrl Pts',(-43.5588488272141,-3.21582232804,0.848696390202636));
#41447=CARTESIAN_POINT('Ctrl Pts',(-43.5062265507269,-3.22367341548636,
-0.00287087988505616));
#41448=CARTESIAN_POINT('Origin',(-56.8777734492732,0.,0.));
#41449=CARTESIAN_POINT('',(-46.2527734492731,-3.22651385010114,-0.00196162169800456));
#41450=CARTESIAN_POINT('',(-46.0062265507269,-3.22384686894452,0.00284660154848987));
#41451=CARTESIAN_POINT('',(-56.8777734492732,-3.22275,1.66140794472856E-12));
#41452=CARTESIAN_POINT('Ctrl Pts',(-46.2527734492731,-3.22651385010114,
-0.00196162169800482));
#41453=CARTESIAN_POINT('Ctrl Pts',(-46.2455581753216,-3.22734896786933,
-0.118457092701875));
#41454=CARTESIAN_POINT('Ctrl Pts',(-46.1721851841273,-3.16874982256624,
-1.30226456697049));
#41455=CARTESIAN_POINT('Ctrl Pts',(-46.0326544756905,-1.70594961134342,
-3.40585103076117));
#41456=CARTESIAN_POINT('Ctrl Pts',(-45.8341813239623,1.93644344289748,-3.28028537061014));
#41457=CARTESIAN_POINT('Ctrl Pts',(-45.6357081722341,3.80618123172504,-0.151887298493708));
#41458=CARTESIAN_POINT('Ctrl Pts',(-45.4372350205061,2.19167204898115,3.11555114705157));
#41459=CARTESIAN_POINT('Ctrl Pts',(-45.2387618687778,-1.42913327008184,
3.53095786105198));
#41460=CARTESIAN_POINT('Ctrl Pts',(-45.0939413450337,-3.11653952747685,
1.47554470212732));
#41461=CARTESIAN_POINT('Ctrl Pts',(-45.015278538532,-3.22602176446174,0.205075079288332));
#41462=CARTESIAN_POINT('Ctrl Pts',(-45.0027734492731,-3.22417653578848,
0.00279102537114981));
#41463=CARTESIAN_POINT('Ctrl Pts',(-46.0062265507269,-3.22384686894453,
0.00284660154848976));
#41464=CARTESIAN_POINT('Ctrl Pts',(-45.9532503835506,-3.21596457240548,
-0.854328906569246));
#41465=CARTESIAN_POINT('Ctrl Pts',(-45.8341164991316,-2.42393033646003,
-2.79482768367397));
#41466=CARTESIAN_POINT('Ctrl Pts',(-45.6488248974699,0.852459331624162,
-3.71259983171912));
#41467=CARTESIAN_POINT('Ctrl Pts',(-45.4503517457417,3.5815730376942,-1.29708095283833));
#41468=CARTESIAN_POINT('Ctrl Pts',(-45.2518785940136,3.03205016544447,2.30580923252167));
#41469=CARTESIAN_POINT('Ctrl Pts',(-45.0534054422855,-0.29306613324189,
3.79792004445863));
#41470=CARTESIAN_POINT('Ctrl Pts',(-44.8881880945232,-2.83770608863998,
2.14587792408869));
#41471=CARTESIAN_POINT('Ctrl Pts',(-44.7891284640037,-3.21753610975382,
0.535089546179736));
#41472=CARTESIAN_POINT('Ctrl Pts',(-44.7562265507269,-3.21746616228897,
4.72427012538842E-5));
#41473=CARTESIAN_POINT('Origin',(-56.8777734492732,0.,0.));
#41474=CARTESIAN_POINT('',(-47.5027734492731,-3.2182073643014,-0.00155924202532693));
#41475=CARTESIAN_POINT('',(-47.2562265507269,-3.22676077824252,-0.00180977931619031));
#41476=CARTESIAN_POINT('',(-56.8777734492732,-3.22275,1.66140794472856E-12));
#41477=CARTESIAN_POINT('Ctrl Pts',(-47.5027734492731,-3.21820736430141,
-0.00155924202532676));
#41478=CARTESIAN_POINT('Ctrl Pts',(-47.4758378121112,-3.22012238586887,
-0.439327612385657));
#41479=CARTESIAN_POINT('Ctrl Pts',(-47.3827444577066,-2.93287246486136,
-1.94990972203441));
#41480=CARTESIAN_POINT('Ctrl Pts',(-47.2234933860592,-0.633116354570043,
-3.75622802845598));
#41481=CARTESIAN_POINT('Ctrl Pts',(-47.025020234331,2.81261475191178,-2.56890707841041));
#41482=CARTESIAN_POINT('Ctrl Pts',(-46.826547082603,3.68362756861194,0.970037760059602));
#41483=CARTESIAN_POINT('Ctrl Pts',(-46.6280739308748,1.18258124809755,3.62099253131349));
#41484=CARTESIAN_POINT('Ctrl Pts',(-46.4368160530982,-2.27074334009362,
2.98135593498794));
#41485=CARTESIAN_POINT('Ctrl Pts',(-46.3117158925643,-3.2196916723122,0.949703933825722));
#41486=CARTESIAN_POINT('Ctrl Pts',(-46.2527734492731,-3.22651385010114,
-0.00196162169800482));
#41487=CARTESIAN_POINT('Ctrl Pts',(-47.2562265507269,-3.22676077824252,
-0.00180977931619085));
#41488=CARTESIAN_POINT('Ctrl Pts',(-47.2496877375829,-3.22747103515158,
-0.10736207527441));
#41489=CARTESIAN_POINT('Ctrl Pts',(-47.1769912071962,-3.17488133388419,
-1.28014382472976));
#41490=CARTESIAN_POINT('Ctrl Pts',(-47.0381369595668,-1.74060256508747,
-3.38827199807887));
#41491=CARTESIAN_POINT('Ctrl Pts',(-46.8396638078386,1.90288171805956,-3.29986751092048));
#41492=CARTESIAN_POINT('Ctrl Pts',(-46.6411906561105,3.80443374423865,-0.190704767250943));
#41493=CARTESIAN_POINT('Ctrl Pts',(-46.4427175043824,2.22333848041998,3.09303256110211));
#41494=CARTESIAN_POINT('Ctrl Pts',(-46.2442443526542,-1.39304094239042,
3.54535207777422));
#41495=CARTESIAN_POINT('Ctrl Pts',(-46.0987473681024,-3.10930527441843,
1.49773850278433));
#41496=CARTESIAN_POINT('Ctrl Pts',(-46.0194081007933,-3.22580814496742,
0.21612933750686));
#41497=CARTESIAN_POINT('Ctrl Pts',(-46.0062265507269,-3.22384686894453,
0.00284660154848976));
#41498=CARTESIAN_POINT('Origin',(-56.8777734492732,0.,0.));
#41499=CARTESIAN_POINT('',(-48.7527734492731,-3.22081842851865,0.00278806351307224));
#41500=CARTESIAN_POINT('',(-48.5062265507269,-3.21837549758788,-0.00171032771080215));
#41501=CARTESIAN_POINT('',(-56.8777734492732,-3.22275,1.66140794472856E-12));
#41502=CARTESIAN_POINT('Ctrl Pts',(-48.7527734492731,-3.22081842851865,
0.00278806351307209));
#41503=CARTESIAN_POINT('Ctrl Pts',(-48.7061174489008,-3.21456284440464,
-0.75393734371017));
#41504=CARTESIAN_POINT('Ctrl Pts',(-48.5933037312858,-2.57062144258657,
-2.59327646914024));
#41505=CARTESIAN_POINT('Ctrl Pts',(-48.414332296428,0.495293598847041,-3.77687298849846));
#41506=CARTESIAN_POINT('Ctrl Pts',(-48.2158591446999,3.44188699455041,-1.63202305036004));
#41507=CARTESIAN_POINT('Ctrl Pts',(-48.0173859929717,3.23771493607145,2.00681023340388));
#41508=CARTESIAN_POINT('Ctrl Pts',(-47.8189128412436,0.0696802094731201,
3.80857322216686));
#41509=CARTESIAN_POINT('Ctrl Pts',(-47.6473753266774,-2.72353680500992,
2.35253380852171));
#41510=CARTESIAN_POINT('Ctrl Pts',(-47.5419955293539,-3.21541882327584,
0.635893140329142));
#41511=CARTESIAN_POINT('Ctrl Pts',(-47.5027734492731,-3.21820736430141,
-0.00155924202532676));
#41512=CARTESIAN_POINT('Ctrl Pts',(-48.5062265507269,-3.21837549758788,
-0.0017103277108025));
#41513=CARTESIAN_POINT('Ctrl Pts',(-48.4799673743725,-3.22042966490226,
-0.428428751773469));
#41514=CARTESIAN_POINT('Ctrl Pts',(-48.3875504807753,-2.94292001229825,
-1.92766318074928));
#41515=CARTESIAN_POINT('Ctrl Pts',(-48.2289758699356,-0.671399218037883,
-3.74957431085067));
#41516=CARTESIAN_POINT('Ctrl Pts',(-48.0305027182074,2.78626390843014,-2.59746373509423));
#41517=CARTESIAN_POINT('Ctrl Pts',(-47.8320295664793,3.69333078266646,0.932412007837439));
#41518=CARTESIAN_POINT('Ctrl Pts',(-47.6335564147512,1.21945602247574,3.6087409759921));
#41519=CARTESIAN_POINT('Ctrl Pts',(-47.441622076167,-2.25244999498725,3.00222607590046));
#41520=CARTESIAN_POINT('Ctrl Pts',(-47.3158454548256,-3.22028487235349,
0.960583864842949));
#41521=CARTESIAN_POINT('Ctrl Pts',(-47.2562265507269,-3.22676077824252,
-0.00180977931619085));
#41522=CARTESIAN_POINT('Origin',(-56.8777734492732,0.,0.));
#41523=CARTESIAN_POINT('',(-50.0027734492731,-3.2280388681347,-6.59018652397875E-5));
#41524=CARTESIAN_POINT('',(-49.7562265507269,-3.2205221309114,0.00272251988370595));
#41525=CARTESIAN_POINT('',(-56.8777734492732,-3.22275,1.66140794472856E-12));
#41526=CARTESIAN_POINT('Ctrl Pts',(-50.0027734492731,-3.2280388681347,-6.59018652398626E-5));
#41527=CARTESIAN_POINT('Ctrl Pts',(-50.0025548029331,-3.22803992941049,
-0.00359167159406266));
#41528=CARTESIAN_POINT('Ctrl Pts',(-49.9361784393503,-3.22643794640511,
-1.07393913886435));
#41529=CARTESIAN_POINT('Ctrl Pts',(-49.8036443585249,-2.05513705304844,
-3.20725692790933));
#41530=CARTESIAN_POINT('Ctrl Pts',(-49.6051712067968,1.58022531640166,-3.46597364026232));
#41531=CARTESIAN_POINT('Ctrl Pts',(-49.4066980550686,3.7690209209745,-0.551875545371135));
#41532=CARTESIAN_POINT('Ctrl Pts',(-49.2082249033405,2.50758677259566,2.8674193792543));
#41533=CARTESIAN_POINT('Ctrl Pts',(-49.0097517516124,-1.04933754975442,
3.66182687025214));
#41534=CARTESIAN_POINT('Ctrl Pts',(-48.8579346002566,-3.03534529000393,
1.70538112699385));
#41535=CARTESIAN_POINT('Ctrl Pts',(-48.7722751661435,-3.22343319680733,
0.319091315453159));
#41536=CARTESIAN_POINT('Ctrl Pts',(-48.7527734492731,-3.22081842851865,
0.00278806351307209));
#41537=CARTESIAN_POINT('Ctrl Pts',(-49.7562265507269,-3.2205221309114,0.00272251988370574));
#41538=CARTESIAN_POINT('Ctrl Pts',(-49.7102470111621,-3.21454231443744,
-0.743204705410713));
#41539=CARTESIAN_POINT('Ctrl Pts',(-49.5981097543545,-2.5853985811797,-2.57151118715912));
#41540=CARTESIAN_POINT('Ctrl Pts',(-49.4198147803043,0.456741400770442,
-3.78172866771592));
#41541=CARTESIAN_POINT('Ctrl Pts',(-49.2213416285762,3.42506018203235,-1.66704744142366));
#41542=CARTESIAN_POINT('Ctrl Pts',(-49.022868476848,3.25801707681289,1.97367908980867));
#41543=CARTESIAN_POINT('Ctrl Pts',(-48.82439532512,0.108526357580573,3.80766417274334));
#41544=CARTESIAN_POINT('Ctrl Pts',(-48.6521813497462,-2.71047082998708,
2.37456382570328));
#41545=CARTESIAN_POINT('Ctrl Pts',(-48.5461250916152,-3.21525436852128,
0.646651306350763));
#41546=CARTESIAN_POINT('Ctrl Pts',(-48.5062265507269,-3.21837549758788,
-0.0017103277108025));
#41547=CARTESIAN_POINT('Origin',(-56.8777734492732,0.,0.));
#41548=CARTESIAN_POINT('',(-51.2527734492731,-3.22062593581149,-0.00274689833755447));
#41549=CARTESIAN_POINT('',(-51.0062265507269,-3.22803304482756,0.000137933179436404));
#41550=CARTESIAN_POINT('',(-56.8777734492732,-3.22275,1.66140794472856E-12));
#41551=CARTESIAN_POINT('Ctrl Pts',(-51.2527734492731,-3.22062593581149,
-0.00274689833755396));
#41552=CARTESIAN_POINT('Ctrl Pts',(-51.2328344397227,-3.22324839602356,
-0.326191645141541));
#41553=CARTESIAN_POINT('Ctrl Pts',(-51.1467377129296,-3.0297912547185,-1.71976224857695));
#41554=CARTESIAN_POINT('Ctrl Pts',(-50.9944832688937,-1.02516800960105,
-3.66866668622662));
#41555=CARTESIAN_POINT('Ctrl Pts',(-50.7960101171655,2.52644049755188,-2.85082162384731));
#41556=CARTESIAN_POINT('Ctrl Pts',(-50.5975369654374,3.76529981837076,0.576717135381059));
#41557=CARTESIAN_POINT('Ctrl Pts',(-50.3990638137093,1.55733573647028,3.47631854666922));
#41558=CARTESIAN_POINT('Ctrl Pts',(-50.2008093083212,-2.07223866782462,
3.1939466957081));
#41559=CARTESIAN_POINT('Ctrl Pts',(-50.0687125201758,-3.22771881000176,
1.06323101909589));
#41560=CARTESIAN_POINT('Ctrl Pts',(-50.0027734492731,-3.2280388681347,-6.59018652398626E-5));
#41561=CARTESIAN_POINT('Ctrl Pts',(-51.0062265507269,-3.22803304482756,
0.000137933179436442));
#41562=CARTESIAN_POINT('Ctrl Pts',(-50.9405266479517,-3.2273719077905,-1.05930734273043));
#41563=CARTESIAN_POINT('Ctrl Pts',(-50.8086690279337,-2.07936694243932,
-3.18680858367589));
#41564=CARTESIAN_POINT('Ctrl Pts',(-50.6106536906731,1.54478799997451,-3.48191247610533));
#41565=CARTESIAN_POINT('Ctrl Pts',(-50.412180538945,3.76319524430468,-0.590293130886969));
#41566=CARTESIAN_POINT('Ctrl Pts',(-50.2137073872169,2.53670566171588,2.84169118600161));
#41567=CARTESIAN_POINT('Ctrl Pts',(-50.0152342354887,-1.01193004948523,
3.67234012625855));
#41568=CARTESIAN_POINT('Ctrl Pts',(-49.8627406233254,-3.02672898098561,
1.72762799301611));
#41569=CARTESIAN_POINT('Ctrl Pts',(-49.7764047284048,-3.22314638075024,
0.330073603196574));
#41570=CARTESIAN_POINT('Ctrl Pts',(-49.7562265507269,-3.2205221309114,0.00272251988370574));
#41571=CARTESIAN_POINT('Origin',(-56.8777734492732,0.,0.));
#41572=CARTESIAN_POINT('',(-52.5027734492731,-3.21831359885928,0.00166126316387731));
#41573=CARTESIAN_POINT('',(-52.2562265507269,-3.22092507366678,-0.00280858089474589));
#41574=CARTESIAN_POINT('',(-56.8777734492732,-3.22275,1.66140794472856E-12));
#41575=CARTESIAN_POINT('Ctrl Pts',(-52.5027734492731,-3.21831359885928,
0.00166126316387728));
#41576=CARTESIAN_POINT('Ctrl Pts',(-52.4631140765123,-3.21531050958603,
-0.642846125141404));
#41577=CARTESIAN_POINT('Ctrl Pts',(-52.3572969865087,-2.71511064840447,
-2.36678331187106));
#41578=CARTESIAN_POINT('Ctrl Pts',(-52.1853221792625,0.0947938145258543,
-3.80802701948498));
#41579=CARTESIAN_POINT('Ctrl Pts',(-51.9868490275343,3.25087740482292,-1.98541860413584));
#41580=CARTESIAN_POINT('Ctrl Pts',(-51.7883758758062,3.43105052559699,1.65468502690142));
#41581=CARTESIAN_POINT('Ctrl Pts',(-51.5899027240781,0.47037738033959,3.78005636351393));
#41582=CARTESIAN_POINT('Ctrl Pts',(-51.4113685819003,-2.58019410180226,
2.57921047192559));
#41583=CARTESIAN_POINT('Ctrl Pts',(-51.2989921569654,-3.2145470620505,0.746999380148212));
#41584=CARTESIAN_POINT('Ctrl Pts',(-51.2527734492731,-3.22062593581149,
-0.00274689833755396));
#41585=CARTESIAN_POINT('Ctrl Pts',(-52.2562265507269,-3.22092507366678,
-0.00280858089474579));
#41586=CARTESIAN_POINT('Ctrl Pts',(-52.236964001984,-3.22353331455023,-0.31520661263699));
#41587=CARTESIAN_POINT('Ctrl Pts',(-52.1515437359983,-3.03835869510582,
-1.69751686651351));
#41588=CARTESIAN_POINT('Ctrl Pts',(-51.99996575277,-1.06253710715876,-3.65801790350669));
#41589=CARTESIAN_POINT('Ctrl Pts',(-51.8014926010418,2.49722875856415,-2.87644469098565));
#41590=CARTESIAN_POINT('Ctrl Pts',(-51.6030194493138,3.77098671823784,0.538278876876041));
#41591=CARTESIAN_POINT('Ctrl Pts',(-51.4045462975856,1.59271521326821,3.46025173262707));
#41592=CARTESIAN_POINT('Ctrl Pts',(-51.2060731458574,-2.04355643697909,
3.21464799167866));
#41593=CARTESIAN_POINT('Ctrl Pts',(-51.0732998969046,-3.22467120902133,
1.08172637814565));
#41594=CARTESIAN_POINT('Ctrl Pts',(-51.0066843651944,-3.22803765180699,
0.0075204307834513));
#41595=CARTESIAN_POINT('Ctrl Pts',(-51.0062265507269,-3.22803304482756,
0.000137933179436442));
#41596=CARTESIAN_POINT('Origin',(-56.8777734492732,0.,0.));
#41597=CARTESIAN_POINT('',(-53.7527734492731,-3.22663436289375,0.00208142861643813));
#41598=CARTESIAN_POINT('',(-53.5062265507269,-3.21814301605221,0.00152842760642868));
#41599=CARTESIAN_POINT('',(-56.8777734492732,-3.22275,1.66140794472856E-12));
#41600=CARTESIAN_POINT('Ctrl Pts',(-53.7527734492731,-3.22663436289375,
0.00208142861643813));
#41601=CARTESIAN_POINT('Ctrl Pts',(-53.6933937133019,-3.22001905440489,
-0.956459817829004));
#41602=CARTESIAN_POINT('Ctrl Pts',(-53.5678562600879,-2.25900515456935,
-2.99520192780961));
#41603=CARTESIAN_POINT('Ctrl Pts',(-53.3761610896312,1.20646915281294,-3.61292403145259));
#41604=CARTESIAN_POINT('Ctrl Pts',(-53.1776879379031,3.68992516100066,-0.945826390348501));
#41605=CARTESIAN_POINT('Ctrl Pts',(-52.979214786175,2.79562367813024,2.58745046926129));
#41606=CARTESIAN_POINT('Ctrl Pts',(-52.7807416344468,-0.657876967632621,
3.75194409668105));
#41607=CARTESIAN_POINT('Ctrl Pts',(-52.6219278554796,-2.93938347591651,
1.93553501403558));
#41608=CARTESIAN_POINT('Ctrl Pts',(-52.529271793755,-3.22032010800284,0.432287811380001));
#41609=CARTESIAN_POINT('Ctrl Pts',(-52.5027734492731,-3.21831359885928,
0.00166126316387728));
#41610=CARTESIAN_POINT('Ctrl Pts',(-53.5062265507269,-3.21814301605221,
0.00152842760642868));
#41611=CARTESIAN_POINT('Ctrl Pts',(-53.4672436387736,-3.21547541045439,
-0.632074783174344));
#41612=CARTESIAN_POINT('Ctrl Pts',(-53.3621030095775,-2.72813073009025,
-2.34477970215022));
#41613=CARTESIAN_POINT('Ctrl Pts',(-53.1908046631388,0.055953337280497,
-3.80877338647033));
#41614=CARTESIAN_POINT('Ctrl Pts',(-52.9923315114106,3.23045115613742,-2.01848786902524));
#41615=CARTESIAN_POINT('Ctrl Pts',(-52.7938583596826,3.44775307743432,1.61960618367426));
#41616=CARTESIAN_POINT('Ctrl Pts',(-52.5953852079543,0.508910540986547,
3.77505824730967));
#41617=CARTESIAN_POINT('Ctrl Pts',(-52.4161746049693,-2.56535413208167,
2.60096512785637));
#41618=CARTESIAN_POINT('Ctrl Pts',(-52.3031217192267,-3.21457524440225,
0.757732432294889));
#41619=CARTESIAN_POINT('Ctrl Pts',(-52.2562265507269,-3.22092507366678,
-0.00280858089474579));
#41620=CARTESIAN_POINT('Ctrl Pts',(-54.9770630286919,-1.43290239521256,
2.88667772504901));
#41621=CARTESIAN_POINT('Ctrl Pts',(-54.9109053114492,-2.3928525167459,2.41017325886154));
#41622=CARTESIAN_POINT('Ctrl Pts',(-54.7785898769638,-3.7834146058807,0.432460660303072));
#41623=CARTESIAN_POINT('Ctrl Pts',(-54.5801167252357,-2.41256151508884,
-2.9510558129106));
#41624=CARTESIAN_POINT('Ctrl Pts',(-54.3816435735076,1.16997685241348,-3.6239435622357));
#41625=CARTESIAN_POINT('Ctrl Pts',(-54.1831704217794,3.67986340215961,-0.983988949453548));
#41626=CARTESIAN_POINT('Ctrl Pts',(-53.9846972700513,2.8219875869866,2.55909768807962));
#41627=CARTESIAN_POINT('Ctrl Pts',(-53.7862241183231,-0.619631178725218,
3.75830321175399));
#41628=CARTESIAN_POINT('Ctrl Pts',(-53.587750966595,-3.49379594847047,1.51773663572276));
#41629=CARTESIAN_POINT('Ctrl Pts',(-53.3892778148669,-3.16979840530699,
-2.1125314397275));
#41630=CARTESIAN_POINT('Ctrl Pts',(-53.1908046631388,0.055953337280497,
-3.80877338647033));
#41631=CARTESIAN_POINT('Ctrl Pts',(-52.9923315114106,3.23045115613742,-2.01848786902524));
#41632=CARTESIAN_POINT('Ctrl Pts',(-52.7938583596826,3.44775307743432,1.61960618367426));
#41633=CARTESIAN_POINT('Ctrl Pts',(-52.5953852079543,0.508910540986547,
3.77505824730967));
#41634=CARTESIAN_POINT('Ctrl Pts',(-52.3969120562264,-2.89579313584141,
2.47476709288819));
#41635=CARTESIAN_POINT('Ctrl Pts',(-52.1984389044981,-3.64963801363799,
-1.09097741721031));
#41636=CARTESIAN_POINT('Ctrl Pts',(-51.99996575277,-1.06253710715876,-3.65801790350669));
#41637=CARTESIAN_POINT('Ctrl Pts',(-51.8014926010418,2.49722875856415,-2.87644469098565));
#41638=CARTESIAN_POINT('Ctrl Pts',(-51.6030194493138,3.77098671823784,0.538278876876041));
#41639=CARTESIAN_POINT('Ctrl Pts',(-51.4045462975856,1.59271521326821,3.46025173262707));
#41640=CARTESIAN_POINT('Ctrl Pts',(-51.2060731458574,-2.04355643697909,
3.21464799167866));
#41641=CARTESIAN_POINT('Ctrl Pts',(-51.0075999941294,-3.80911970524725,
0.0262973384752155));
#41642=CARTESIAN_POINT('Ctrl Pts',(-50.8091268424012,-2.08774604371503,
-3.18612629899413));
#41643=CARTESIAN_POINT('Ctrl Pts',(-50.6106536906731,1.54478799997451,-3.48191247610533));
#41644=CARTESIAN_POINT('Ctrl Pts',(-50.412180538945,3.76319524430468,-0.590293130886969));
#41645=CARTESIAN_POINT('Ctrl Pts',(-50.2137073872169,2.53670566171588,2.84169118600161));
#41646=CARTESIAN_POINT('Ctrl Pts',(-50.0152342354887,-1.01193004948523,
3.67234012625855));
#41647=CARTESIAN_POINT('Ctrl Pts',(-49.8167610837606,-3.63422673693658,
1.14126265479567));
#41648=CARTESIAN_POINT('Ctrl Pts',(-49.6182879320324,-2.92968669924813,
-2.43454724029718));
#41649=CARTESIAN_POINT('Ctrl Pts',(-49.4198147803043,0.456741400770442,
-3.78172866771592));
#41650=CARTESIAN_POINT('Ctrl Pts',(-49.2213416285762,3.42506018203235,-1.66704744142366));
#41651=CARTESIAN_POINT('Ctrl Pts',(-49.022868476848,3.25801707681289,1.97367908980867));
#41652=CARTESIAN_POINT('Ctrl Pts',(-48.82439532512,0.108526357580573,3.80766417274334));
#41653=CARTESIAN_POINT('Ctrl Pts',(-48.6259221733918,-3.14031134746123,
2.15604477308386));
#41654=CARTESIAN_POINT('Ctrl Pts',(-48.4274490216636,-3.5144513867625,-1.46925691171152));
#41655=CARTESIAN_POINT('Ctrl Pts',(-48.2289758699356,-0.671399218037883,
-3.74957431085067));
#41656=CARTESIAN_POINT('Ctrl Pts',(-48.0305027182074,2.78626390843014,-2.59746373509423));
#41657=CARTESIAN_POINT('Ctrl Pts',(-47.8320295664793,3.69333078266646,0.932412007837439));
#41658=CARTESIAN_POINT('Ctrl Pts',(-47.6335564147512,1.21945602247574,3.6087409759921));
#41659=CARTESIAN_POINT('Ctrl Pts',(-47.435083263023,-2.37073078241276,2.98156334493733));
#41660=CARTESIAN_POINT('Ctrl Pts',(-47.2366101112949,-3.79070785577725,
-0.374991166165694));
#41661=CARTESIAN_POINT('Ctrl Pts',(-47.0381369595668,-1.74060256508747,
-3.38827199807887));
#41662=CARTESIAN_POINT('Ctrl Pts',(-46.8396638078386,1.90288171805956,-3.29986751092048));
#41663=CARTESIAN_POINT('Ctrl Pts',(-46.6411906561105,3.80443374423865,-0.190704767250943));
#41664=CARTESIAN_POINT('Ctrl Pts',(-46.4427175043824,2.22333848041998,3.09303256110211));
#41665=CARTESIAN_POINT('Ctrl Pts',(-46.2442443526542,-1.39304094239042,
3.54535207777422));
#41666=CARTESIAN_POINT('Ctrl Pts',(-46.0457712009261,-3.7342055529521,0.752192336344735));
#41667=CARTESIAN_POINT('Ctrl Pts',(-45.847298049198,-2.65701102689385,-2.72953784101238));
#41668=CARTESIAN_POINT('Ctrl Pts',(-45.6488248974699,0.852459331624162,
-3.71259983171912));
#41669=CARTESIAN_POINT('Ctrl Pts',(-45.4503517457417,3.5815730376942,-1.29708095283833));
#41670=CARTESIAN_POINT('Ctrl Pts',(-45.2518785940136,3.03205016544447,2.30580923252167));
#41671=CARTESIAN_POINT('Ctrl Pts',(-45.0534054422855,-0.29306613324189,
3.79792004445863));
#41672=CARTESIAN_POINT('Ctrl Pts',(-44.8549322905573,-3.34990440598796,
1.8133463246982));
#41673=CARTESIAN_POINT('Ctrl Pts',(-44.6564591388292,-3.34017974570013,
-1.83119733752774));
#41674=CARTESIAN_POINT('Ctrl Pts',(-44.4579859871011,-0.272794281860559,
-3.79942991807168));
#41675=CARTESIAN_POINT('Ctrl Pts',(-44.2595128353729,3.04431198941514,-2.28959580137133));
#41676=CARTESIAN_POINT('Ctrl Pts',(-44.0610396836448,3.57460013936063,1.31617562135035));
#41677=CARTESIAN_POINT('Ctrl Pts',(-43.8625665319167,0.832634827927634,
3.71709613352627));
#41678=CARTESIAN_POINT('Ctrl Pts',(-43.6640933801885,-2.671539427591,2.71531978031699));
#41679=CARTESIAN_POINT('Ctrl Pts',(-43.4656202284604,-3.73013829052675,
-0.772109290256342));
#41680=CARTESIAN_POINT('Ctrl Pts',(-43.2671470767323,-1.3741012622493,-3.55273558594484));
#41681=CARTESIAN_POINT('Ctrl Pts',(-43.0686739250041,2.23981285336136,-3.0811236269373));
#41682=CARTESIAN_POINT('Ctrl Pts',(-42.8702007732761,3.80336187175512,0.211004490552806));
#41683=CARTESIAN_POINT('Ctrl Pts',(-42.6717276215479,1.88524481156147,3.30997529039638));
#41684=CARTESIAN_POINT('Ctrl Pts',(-42.4732544698198,-1.75865936318237,
3.37893499002941));
#41685=CARTESIAN_POINT('Ctrl Pts',(-42.2747813180916,-3.79265502670778,
0.354756636220095));
#41686=CARTESIAN_POINT('Ctrl Pts',(-42.0763081663635,-2.35478585077766,
-2.99417234299084));
#41687=CARTESIAN_POINT('Ctrl Pts',(-41.8778350146354,1.2386967785751,-3.60218193784014));
#41688=CARTESIAN_POINT('Ctrl Pts',(-41.6793618629072,3.69825402795075,-0.912689195345268));
#41689=CARTESIAN_POINT('Ctrl Pts',(-41.4808887111792,2.77236281533892,2.61229570352975));
#41690=CARTESIAN_POINT('Ctrl Pts',(-41.2824155594509,-0.691399338080392,
3.7459379837173));
#41691=CARTESIAN_POINT('Ctrl Pts',(-41.0839424077229,-3.52224206302542,
1.45048104848306));
#41692=CARTESIAN_POINT('Ctrl Pts',(-40.8854692559947,-3.12876085432636,
-2.17277240846552));
#41693=CARTESIAN_POINT('Ctrl Pts',(-40.6869961042666,0.128844490289695,
-3.80703080101488));
#41694=CARTESIAN_POINT('Ctrl Pts',(-40.4885229525384,3.26850326385081,-1.95626451093675));
#41695=CARTESIAN_POINT('Ctrl Pts',(-40.2900498008104,3.41611517854965,1.68530160785441));
#41696=CARTESIAN_POINT('Ctrl Pts',(-40.0915766490822,0.436553624420728,
3.78411222819291));
#41697=CARTESIAN_POINT('Ctrl Pts',(-39.8931034973541,-2.94263699390992,
2.41887824096765));
#41698=CARTESIAN_POINT('Ctrl Pts',(-39.694630345626,-3.62808461624092,-1.1606405300307));
#41699=CARTESIAN_POINT('Ctrl Pts',(-39.4961571938978,-0.992318122077262,
-3.67768801927938));
#41700=CARTESIAN_POINT('Ctrl Pts',(-39.2976840421697,2.55183428468159,-2.82811354193527));
#41701=CARTESIAN_POINT('Ctrl Pts',(-39.0992108904416,3.7599915464262,0.610367097210888));
#41702=CARTESIAN_POINT('Ctrl Pts',(-38.9007377387134,1.52618470788745,3.4901066831781));
#41703=CARTESIAN_POINT('Ctrl Pts',(-38.7022645869853,-2.10471914804825,
3.17493964200786));
#41704=CARTESIAN_POINT('Ctrl Pts',(-38.5037914352571,-3.80892512200428,
-0.0466244304919306));
#41705=CARTESIAN_POINT('Ctrl Pts',(-38.3053182835291,-2.02637231772134,
-3.22550765811006));
#41706=CARTESIAN_POINT('Ctrl Pts',(-38.1068451318009,1.6111582665074,-3.45170298009821));
#41707=CARTESIAN_POINT('Ctrl Pts',(-37.9083719800728,3.77380550466478,-0.518147117637242));
#41708=CARTESIAN_POINT('Ctrl Pts',(-37.7098988283447,2.48184309593248,2.88972996484555));
#41709=CARTESIAN_POINT('Ctrl Pts',(-37.5114256766165,-1.082043260835,3.65229610029575));
#41710=CARTESIAN_POINT('Ctrl Pts',(-37.3129525248884,-3.65540769414567,
1.07148448991797));
#41711=CARTESIAN_POINT('Ctrl Pts',(-37.1144793731602,-2.88254597247797,
-2.49018335451532));
#41712=CARTESIAN_POINT('Ctrl Pts',(-36.9160062214322,0.529050339993744,
-3.77229242772965));
#41713=CARTESIAN_POINT('Ctrl Pts',(-36.717533069704,3.45634442597985,-1.60117695198001));
#41714=CARTESIAN_POINT('Ctrl Pts',(-36.5190599179759,3.21963846421469,2.03568479443731));
#41715=CARTESIAN_POINT('Ctrl Pts',(-36.3205867662477,0.0356173628047984,
3.80904395170505));
#41716=CARTESIAN_POINT('Ctrl Pts',(-36.1221136145196,-3.18100851513376,
2.09553555188179));
#41717=CARTESIAN_POINT('Ctrl Pts',(-35.9236404627915,-3.48568180578722,
-1.53626390029769));
#41718=CARTESIAN_POINT('Ctrl Pts',(-35.7251673110634,-0.599499081901595,
-3.76173966049661));
#41719=CARTESIAN_POINT('Ctrl Pts',(-35.5266941593352,2.83547591786548,-2.54365106525228));
#41720=CARTESIAN_POINT('Ctrl Pts',(-35.3282210076071,3.67480510407022,1.0029416082971));
#41721=CARTESIAN_POINT('Ctrl Pts',(-35.1297478558789,1.15015139627886,3.6314234382941));
#41722=CARTESIAN_POINT('Ctrl Pts',(-34.9312747041509,-2.42737165097821,
2.9356347338491));
#41723=CARTESIAN_POINT('Ctrl Pts',(-34.7328015524227,-3.78283489369835,
-0.447486971399394));
#41724=CARTESIAN_POINT('Ctrl Pts',(-34.5343284006946,-1.67542282389703,
-3.42097102935977));
#41725=CARTESIAN_POINT('Ctrl Pts',(-34.3358552489665,1.96570152728694,-3.26283648505036));
#41726=CARTESIAN_POINT('Ctrl Pts',(-34.1373820972383,3.80738723472595,-0.117842553434008));
#41727=CARTESIAN_POINT('Ctrl Pts',(-33.9389089455102,2.16372197368752,3.13502657773993));
#41728=CARTESIAN_POINT('Ctrl Pts',(-33.740435793782,-1.46065342046419,3.51803581673643));
#41729=CARTESIAN_POINT('Ctrl Pts',(-33.541962642054,-3.74792032005764,0.680571595831895));
#41730=CARTESIAN_POINT('Ctrl Pts',(-33.3434894903258,-2.60427333777752,
-2.77990014293592));
#41731=CARTESIAN_POINT('Ctrl Pts',(-33.1450163385977,0.923372444839,-3.6956011352236));
#41732=CARTESIAN_POINT('Ctrl Pts',(-32.9465431868696,3.60574643173899,-1.22828217139039));
#41733=CARTESIAN_POINT('Ctrl Pts',(-32.7480700351414,2.98735507926837,2.36342845310018));
#41734=CARTESIAN_POINT('Ctrl Pts',(-32.5495968834133,-0.365715011353638,
3.79161403007012));
#41735=CARTESIAN_POINT('Ctrl Pts',(-32.3511237316851,-3.38400298226306,
1.74888771468858));
#41736=CARTESIAN_POINT('Ctrl Pts',(-32.152650579957,-3.30451356820155,-1.89480196857768));
#41737=CARTESIAN_POINT('Ctrl Pts',(-31.9541774282289,-0.200012812968363,
-3.80395574332859));
#41738=CARTESIAN_POINT('Ctrl Pts',(-31.7557042765008,3.08758327993605,-2.23089979873894));
#41739=CARTESIAN_POINT('Ctrl Pts',(-31.5572311247726,3.54874993145618,1.38436207205476));
#41740=CARTESIAN_POINT('Ctrl Pts',(-31.3587579730445,0.761326868309329,
3.73235392509128));
#41741=CARTESIAN_POINT('Ctrl Pts',(-31.1602848213164,-2.72302854613296,
2.66368165505921));
#41742=CARTESIAN_POINT('Ctrl Pts',(-30.9618116695882,-3.71467449989982,
-0.843372860808289));
#41743=CARTESIAN_POINT('Ctrl Pts',(-30.7633385178601,-1.30584039539486,
-3.57838864355298));
#41744=CARTESIAN_POINT('Ctrl Pts',(-30.5648653661319,2.29838356734553,-3.03768289982842));
#41745=CARTESIAN_POINT('Ctrl Pts',(-30.3663922144039,3.79862574454081,0.283772577015008));
#41746=CARTESIAN_POINT('Ctrl Pts',(-30.1679190626757,1.82153737945105,3.34545751696486));
#41747=CARTESIAN_POINT('Ctrl Pts',(-29.9694459109477,-1.82301916741003,
3.34465028632439));
#41748=CARTESIAN_POINT('Ctrl Pts',(-29.7709727592194,-3.79875107706736,
0.282089838586104));
#41749=CARTESIAN_POINT('Ctrl Pts',(-29.5724996074914,-2.29703771278357,
-3.03870073692754));
#41750=CARTESIAN_POINT('Ctrl Pts',(-29.3740264557631,1.30742541749708,-3.57780983287773));
#41751=CARTESIAN_POINT('Ctrl Pts',(-29.1755533040351,3.71504773171258,-0.841727256093824));
#41752=CARTESIAN_POINT('Ctrl Pts',(-28.9770801523069,2.72184832452091,2.66488763756686));
#41753=CARTESIAN_POINT('Ctrl Pts',(-28.7786070005788,-0.762980147188692,
3.732016307246));
#41754=CARTESIAN_POINT('Ctrl Pts',(-28.5801338488507,-3.54936282628784,
1.38278991532342));
#41755=CARTESIAN_POINT('Ctrl Pts',(-28.3816606971225,-3.08659473573302,
-2.2322673137192));
#41756=CARTESIAN_POINT('Ctrl Pts',(-28.1831875453944,0.201697865006982,
-3.80386676867179));
#41757=CARTESIAN_POINT('Ctrl Pts',(-27.9847143936663,3.30535260103752,-1.89333795329003));
#41758=CARTESIAN_POINT('Ctrl Pts',(-27.7862412419381,3.38322793010033,1.75038658459866));
#41759=CARTESIAN_POINT('Ctrl Pts',(-27.5877680902101,0.364035370925649,
3.79177566204397));
#41760=CARTESIAN_POINT('Ctrl Pts',(-27.3892949384819,-2.98840173480935,
2.36210488631272));
#41761=CARTESIAN_POINT('Ctrl Pts',(-27.1908217867538,-3.60520197502674,
-1.22987932002179));
#41762=CARTESIAN_POINT('Ctrl Pts',(-26.9923486350256,-0.921735281371103,
-3.69600980702566));
#41763=CARTESIAN_POINT('Ctrl Pts',(-26.7938754832976,2.60550451902449,-2.77874623236759));
#41764=CARTESIAN_POINT('Ctrl Pts',(-26.5954023315693,3.74761847355685,0.682231778217214));
#41765=CARTESIAN_POINT('Ctrl Pts',(-26.3969291798413,1.45909486194852,3.51868251002977));
#41766=CARTESIAN_POINT('Ctrl Pts',(-26.1984560281131,-2.16511051163293,
3.13406778723285));
#41767=CARTESIAN_POINT('Ctrl Pts',(-25.999982876385,-3.80733465941356,-0.119529133612606));
#41768=CARTESIAN_POINT('Ctrl Pts',(-25.8015097246568,-1.9642559671063,-3.26370692897528));
#41769=CARTESIAN_POINT('Ctrl Pts',(-25.6030365729288,1.67693807707542,-3.4202285169574));
#41770=CARTESIAN_POINT('Ctrl Pts',(-25.4045634212006,3.78303274977641,-0.445811211919431));
#41771=CARTESIAN_POINT('Ctrl Pts',(-25.2060902694725,2.42607098893233,2.93670971994425));
#41772=CARTESIAN_POINT('Ctrl Pts',(-25.0076171177444,-1.15175992694511,
3.63091358933775));
#41773=CARTESIAN_POINT('Ctrl Pts',(-24.8091439660162,-3.67524902536336,
1.00131364922265));
#41774=CARTESIAN_POINT('Ctrl Pts',(-24.6106708142881,-2.83434885622448,
-2.54490687133595));
#41775=CARTESIAN_POINT('Ctrl Pts',(-24.41219766256,0.601165393915808,-3.76147372604303));
#41776=CARTESIAN_POINT('Ctrl Pts',(-24.2137245108318,3.48636199609287,-1.53471966650373));
#41777=CARTESIAN_POINT('Ctrl Pts',(-24.0152513591037,3.18007992525289,2.09694446553971));
#41778=CARTESIAN_POINT('Ctrl Pts',(-23.8167782073755,-0.0373046849413855,
3.80902780024449));
#41779=CARTESIAN_POINT('Ctrl Pts',(-23.6183050556475,-3.22053991348009,
2.03425836319669));
#41780=CARTESIAN_POINT('Ctrl Pts',(-23.4198319039193,-3.45563479945234,
-1.60270788210705));
#41781=CARTESIAN_POINT('Ctrl Pts',(-23.2213587521912,-0.527379242599795,
-3.77252641568339));
#41782=CARTESIAN_POINT('Ctrl Pts',(-23.022885600463,2.88364878803355,-2.48890620350118));
#41783=CARTESIAN_POINT('Ctrl Pts',(-22.8244124487349,3.65493269060604,1.0731036528189));
#41784=CARTESIAN_POINT('Ctrl Pts',(-22.6259392970067,1.08042526501054,3.65277506415067));
#41785=CARTESIAN_POINT('Ctrl Pts',(-22.4274661452787,-2.48312294147182,
2.8886302775001));
#41786=CARTESIAN_POINT('Ctrl Pts',(-22.2289929935505,-3.77357560622099,
-0.519818782546203));
#41787=CARTESIAN_POINT('Ctrl Pts',(-22.0305198418224,-1.60962907726382,
-3.45241635035243));
#41788=CARTESIAN_POINT('Ctrl Pts',(-21.8320466900942,2.02780095034114,-3.22460970170803));
#41789=CARTESIAN_POINT('Ctrl Pts',(-21.6335735383662,3.80894540192439,-0.0449371529252134));
#41790=CARTESIAN_POINT('Ctrl Pts',(-21.435100386638,2.1033125106639,3.17587167641245));
#41791=CARTESIAN_POINT('Ctrl Pts',(-21.2366272349099,-1.52773060133581,
3.48943027331057));
#41792=CARTESIAN_POINT('Ctrl Pts',(-21.0381540831817,-3.76026155718447,
0.608701440867885));
#41793=CARTESIAN_POINT('Ctrl Pts',(-20.8396809314537,-2.5505812400301,-2.82924367288512));
#41794=CARTESIAN_POINT('Ctrl Pts',(-20.6412077797255,0.993947162456761,
-3.67724808257454));
#41795=CARTESIAN_POINT('Ctrl Pts',(-20.4427346279974,3.62859839939353,-1.15903325166825));
#41796=CARTESIAN_POINT('Ctrl Pts',(-20.2442614762692,2.94156519346794,2.42018152937583));
#41797=CARTESIAN_POINT('Ctrl Pts',(-20.0457883245411,-0.438229862995021,
3.78391847292371));
#41798=CARTESIAN_POINT('Ctrl Pts',(-19.847315172813,-3.41686139622225,1.68378817597706));
#41799=CARTESIAN_POINT('Ctrl Pts',(-19.6488420210848,-3.26763635950076,
-1.95771219657607));
#41800=CARTESIAN_POINT('Ctrl Pts',(-19.4503688693567,-0.12715804379987,
-3.80708750286241));
#41801=CARTESIAN_POINT('Ctrl Pts',(-19.2518957176286,3.12972303941186,-2.17138622062695));
#41802=CARTESIAN_POINT('Ctrl Pts',(-19.0534225659005,3.52159918511936,1.4520411846503));
#41803=CARTESIAN_POINT('Ctrl Pts',(-18.8549494141723,0.689739899217004,
3.74624389141739));
#41804=CARTESIAN_POINT('Ctrl Pts',(-18.6564762624442,-2.77351973488412,
2.61106734933481));
#41805=CARTESIAN_POINT('Ctrl Pts',(-18.4580031107161,-3.69784936315266,
-0.914327353842945));
#41806=CARTESIAN_POINT('Ctrl Pts',(-18.2595299589879,-1.23710096689095,
-3.6027303007957));
#41807=CARTESIAN_POINT('Ctrl Pts',(-18.0610568072598,2.35611197454017,-2.99312892906109));
#41808=CARTESIAN_POINT('Ctrl Pts',(-17.8625836555317,3.79249750493022,0.356436667098387));
#41809=CARTESIAN_POINT('Ctrl Pts',(-17.6641105038036,1.75716239414189,3.37971370727872));
#41810=CARTESIAN_POINT('Ctrl Pts',(-17.4656373520754,-1.88671087539651,
3.30913984219684));
#41811=CARTESIAN_POINT('Ctrl Pts',(-17.2671642003473,-3.80345496909903,
0.209319661259676));
#41812=CARTESIAN_POINT('Ctrl Pts',(-17.0686910486191,-2.23844776122589,
-3.08211551419099));
#41813=CARTESIAN_POINT('Ctrl Pts',(-16.870217896891,1.37567491389401,-3.55212653967123));
#41814=CARTESIAN_POINT('Ctrl Pts',(-16.6717447451629,3.73047995257294,-0.770456842402849));
#41815=CARTESIAN_POINT('Ctrl Pts',(-16.4732715934348,2.67033633643725,2.7165029491714));
#41816=CARTESIAN_POINT('Ctrl Pts',(-16.2747984417066,-0.834281340932724,
3.71672692926525));
#41817=CARTESIAN_POINT('Ctrl Pts',(-16.0763252899785,-3.57518282650542,
1.31459202021571));
#41818=CARTESIAN_POINT('Ctrl Pts',(-15.8778521382504,-3.04329744837427,
-2.29094414232926));
#41819=CARTESIAN_POINT('Ctrl Pts',(-15.6793789865222,0.274477321913715,
-3.79930870321287));
#41820=CARTESIAN_POINT('Ctrl Pts',(-15.4809058347941,3.34099059953505,-1.82971752912093));
#41821=CARTESIAN_POINT('Ctrl Pts',(-15.282432683066,3.34910080337457,1.81483008333833));
#41822=CARTESIAN_POINT('Ctrl Pts',(-15.0839595313379,0.291383706511294,
3.79804949390259));
#41823=CARTESIAN_POINT('Ctrl Pts',(-14.8854863796097,-3.03307129250833,
2.30446587241291));
#41824=CARTESIAN_POINT('Ctrl Pts',(-14.6870132278816,-3.58099810695365,
-1.29866738641899));
#41825=CARTESIAN_POINT('Ctrl Pts',(-14.4885400761535,-0.850814645052164,
-3.71297708884916));
#41826=CARTESIAN_POINT('Ctrl Pts',(-14.2900669244253,2.6582198935355,-2.72836057370837));
#41827=CARTESIAN_POINT('Ctrl Pts',(-14.0915937726972,3.73387198132893,0.753846436352181));
#41828=CARTESIAN_POINT('Ctrl Pts',(-13.8931206209691,1.39147028998462,3.54596881749461));
#41829=CARTESIAN_POINT('Ctrl Pts',(-13.694647469241,-2.224708410058,3.09204736586798));
#41830=CARTESIAN_POINT('Ctrl Pts',(-13.4961743175128,-3.80434889280168,
-0.192390031947064));
#41831=CARTESIAN_POINT('Ctrl Pts',(-13.2977011657847,-1.9014197600839,-3.30071012336989));
#41832=CARTESIAN_POINT('Ctrl Pts',(-13.0992280140566,1.74210332689385,-3.38750061564265));
#41833=CARTESIAN_POINT('Ctrl Pts',(-12.9007548623284,3.79087359697976,-0.373311926243645));
#41834=CARTESIAN_POINT('Ctrl Pts',(-12.7022817106003,2.36940978052417,2.98261323582365));
#41835=CARTESIAN_POINT('Ctrl Pts',(-12.5038085588722,-1.22105449849256,
3.60820042878236));
#41836=CARTESIAN_POINT('Ctrl Pts',(-12.3053354071441,-3.69374345902606,
0.930775849201267));
#41837=CARTESIAN_POINT('Ctrl Pts',(-12.1068622554159,-2.78511301374644,
-2.5986977360236));
#41838=CARTESIAN_POINT('Ctrl Pts',(-11.9083891036878,0.673060134005079,
-3.74927652735391));
#41839=CARTESIAN_POINT('Ctrl Pts',(-11.7099159519597,3.51510189157322,-1.46769994018271));
#41840=CARTESIAN_POINT('Ctrl Pts',(-11.5114428002315,3.1393559572694,2.15743565283212));
#41841=CARTESIAN_POINT('Ctrl Pts',(-11.3129696485034,-0.110213061344868,
3.80761572426406));
#41842=CARTESIAN_POINT('Ctrl Pts',(-11.1144964967753,-3.2588910551131,1.97223566377292));
#41843=CARTESIAN_POINT('Ctrl Pts',(-10.9160233450471,-3.42432137932337,
-1.66856450689293));
#41844=CARTESIAN_POINT('Ctrl Pts',(-10.717550193319,-0.45506613045934,-3.78193062330111));
#41845=CARTESIAN_POINT('Ctrl Pts',(-10.5190770415909,2.93076486464135,-2.43324921262453));
#41846=CARTESIAN_POINT('Ctrl Pts',(-10.3206038898627,3.63372082507465,1.1428724285645));
#41847=CARTESIAN_POINT('Ctrl Pts',(-10.1221307381346,1.01030318175698,3.67278802866238));
#41848=CARTESIAN_POINT('Ctrl Pts',(-9.92365758640649,-2.53796422227748,
2.8405672019851));
#41849=CARTESIAN_POINT('Ctrl Pts',(-9.72518443467834,-3.76293338666949,
-0.591960091595758));
#41850=CARTESIAN_POINT('Ctrl Pts',(-9.52671128295022,-1.54324543714212,
-3.48259643704148));
#41851=CARTESIAN_POINT('Ctrl Pts',(-9.3282381312221,2.0891572291558,-3.18520117016493));
#41852=CARTESIAN_POINT('Ctrl Pts',(-9.12976497949396,3.80910767480012,0.0279847160571414));
#41853=CARTESIAN_POINT('Ctrl Pts',(-8.93129182776584,2.0421322300825,3.21555288829343));
#41854=CARTESIAN_POINT('Ctrl Pts',(-8.73281867603769,-1.59424790270054,
3.45954593079627));
#41855=CARTESIAN_POINT('Ctrl Pts',(-8.53434552430958,-3.77122474154193,
0.536608210276483));
#41856=CARTESIAN_POINT('Ctrl Pts',(-8.33587237258143,-2.49595441061896,
-2.87755034754663));
#41857=CARTESIAN_POINT('Ctrl Pts',(-8.13739922085333,1.06415762040292,-3.65754739976015));
#41858=CARTESIAN_POINT('Ctrl Pts',(-7.93892606912516,3.65012056591666,-1.08935957187082));
#41859=CARTESIAN_POINT('Ctrl Pts',(-7.74045291739707,2.89469728902442,2.47604766260028));
#41860=CARTESIAN_POINT('Ctrl Pts',(-7.54197976566891,-0.510584113075111,
3.77483619327098));
#41861=CARTESIAN_POINT('Ctrl Pts',(-7.3435066139408,-3.44846760598317,1.61807156610622));
#41862=CARTESIAN_POINT('Ctrl Pts',(-7.14503346221266,-3.22956163427927,
-2.01990496631462));
#41863=CARTESIAN_POINT('Ctrl Pts',(-6.94656031048453,-0.0542566740194617,
-3.80882404895191));
#41864=CARTESIAN_POINT('Ctrl Pts',(-6.74808715875641,3.17071582455421,-2.11107687744781));
#41865=CARTESIAN_POINT('Ctrl Pts',(-6.54961400702828,3.49315785049429,1.51918815623972));
#41866=CARTESIAN_POINT('Ctrl Pts',(-6.35114085530014,0.617900155701453,
3.75876094213507));
#41867=CARTESIAN_POINT('Ctrl Pts',(-6.15266770357201,-2.82299448995578,
2.55749614513145));
#41868=CARTESIAN_POINT('Ctrl Pts',(-5.95419455184388,-3.67966904629497,
-0.984946766120382));
#41869=CARTESIAN_POINT('Ctrl Pts',(-5.75572140011576,-1.16790816827868,
-3.62575163696693));
#41870=CARTESIAN_POINT('Ctrl Pts',(-5.55724824838763,2.41297691887338,-2.94747804273184));
#41871=CARTESIAN_POINT('Ctrl Pts',(-5.35877509665951,3.78497939857008,0.428970131116378));
#41872=CARTESIAN_POINT('Ctrl Pts',(-5.16030194493137,1.69214344806,3.41273130701552));
#41873=CARTESIAN_POINT('Ctrl Pts',(-4.96182879320323,-1.94971114633403,
3.27241667179486));
#41874=CARTESIAN_POINT('Ctrl Pts',(-4.76335564147511,-3.80676497740825,
0.136472772224148));
#41875=CARTESIAN_POINT('Ctrl Pts',(-4.56488248974698,-2.179037470938,-3.12440076292683));
#41876=CARTESIAN_POINT('Ctrl Pts',(-4.36640933801884,1.44342026140034,-3.52514147306206));
#41877=CARTESIAN_POINT('Ctrl Pts',(-4.16793618629072,3.74454502431787,-0.698904068557403));
#41878=CARTESIAN_POINT('Ctrl Pts',(-3.96946303456259,2.61784574945316,2.7671227133945));
#41879=CARTESIAN_POINT('Ctrl Pts',(-3.77098988283447,-0.905276827937616,
3.70007547035483));
#41880=CARTESIAN_POINT('Ctrl Pts',(-3.57251673110632,-3.59969252675421,
1.24591232298042));
#41881=CARTESIAN_POINT('Ctrl Pts',(-3.3740435793782,-2.9988850021576,-2.34878132703989));
#41882=CARTESIAN_POINT('Ctrl Pts',(-3.17557042765007,0.347156461294124,
-3.7933583964979));
#41883=CARTESIAN_POINT('Ctrl Pts',(-2.97709727592195,3.37540367795816,-1.76542632168304));
#41884=CARTESIAN_POINT('Ctrl Pts',(-2.77862412419381,3.31374730129506,1.87860804283756));
#41885=CARTESIAN_POINT('Ctrl Pts',(-2.58015097246569,0.218623351459381,
3.80293227389407));
#41886=CARTESIAN_POINT('Ctrl Pts',(-2.38167782073755,-3.07662565351087,
2.24598069837365));
#41887=CARTESIAN_POINT('Ctrl Pts',(-2.18320466900942,-3.55548884937955,
-1.36697641350964));
#41888=CARTESIAN_POINT('Ctrl Pts',(-1.98473151728128,-0.779568879692582,
-3.72858958741861));
#41889=CARTESIAN_POINT('Ctrl Pts',(-1.78625836555316,2.7099356073734,-2.67696366978096));
#41890=CARTESIAN_POINT('Ctrl Pts',(-1.58778521382502,3.71880583993438,0.825163098419798));
#41891=CARTESIAN_POINT('Ctrl Pts',(-1.3893120620969,1.32324257672849,3.57199715958687));
#41892=CARTESIAN_POINT('Ctrl Pts',(-1.19083891036877,-2.28331276119187,
3.04881430456285));
#41893=CARTESIAN_POINT('Ctrl Pts',(-0.992365758640647,-3.80030983792451,
-0.265028402279971));
#41894=CARTESIAN_POINT('Ctrl Pts',(-0.793892606912507,-1.8372343102454,
-3.33679471955611));
#41895=CARTESIAN_POINT('Ctrl Pts',(-0.59541945518438,1.80537864589007,-3.35297192389334));
#41896=CARTESIAN_POINT('Ctrl Pts',(-0.396946303456254,3.79975239553181,
-0.301770123854898));
#41897=CARTESIAN_POINT('Ctrl Pts',(-0.198473151728127,2.30693671058513,
3.02973452897375));
#41898=CARTESIAN_POINT('Ctrl Pts',(-0.0661577172427008,-0.082916802787829,
3.39526186154233));
#41899=CARTESIAN_POINT('Ctrl Pts',(8.88178419700125E-15,-1.09131022003164,
3.0323521507494));
#41900=CARTESIAN_POINT('Ctrl Pts',(-54.8403753524613,-1.53816642191861,
3.09873914818303));
#41901=CARTESIAN_POINT('Ctrl Pts',(-54.7742176352186,-2.56863650040579,
2.58722966070319));
#41902=CARTESIAN_POINT('Ctrl Pts',(-54.6419022007331,-4.06135220822103,
0.464230130887601));
#41903=CARTESIAN_POINT('Ctrl Pts',(-54.4434290490051,-2.58979336326103,
-3.16784658591715));
#41904=CARTESIAN_POINT('Ctrl Pts',(-54.2449558972769,1.25592581519661,-3.89016608596827));
#41905=CARTESIAN_POINT('Ctrl Pts',(-54.0464827455489,3.95019391506363,-1.0562748493163));
#41906=CARTESIAN_POINT('Ctrl Pts',(-53.8480095938205,3.02929673638347,2.7470943920291));
#41907=CARTESIAN_POINT('Ctrl Pts',(-53.6495364420926,-0.665150589651805,
4.03439607821359));
#41908=CARTESIAN_POINT('Ctrl Pts',(-53.4510632903643,-3.75045755449035,
1.62923276434178));
#41909=CARTESIAN_POINT('Ctrl Pts',(-53.2525901386363,-3.4026584696794,-2.26772244689711));
#41910=CARTESIAN_POINT('Ctrl Pts',(-53.0541169869081,0.0600637872383345,
-4.08857389822173));
#41911=CARTESIAN_POINT('Ctrl Pts',(-52.85564383518,3.46776689928094,-2.16677023749668));
#41912=CARTESIAN_POINT('Ctrl Pts',(-52.6571706834519,3.70103227721164,1.73858586375658));
#41913=CARTESIAN_POINT('Ctrl Pts',(-52.4586975317237,0.546296180759445,
4.05238197395636));
#41914=CARTESIAN_POINT('Ctrl Pts',(-52.2602243799957,-3.10852419624347,
2.65656869376971));
#41915=CARTESIAN_POINT('Ctrl Pts',(-52.0617512282674,-3.91774810586626,
-1.17112291516237));
#41916=CARTESIAN_POINT('Ctrl Pts',(-51.8632780765394,-1.14059332005749,
-3.92674360008736));
#41917=CARTESIAN_POINT('Ctrl Pts',(-51.6648049248112,2.680680440696,-3.08775437389328));
#41918=CARTESIAN_POINT('Ctrl Pts',(-51.4663317730831,4.0480113417869,0.577821976434141));
#41919=CARTESIAN_POINT('Ctrl Pts',(-51.2678586213549,1.70971942604948,3.71444910992895));
#41920=CARTESIAN_POINT('Ctrl Pts',(-51.0693854696268,-2.19368039523064,
3.45080280108978));
#41921=CARTESIAN_POINT('Ctrl Pts',(-50.8709123178987,-4.08894565830513,
0.0282291963244218));
#41922=CARTESIAN_POINT('Ctrl Pts',(-50.6724391661706,-2.24111626351152,
-3.42018584481279));
#41923=CARTESIAN_POINT('Ctrl Pts',(-50.4739660144424,1.65827137876417,-3.73770109722635));
#41924=CARTESIAN_POINT('Ctrl Pts',(-50.2754928627143,4.03964748977492,-0.633657307052364));
#41925=CARTESIAN_POINT('Ctrl Pts',(-50.0770197109862,2.72305740026553,3.05044780326519));
#41926=CARTESIAN_POINT('Ctrl Pts',(-49.878546559258,-1.08626856138223,3.9421179634757));
#41927=CARTESIAN_POINT('Ctrl Pts',(-49.6800734075299,-3.90120468433239,
1.22510221216824));
#41928=CARTESIAN_POINT('Ctrl Pts',(-49.4816002558018,-3.14490765217551,
-2.61339420613093));
#41929=CARTESIAN_POINT('Ctrl Pts',(-49.2831271040736,0.490294585669324,
-4.05954241748915));
#41930=CARTESIAN_POINT('Ctrl Pts',(-49.0846539523456,3.6766723139372,-1.7895122561802));
#41931=CARTESIAN_POINT('Ctrl Pts',(-48.8861808006173,3.49735787052484,2.11866971102118));
#41932=CARTESIAN_POINT('Ctrl Pts',(-48.6877076488894,0.116498932293703,
4.08738319931909));
#41933=CARTESIAN_POINT('Ctrl Pts',(-48.489234497161,-3.37100523048403,2.31443236133217));
#41934=CARTESIAN_POINT('Ctrl Pts',(-48.2907613454331,-3.77263038476602,
-1.57719161773841));
#41935=CARTESIAN_POINT('Ctrl Pts',(-48.0922881937048,-0.720721618121668,
-4.02502593387261));
#41936=CARTESIAN_POINT('Ctrl Pts',(-47.8938150419768,2.99094872118978,-2.78827888963095));
#41937=CARTESIAN_POINT('Ctrl Pts',(-47.6953418902486,3.9646506376959,1.0009089569821));
#41938=CARTESIAN_POINT('Ctrl Pts',(-47.4968687385205,1.30903982926209,3.87384668573263));
#41939=CARTESIAN_POINT('Ctrl Pts',(-47.2983955867924,-2.54488965689468,
3.20059526547526));
#41940=CARTESIAN_POINT('Ctrl Pts',(-47.0999224350642,-4.06918123560976,
-0.402538806718081));
#41941=CARTESIAN_POINT('Ctrl Pts',(-46.9014492833361,-1.86847089408725,
-3.63718159253868));
#41942=CARTESIAN_POINT('Ctrl Pts',(-46.7029761316081,2.04267141529049,-3.54228272563159));
#41943=CARTESIAN_POINT('Ctrl Pts',(-46.5045029798797,4.08391545673528,-0.204714340952344));
#41944=CARTESIAN_POINT('Ctrl Pts',(-46.3060298281518,2.38666960608566,3.32025324494081));
#41945=CARTESIAN_POINT('Ctrl Pts',(-46.1075566764235,-1.49537666285008,
3.80580110559607));
#41946=CARTESIAN_POINT('Ctrl Pts',(-45.9090835246955,-4.00852815466228,
0.80744996899671));
#41947=CARTESIAN_POINT('Ctrl Pts',(-45.7106103729673,-2.85220065085376,
-2.93005543743158));
#41948=CARTESIAN_POINT('Ctrl Pts',(-45.5121372212392,0.915082788846247,
-3.98533523165999));
#41949=CARTESIAN_POINT('Ctrl Pts',(-45.3136640695111,3.84468293348948,-1.39236725043635));
#41950=CARTESIAN_POINT('Ctrl Pts',(-45.115190917783,3.25479095410903,2.47519883326633));
#41951=CARTESIAN_POINT('Ctrl Pts',(-44.9167177660547,-0.314595388395248,
4.07692324685582));
#41952=CARTESIAN_POINT('Ctrl Pts',(-44.7182446143267,-3.59599543635577,
1.94655856342968));
#41953=CARTESIAN_POINT('Ctrl Pts',(-44.5197714625985,-3.58555638204929,
-1.96572094924447));
#41954=CARTESIAN_POINT('Ctrl Pts',(-44.3212983108704,-0.292834324131919,
-4.07854403896331));
#41955=CARTESIAN_POINT('Ctrl Pts',(-44.1228251591423,3.26795355748413,-2.4577943293286));
#41956=CARTESIAN_POINT('Ctrl Pts',(-43.9243520074141,3.83719779136388,1.4128646534984));
#41957=CARTESIAN_POINT('Ctrl Pts',(-43.7258788556861,0.893801935370474,
3.99016184126421));
#41958=CARTESIAN_POINT('Ctrl Pts',(-43.5274057039578,-2.86779633845362,
2.91479288806339));
#41959=CARTESIAN_POINT('Ctrl Pts',(-43.3289325522298,-4.00416210257613,
-0.828830064275004));
#41960=CARTESIAN_POINT('Ctrl Pts',(-43.1304594005017,-1.47504563393096,
-3.81372702182184));
#41961=CARTESIAN_POINT('Ctrl Pts',(-42.9319862487735,2.40435422114778,-3.30746945539968));
#41962=CARTESIAN_POINT('Ctrl Pts',(-42.7335130970454,4.08276484224243,0.226505324666171));
#41963=CARTESIAN_POINT('Ctrl Pts',(-42.5350399453173,2.02373886450903,3.55313304386828));
#41964=CARTESIAN_POINT('Ctrl Pts',(-42.3365667935891,-1.88785418258624,
3.62715866822016));
#41965=CARTESIAN_POINT('Ctrl Pts',(-42.138093641861,-4.07127144981634,0.380817805601726));
#41966=CARTESIAN_POINT('Ctrl Pts',(-41.9396204901328,-2.52777337701186,
-3.21413054707226));
#41967=CARTESIAN_POINT('Ctrl Pts',(-41.7411473384048,1.3296940518132,-3.86680580682888));
#41968=CARTESIAN_POINT('Ctrl Pts',(-41.5426741866766,3.96993555494399,-0.979737265160665));
#41969=CARTESIAN_POINT('Ctrl Pts',(-41.3442010349485,2.9760264245333,2.80420044569437));
#41970=CARTESIAN_POINT('Ctrl Pts',(-41.1457278832203,-0.742190989089927,
4.02112247449225));
#41971=CARTESIAN_POINT('Ctrl Pts',(-40.9472547314922,-3.78099338050939,
1.55703644006726));
#41972=CARTESIAN_POINT('Ctrl Pts',(-40.7487815797641,-3.35860621380553,
-2.33238884402664));
#41973=CARTESIAN_POINT('Ctrl Pts',(-40.550308428036,0.138309677808596,-4.08670329876998));
#41974=CARTESIAN_POINT('Ctrl Pts',(-40.3518352763078,3.50861439493976,-2.09997582052138));
#41975=CARTESIAN_POINT('Ctrl Pts',(-40.1533621245797,3.66707019166621,1.80910741210853));
#41976=CARTESIAN_POINT('Ctrl Pts',(-39.9548889728515,0.46862377276644,4.06210107933703));
#41977=CARTESIAN_POINT('Ctrl Pts',(-39.7564158211235,-3.15880930274817,
2.59657412912179));
#41978=CARTESIAN_POINT('Ctrl Pts',(-39.5579426693953,-3.89461135051907,
-1.24590362691542));
#41979=CARTESIAN_POINT('Ctrl Pts',(-39.3594695176672,-1.06521590049673,
-3.94785872397707));
#41980=CARTESIAN_POINT('Ctrl Pts',(-39.160996365939,2.73929740372549,-3.03587271687992));
#41981=CARTESIAN_POINT('Ctrl Pts',(-38.9625232142109,4.03620844150535,0.655205949205342));
#41982=CARTESIAN_POINT('Ctrl Pts',(-38.7640500624828,1.63830144967379,3.74649726800244));
#41983=CARTESIAN_POINT('Ctrl Pts',(-38.5655769107546,-2.25933624782354,
3.40817739245239));
#41984=CARTESIAN_POINT('Ctrl Pts',(-38.3671037590265,-4.08873678056746,
-0.0500495593165138));
#41985=CARTESIAN_POINT('Ctrl Pts',(-38.1686306072984,-2.17523389439348,
-3.46246024148072));
#41986=CARTESIAN_POINT('Ctrl Pts',(-37.9701574555703,1.72951734480887,-3.70527234804113));
#41987=CARTESIAN_POINT('Ctrl Pts',(-37.7716843038422,4.05103720219932,-0.556211295777075));
#41988=CARTESIAN_POINT('Ctrl Pts',(-37.573211152114,2.66416451489506,3.10201561194119));
#41989=CARTESIAN_POINT('Ctrl Pts',(-37.3747380003859,-1.16153243685025,
3.92060146116609));
#41990=CARTESIAN_POINT('Ctrl Pts',(-37.1762648486577,-3.92394163925128,
1.15019799639151));
#41991=CARTESIAN_POINT('Ctrl Pts',(-36.9777916969297,-3.09430386836932,
-2.67311746643273));
#41992=CARTESIAN_POINT('Ctrl Pts',(-36.7793185452014,0.567915491803217,
-4.04941297144696));
#41993=CARTESIAN_POINT('Ctrl Pts',(-36.5808453934734,3.7102547643092,-1.71880278190193));
#41994=CARTESIAN_POINT('Ctrl Pts',(-36.3823722417452,3.45615988424496,2.18523048525522));
#41995=CARTESIAN_POINT('Ctrl Pts',(-36.1838990900172,0.0382338892631252,
4.08886433974823));
#41996=CARTESIAN_POINT('Ctrl Pts',(-35.9854259382889,-3.41469209777534,
2.24947800534782));
#41997=CARTESIAN_POINT('Ctrl Pts',(-35.7869527865609,-3.74174732980241,
-1.64912108077893));
#41998=CARTESIAN_POINT('Ctrl Pts',(-35.5884796348327,-0.643539546610226,
-4.0380849757158));
#41999=CARTESIAN_POINT('Ctrl Pts',(-35.3900064831046,3.04377594844649,-2.73051302776818));
#42000=CARTESIAN_POINT('Ctrl Pts',(-35.1915333313765,3.94476402374705,1.07661981038065));
#42001=CARTESIAN_POINT('Ctrl Pts',(-34.9930601796483,1.23464393931464,3.89819544946974));
#42002=CARTESIAN_POINT('Ctrl Pts',(-34.7945870279202,-2.6056914829135,3.15129264192092));
#42003=CARTESIAN_POINT('Ctrl Pts',(-34.5961138761921,-4.06072990916123,
-0.480360306432908));
#42004=CARTESIAN_POINT('Ctrl Pts',(-34.397640724464,-1.79850291188313,-3.67228276350022));
#42005=CARTESIAN_POINT('Ctrl Pts',(-34.1991675727358,2.11010609996108,-3.50253132263795));
#42006=CARTESIAN_POINT('Ctrl Pts',(-34.0006944210077,4.08708591685189,-0.126499515508336));
#42007=CARTESIAN_POINT('Ctrl Pts',(-33.8022212692795,2.32267354525533,3.36533223045274));
#42008=CARTESIAN_POINT('Ctrl Pts',(-33.6037481175514,-1.56795609591073,
3.77647813451229));
#42009=CARTESIAN_POINT('Ctrl Pts',(-33.4052749658233,-4.02325043743371,
0.730567818099445));
#42010=CARTESIAN_POINT('Ctrl Pts',(-33.2068018140952,-2.79558874006392,
-2.98411746008444));
#42011=CARTESIAN_POINT('Ctrl Pts',(-33.008328662367,0.991205328654403,-3.96708777513178));
#42012=CARTESIAN_POINT('Ctrl Pts',(-32.8098555106389,3.87063215595414,-1.31851436565809));
#42013=CARTESIAN_POINT('Ctrl Pts',(-32.6113823589108,3.20681247280386,2.53705088309687));
#42014=CARTESIAN_POINT('Ctrl Pts',(-32.4129092071826,-0.392581206044021,
4.07015397937399));
#42015=CARTESIAN_POINT('Ctrl Pts',(-32.2144360554545,-3.63259896583331,
1.87736468822116));
#42016=CARTESIAN_POINT('Ctrl Pts',(-32.0159629037264,-3.54727009206207,
-2.03399811040102));
#42017=CARTESIAN_POINT('Ctrl Pts',(-31.8174897519982,-0.214706175304816,
-4.08340234087202));
#42018=CARTESIAN_POINT('Ctrl Pts',(-31.6190166002702,3.31440364810769,-2.39478639476751));
#42019=CARTESIAN_POINT('Ctrl Pts',(-31.420543448542,3.80944857276316,1.48606022442755));
#42020=CARTESIAN_POINT('Ctrl Pts',(-31.2220702968139,0.817255542910768,
4.0065405023205));
#42021=CARTESIAN_POINT('Ctrl Pts',(-31.0235971450857,-2.92306795604602,
2.85936131740812));
#42022=CARTESIAN_POINT('Ctrl Pts',(-30.8251239933576,-3.98756230933313,
-0.905328806754085));
#42023=CARTESIAN_POINT('Ctrl Pts',(-30.6266508416295,-1.40177018008474,
-3.84126460705041));
#42024=CARTESIAN_POINT('Ctrl Pts',(-30.4281776899013,2.46722766309277,-3.26083748101967));
#42025=CARTESIAN_POINT('Ctrl Pts',(-30.2297045381732,4.07768078915179,0.304619107961798));
#42026=CARTESIAN_POINT('Ctrl Pts',(-30.031231386445,1.95535135030967,3.5912218695028));
#42027=CARTESIAN_POINT('Ctrl Pts',(-29.832758234717,-1.95694199353205,3.59035533799984));
#42028=CARTESIAN_POINT('Ctrl Pts',(-29.6342850829888,-4.07781532886962,
0.302812752024875));
#42029=CARTESIAN_POINT('Ctrl Pts',(-29.4358119312607,-2.46578293922098,
-3.26193009057516));
#42030=CARTESIAN_POINT('Ctrl Pts',(-29.2373387795326,1.40347164124787,-3.84064327572426));
#42031=CARTESIAN_POINT('Ctrl Pts',(-29.0388656278044,3.98796295954069,-0.903562312452452));
#42032=CARTESIAN_POINT('Ctrl Pts',(-28.8403924760763,2.92180103286938,2.86065589392999));
#42033=CARTESIAN_POINT('Ctrl Pts',(-28.6419193243482,-0.819030275137617,
4.00617808235744));
#42034=CARTESIAN_POINT('Ctrl Pts',(-28.4434461726201,-3.81010649213961,
1.48437257375252));
#42035=CARTESIAN_POINT('Ctrl Pts',(-28.2449730208919,-3.31334248336611,
-2.39625437027754));
#42036=CARTESIAN_POINT('Ctrl Pts',(-28.0464998691638,0.216515014814097,
-4.08330682994959));
#42037=CARTESIAN_POINT('Ctrl Pts',(-27.8480267174356,3.54817076201677,-2.03242654546783));
#42038=CARTESIAN_POINT('Ctrl Pts',(-27.6495535657076,3.63176697670682,1.87897366827073));
#42039=CARTESIAN_POINT('Ctrl Pts',(-27.4510804139794,0.390778175693683,
4.07032748517296));
#42040=CARTESIAN_POINT('Ctrl Pts',(-27.2526072622513,-3.20793601786463,
2.53563008430642));
#42041=CARTESIAN_POINT('Ctrl Pts',(-27.0541341105231,-3.87004770230544,
-1.32022884419077));
#42042=CARTESIAN_POINT('Ctrl Pts',(-26.855660958795,-0.98944789571108,-3.96752646882488));
#42043=CARTESIAN_POINT('Ctrl Pts',(-26.6571878070669,2.79691036647756,-2.98287878081619));
#42044=CARTESIAN_POINT('Ctrl Pts',(-26.4587146553387,4.02292641665342,0.732349960978325));
#42045=CARTESIAN_POINT('Ctrl Pts',(-26.2602415036106,1.56628304240493,3.77717233525659));
#42046=CARTESIAN_POINT('Ctrl Pts',(-26.0617683518825,-2.32416408812179,
3.36430300517625));
#42047=CARTESIAN_POINT('Ctrl Pts',(-25.8632952001543,-4.08702947924636,
-0.12830999541797));
#42048=CARTESIAN_POINT('Ctrl Pts',(-25.6648220484262,-2.10855434588592,
-3.50346571120634));
#42049=CARTESIAN_POINT('Ctrl Pts',(-25.4663488966981,1.80012947875039,-3.67148570457339));
#42050=CARTESIAN_POINT('Ctrl Pts',(-25.26787574497,4.06094230016339,-0.478561442133215));
#42051=CARTESIAN_POINT('Ctrl Pts',(-25.0694025932418,2.60429527149516,3.15244659875803));
#42052=CARTESIAN_POINT('Ctrl Pts',(-24.8709294415137,-1.23637063603042,
3.89764814593555));
#42053=CARTESIAN_POINT('Ctrl Pts',(-24.6724562897856,-3.94524055643307,
1.07487225800491));
#42054=CARTESIAN_POINT('Ctrl Pts',(-24.4739831380575,-3.0425660904843,-2.73186108801089));
#42055=CARTESIAN_POINT('Ctrl Pts',(-24.2755099863293,0.645328269413449,
-4.03779950515733));
#42056=CARTESIAN_POINT('Ctrl Pts',(-24.0770368346012,3.74247748832006,-1.64746340431906));
#42057=CARTESIAN_POINT('Ctrl Pts',(-23.878563682873,3.41369529172666,2.25099042076953));
#42058=CARTESIAN_POINT('Ctrl Pts',(-23.6800905311449,-0.0400451656365475,
4.08884700176738));
#42059=CARTESIAN_POINT('Ctrl Pts',(-23.4816173794168,-3.45712755587142,
2.18369926537229));
#42060=CARTESIAN_POINT('Ctrl Pts',(-23.2831442276887,-3.70949300712285,
-1.72044617737949));
#42061=CARTESIAN_POINT('Ctrl Pts',(-23.0846710759605,-0.56612163207619,
-4.04966414864845));
#42062=CARTESIAN_POINT('Ctrl Pts',(-22.8861979242324,3.09548769907761,-2.67174649321603));
#42063=CARTESIAN_POINT('Ctrl Pts',(-22.6877247725043,3.9234317409515,1.15193610640832));
#42064=CARTESIAN_POINT('Ctrl Pts',(-22.4892516207761,1.1597955796458,3.92111561071425));
#42065=CARTESIAN_POINT('Ctrl Pts',(-22.290778469048,-2.66553838058246,3.10083513924794));
#42066=CARTESIAN_POINT('Ctrl Pts',(-22.0923053173199,-4.0507904149318,-0.558005764709968));
#42067=CARTESIAN_POINT('Ctrl Pts',(-21.8938321655918,-1.72787581810372,
-3.70603812397624));
#42068=CARTESIAN_POINT('Ctrl Pts',(-21.6953590138636,2.17676747737354,-3.46149631931074));
#42069=CARTESIAN_POINT('Ctrl Pts',(-21.4968858621355,4.08875855029321,-0.0482383307871566));
#42070=CARTESIAN_POINT('Ctrl Pts',(-21.2984127104073,2.25782627589523,3.40917789606675));
#42071=CARTESIAN_POINT('Ctrl Pts',(-21.0999395586792,-1.63996090770976,
3.74577116764184));
#42072=CARTESIAN_POINT('Ctrl Pts',(-20.9014664069511,-4.03649828782243,
0.653417930240319));
#42073=CARTESIAN_POINT('Ctrl Pts',(-20.702993255223,-2.73795230777559,-3.03708586962885));
#42074=CARTESIAN_POINT('Ctrl Pts',(-20.5045201034949,1.06696461361248,-3.94738646859561));
#42075=CARTESIAN_POINT('Ctrl Pts',(-20.3060469517667,3.89516287726385,-1.24417827450031));
#42076=CARTESIAN_POINT('Ctrl Pts',(-20.1075738000386,3.15765876558903,2.59797315984052));
#42077=CARTESIAN_POINT('Ctrl Pts',(-19.9091006483104,-0.47042315135575,
4.06189309039781));
#42078=CARTESIAN_POINT('Ctrl Pts',(-19.7106274965824,-3.66787122806022,
1.80748280033891));
#42079=CARTESIAN_POINT('Ctrl Pts',(-19.5121543448542,-3.50768380597088,
-2.10152985619589));
#42080=CARTESIAN_POINT('Ctrl Pts',(-19.3136811931261,-0.136499341408789,
-4.08676416605462));
#42081=CARTESIAN_POINT('Ctrl Pts',(-19.1152080413979,3.3596390830333,-2.33090082391081));
#42082=CARTESIAN_POINT('Ctrl Pts',(-18.9167348896698,3.78030327543875,1.55871118712222));
#42083=CARTESIAN_POINT('Ctrl Pts',(-18.7182617379417,0.740409644353662,
4.02145085481609));
#42084=CARTESIAN_POINT('Ctrl Pts',(-18.5197885862136,-2.9772683338242,2.80288185401394));
#42085=CARTESIAN_POINT('Ctrl Pts',(-18.3213154344854,-3.9695011626178,-0.981495766230743));
#42086=CARTESIAN_POINT('Ctrl Pts',(-18.1228422827573,-1.32798100844273,
-3.86739445368175));
#42087=CARTESIAN_POINT('Ctrl Pts',(-17.9243691310291,2.52919692061813,-3.2130104817583));
#42088=CARTESIAN_POINT('Ctrl Pts',(-17.725895979301,4.07110235615733,0.382621255085668));
#42089=CARTESIAN_POINT('Ctrl Pts',(-17.5274228275729,1.88624724304817,3.62799459167821));
#42090=CARTESIAN_POINT('Ctrl Pts',(-17.3289496758448,-2.02531262848022,
3.55223622188495));
#42091=CARTESIAN_POINT('Ctrl Pts',(-17.1304765241166,-4.08286477871325,
0.224696724265731));
#42092=CARTESIAN_POINT('Ctrl Pts',(-16.9320033723885,-2.40288884646982,
-3.30853420877946));
#42093=CARTESIAN_POINT('Ctrl Pts',(-16.7335302206604,1.47673488933885,-3.81307323372661));
#42094=CARTESIAN_POINT('Ctrl Pts',(-16.5350570689322,4.0045288638356,-0.827056224122942));
#42095=CARTESIAN_POINT('Ctrl Pts',(-16.3365839172041,2.86650486569058,2.91606297499303));
#42096=CARTESIAN_POINT('Ctrl Pts',(-16.138110765476,-0.895569404687675,
3.98976551448081));
#42097=CARTESIAN_POINT('Ctrl Pts',(-15.9396376137478,-3.83782328393318,
1.41116471769011));
#42098=CARTESIAN_POINT('Ctrl Pts',(-15.7411644620197,-3.26686448612226,
-2.45924172225226));
#42099=CARTESIAN_POINT('Ctrl Pts',(-15.5426913102916,0.294641003851046,
-4.07841391940575));
#42100=CARTESIAN_POINT('Ctrl Pts',(-15.3442181585635,3.5864268029142,-1.96413243099634));
#42101=CARTESIAN_POINT('Ctrl Pts',(-15.1457450068353,3.5951327994024,1.94815132210359));
#42102=CARTESIAN_POINT('Ctrl Pts',(-14.9472718551072,0.312789367054645,
4.07706220592849));
#42103=CARTESIAN_POINT('Ctrl Pts',(-14.7487987033791,-3.255887095317,2.47375678709552));
#42104=CARTESIAN_POINT('Ctrl Pts',(-14.5503255516509,-3.84406576712621,
-1.39407022676811));
#42105=CARTESIAN_POINT('Ctrl Pts',(-14.3518523999228,-0.913317280135754,
-3.98574020289311));
#42106=CARTESIAN_POINT('Ctrl Pts',(-14.1533792481947,2.85349832338418,-2.92879168559267));
#42107=CARTESIAN_POINT('Ctrl Pts',(-13.9549060964666,4.00817007816534,0.809225582673443));
#42108=CARTESIAN_POINT('Ctrl Pts',(-13.7564329447384,1.49369062701152,3.80646315231487));
#42109=CARTESIAN_POINT('Ctrl Pts',(-13.5579597930103,-2.38814017363929,
3.31919567519045));
#42110=CARTESIAN_POINT('Ctrl Pts',(-13.3594866412822,-4.0838243719331,-0.206523408741399));
#42111=CARTESIAN_POINT('Ctrl Pts',(-13.161013489554,-2.04110205880377,-3.54318723816566));
#42112=CARTESIAN_POINT('Ctrl Pts',(-12.9625403378259,1.8700819050158,-3.63635354272455));
#42113=CARTESIAN_POINT('Ctrl Pts',(-12.7640671860978,4.06935915250997,-0.400736206295686));
#42114=CARTESIAN_POINT('Ctrl Pts',(-12.5655940343697,2.54347161142596,3.20172228355665));
#42115=CARTESIAN_POINT('Ctrl Pts',(-12.3671208826415,-1.31075573269272,
3.87326642878672));
#42116=CARTESIAN_POINT('Ctrl Pts',(-12.1686477309134,-3.96509363012978,
0.999152602687558));
#42117=CARTESIAN_POINT('Ctrl Pts',(-11.9701745791853,-2.9897132793594,-2.7896035428668));
#42118=CARTESIAN_POINT('Ctrl Pts',(-11.7717014274571,0.722504548472898,
-4.0247062745732));
#42119=CARTESIAN_POINT('Ctrl Pts',(-11.573228275729,3.77332867702978,-1.57552026780286));
#42120=CARTESIAN_POINT('Ctrl Pts',(-11.3747551240009,3.36997965531711,2.31592541803525));
#42121=CARTESIAN_POINT('Ctrl Pts',(-11.1762819722727,-0.118309544867903,
4.08733119171252));
#42122=CARTESIAN_POINT('Ctrl Pts',(-10.9778088205446,-3.49829605311116,
2.11712024786968));
#42123=CARTESIAN_POINT('Ctrl Pts',(-10.7793356688165,-3.67587923722566,
-1.79114076847305));
#42124=CARTESIAN_POINT('Ctrl Pts',(-10.5808625170884,-0.488496246473859,
-4.05975920915685));
#42125=CARTESIAN_POINT('Ctrl Pts',(-10.3823893653602,3.1460650218686,-2.61200082261243));
#42126=CARTESIAN_POINT('Ctrl Pts',(-10.1839162136321,3.90066160711989,1.22683024330753));
#42127=CARTESIAN_POINT('Ctrl Pts',(-9.98544306190397,1.08452218052527,3.94259876973319));
#42128=CARTESIAN_POINT('Ctrl Pts',(-9.78696991017584,-2.7244084173359,3.04924124901626));
#42129=CARTESIAN_POINT('Ctrl Pts',(-9.5884967584477,-4.0393663955265,-0.635446726204635));
#42130=CARTESIAN_POINT('Ctrl Pts',(-9.39002360671958,-1.65661549601823,
-3.73843530337295));
#42131=CARTESIAN_POINT('Ctrl Pts',(-9.19155045499145,2.24263111760604,-3.41919275407193));
#42132=CARTESIAN_POINT('Ctrl Pts',(-8.99307730326332,4.08893274407603,0.0300405322163189));
#42133=CARTESIAN_POINT('Ctrl Pts',(-8.79460415153519,2.19215156309674,3.45177417331515));
#42134=CARTESIAN_POINT('Ctrl Pts',(-8.59613099980706,-1.71136471007461,
3.71369145840958));
#42135=CARTESIAN_POINT('Ctrl Pts',(-8.39765784807893,-4.04826685078408,
0.576028579148569));
#42136=CARTESIAN_POINT('Ctrl Pts',(-8.1991846963508,-2.67931247646759,-3.0889412543132));
#42137=CARTESIAN_POINT('Ctrl Pts',(-8.00071154462267,1.14233287961659,-3.92623853214494));
#42138=CARTESIAN_POINT('Ctrl Pts',(-7.80223839289453,3.91826610745135,-1.16938621949784));
#42139=CARTESIAN_POINT('Ctrl Pts',(-7.60376524116641,3.10734784621199,2.65794333682912));
#42140=CARTESIAN_POINT('Ctrl Pts',(-7.40529208943829,-0.548092696977365,
4.05214360736044));
#42141=CARTESIAN_POINT('Ctrl Pts',(-7.20681893771015,-3.70179929653215,
1.73693850995084));
#42142=CARTESIAN_POINT('Ctrl Pts',(-7.00834578598201,-3.46681203127418,
-2.16829143773666));
#42143=CARTESIAN_POINT('Ctrl Pts',(-6.8098726342539,-0.058242483521796,
-4.08862828247588));
#42144=CARTESIAN_POINT('Ctrl Pts',(-6.61139948252575,3.40364328447616,-2.26616102940976));
#42145=CARTESIAN_POINT('Ctrl Pts',(-6.41292633079764,3.74977258049331,1.63079091661213));
#42146=CARTESIAN_POINT('Ctrl Pts',(-6.2144531790695,0.663292402032029,4.03488743443219));
#42147=CARTESIAN_POINT('Ctrl Pts',(-6.01598002734137,-3.03037760856484,
2.74537519636395));
#42148=CARTESIAN_POINT('Ctrl Pts',(-5.81750687561324,-3.9499852814079,-1.05730302921229));
#42149=CARTESIAN_POINT('Ctrl Pts',(-5.61903372388512,-1.25370516116971,
-3.89210698567597));
#42150=CARTESIAN_POINT('Ctrl Pts',(-5.42056057215698,2.59023928348237,-3.16400598520845));
#42151=CARTESIAN_POINT('Ctrl Pts',(-5.22208742042886,4.06303195387578,0.460483180078377));
#42152=CARTESIAN_POINT('Ctrl Pts',(-5.02361426870073,1.81645186829979,3.6634377338051));
#42153=CARTESIAN_POINT('Ctrl Pts',(-4.82514111697259,-2.09294103195811,
3.51281529007031));
#42154=CARTESIAN_POINT('Ctrl Pts',(-4.62666796524447,-4.08641794720157,
0.146498349393829));
#42155=CARTESIAN_POINT('Ctrl Pts',(-4.42819481351633,-2.33911415117824,
-3.35392582091246));
#42156=CARTESIAN_POINT('Ctrl Pts',(-4.2297216617882,1.54945695270031,-3.78410578731147));
#42157=CARTESIAN_POINT('Ctrl Pts',(-4.03124851006007,4.01962718536272,-0.750247032867542));
#42158=CARTESIAN_POINT('Ctrl Pts',(-3.83277535833195,2.81015820967587,2.97040137366801));
#42159=CARTESIAN_POINT('Ctrl Pts',(-3.63430220660382,-0.971780369637932,
3.97189080434176));
#42160=CARTESIAN_POINT('Ctrl Pts',(-3.43582905487568,-3.86413351836361,
1.33743966530148));
#42161=CARTESIAN_POINT('Ctrl Pts',(-3.23735590314755,-3.219189408103,-2.52132774831895));
#42162=CARTESIAN_POINT('Ctrl Pts',(-3.03888275141943,0.372659305824992,
-4.07202649063205));
#42163=CARTESIAN_POINT('Ctrl Pts',(-2.8404095996913,3.62336793852966,-1.8951182561049));
#42164=CARTESIAN_POINT('Ctrl Pts',(-2.64193644796316,3.55718215462882,2.01661454478224));
#42165=CARTESIAN_POINT('Ctrl Pts',(-2.44346329623504,0.234683883134984,
4.08230368521807));
#42166=CARTESIAN_POINT('Ctrl Pts',(-2.24499014450691,-3.30264105137573,
2.41097516903988));
#42167=CARTESIAN_POINT('Ctrl Pts',(-2.04651699277877,-3.81668254578493,
-1.4673973788029));
#42168=CARTESIAN_POINT('Ctrl Pts',(-1.84804384105064,-0.836837650855956,
-4.00249962847716));
#42169=CARTESIAN_POINT('Ctrl Pts',(-1.64957068932252,2.90901318244003,-2.87361905689455));
#42170=CARTESIAN_POINT('Ctrl Pts',(-1.45109753759438,3.99199714630452,0.885781316882712));
#42171=CARTESIAN_POINT('Ctrl Pts',(-1.25262438586625,1.42045076229673,3.83440359121586));
#42172=CARTESIAN_POINT('Ctrl Pts',(-1.05415123413812,-2.45104972378982,
3.27278662218134));
#42173=CARTESIAN_POINT('Ctrl Pts',(-0.855678082410002,-4.07948859958104,
-0.28449794668778));
#42174=CARTESIAN_POINT('Ctrl Pts',(-0.657204930681864,-1.97220141068763,
-3.58192268475822));
#42175=CARTESIAN_POINT('Ctrl Pts',(-0.458731778953736,1.93800556216186,
-3.59928830058453));
#42176=CARTESIAN_POINT('Ctrl Pts',(-0.26025862722561,4.07889020629659,-0.323938792483296));
#42177=CARTESIAN_POINT('Ctrl Pts',(-0.0617854754974834,2.47640913824184,
3.25230520610813));
#42178=CARTESIAN_POINT('Ctrl Pts',(0.070529958987943,-0.0890080456892121,
3.64468494608818));
#42179=CARTESIAN_POINT('Ctrl Pts',(0.136687676230653,-1.17148016637959,
3.25511512389028));
#42180=CARTESIAN_POINT('Ctrl Pts',(-54.7036876762307,-1.64343044862466,
3.31080057131706));
#42181=CARTESIAN_POINT('Ctrl Pts',(-54.6375299589879,-2.74442048406567,
2.76428606254484));
#42182=CARTESIAN_POINT('Ctrl Pts',(-54.5052145245025,-4.33928981056137,
0.495999601472129));
#42183=CARTESIAN_POINT('Ctrl Pts',(-54.3067413727745,-2.76702521143321,
-3.38463735892371));
#42184=CARTESIAN_POINT('Ctrl Pts',(-54.1082682210462,1.34187477797974,-4.15638860970085));
#42185=CARTESIAN_POINT('Ctrl Pts',(-53.9097950693182,4.22052442796764,-1.12856074917905));
#42186=CARTESIAN_POINT('Ctrl Pts',(-53.71132191759,3.23660588578034,2.93509109597859));
#42187=CARTESIAN_POINT('Ctrl Pts',(-53.512848765862,-0.710670000578388,
4.31048894467319));
#42188=CARTESIAN_POINT('Ctrl Pts',(-53.3143756141337,-4.00711916051023,
1.7407288929608));
#42189=CARTESIAN_POINT('Ctrl Pts',(-53.1159024624056,-3.6355185340518,-2.42291345406673));
#42190=CARTESIAN_POINT('Ctrl Pts',(-52.9174293106775,0.0641742371961704,
-4.36837440997313));
#42191=CARTESIAN_POINT('Ctrl Pts',(-52.7189561589494,3.70508264242447,-2.31505260596812));
#42192=CARTESIAN_POINT('Ctrl Pts',(-52.5204830072212,3.95431147698897,1.8575655438389));
#42193=CARTESIAN_POINT('Ctrl Pts',(-52.3220098554931,0.583681820532341,
4.32970570060305));
#42194=CARTESIAN_POINT('Ctrl Pts',(-52.123536703765,-3.32125525664554,2.83837029465124));
#42195=CARTESIAN_POINT('Ctrl Pts',(-51.9250635520368,-4.18585819809453,
-1.25126841311442));
#42196=CARTESIAN_POINT('Ctrl Pts',(-51.7265904003087,-1.21864953295622,
-4.19546929666802));
#42197=CARTESIAN_POINT('Ctrl Pts',(-51.5281172485806,2.86413212282785,-3.2990640568009));
#42198=CARTESIAN_POINT('Ctrl Pts',(-51.3296440968525,4.32503596533597,0.617365075992241));
#42199=CARTESIAN_POINT('Ctrl Pts',(-51.1311709451243,1.82672363883074,3.96864648723083));
#42200=CARTESIAN_POINT('Ctrl Pts',(-50.9326977933962,-2.34380435348219,
3.6869576105009));
#42201=CARTESIAN_POINT('Ctrl Pts',(-50.7342246416681,-4.36877161136301,
0.0301610541736334));
#42202=CARTESIAN_POINT('Ctrl Pts',(-50.5357514899399,-2.39448648330802,
-3.65424539063146));
#42203=CARTESIAN_POINT('Ctrl Pts',(-50.3372783382118,1.77175475755383,-3.99348971834736));
#42204=CARTESIAN_POINT('Ctrl Pts',(-50.1388051864837,4.31609973524516,-0.677021483217761));
#42205=CARTESIAN_POINT('Ctrl Pts',(-49.9403320347555,2.90940913881518,3.25920442052877));
#42206=CARTESIAN_POINT('Ctrl Pts',(-49.7418588830275,-1.16060707327924,
4.21189580069286));
#42207=CARTESIAN_POINT('Ctrl Pts',(-49.5433857312992,-4.16818263172822,
1.3089417695408));
#42208=CARTESIAN_POINT('Ctrl Pts',(-49.3449125795711,-3.36012860510288,
-2.79224117196468));
#42209=CARTESIAN_POINT('Ctrl Pts',(-49.1464394278431,0.523847770568201,
-4.33735616726239));
#42210=CARTESIAN_POINT('Ctrl Pts',(-48.9479662761149,3.92828444584205,-1.91197707093674));
#42211=CARTESIAN_POINT('Ctrl Pts',(-48.7494931243868,3.7366986642368,2.26366033223368));
#42212=CARTESIAN_POINT('Ctrl Pts',(-48.5510199726586,0.12447150700683,4.36710222589484));
#42213=CARTESIAN_POINT('Ctrl Pts',(-48.3525468209305,-3.60169911350682,
2.47281994958047));
#42214=CARTESIAN_POINT('Ctrl Pts',(-48.1540736692024,-4.03080938276955,
-1.68512632376529));
#42215=CARTESIAN_POINT('Ctrl Pts',(-47.9556005174743,-0.770044018205449,
-4.30047755689456));
#42216=CARTESIAN_POINT('Ctrl Pts',(-47.7571273657461,3.19563353394943,-2.97909404416766));
#42217=CARTESIAN_POINT('Ctrl Pts',(-47.558654214018,4.23597049272536,1.06940590612676));
#42218=CARTESIAN_POINT('Ctrl Pts',(-47.3601810622898,1.39862363604842,4.13895239547316));
#42219=CARTESIAN_POINT('Ctrl Pts',(-47.1617079105618,-2.71904853137658,
3.41962718601319));
#42220=CARTESIAN_POINT('Ctrl Pts',(-46.9632347588336,-4.34765461544227,
-0.43008644727046));
#42221=CARTESIAN_POINT('Ctrl Pts',(-46.7647616071055,-1.99633922308703,
-3.8860911869985));
#42222=CARTESIAN_POINT('Ctrl Pts',(-46.5662884553773,2.18246111252143,-3.78469794034269));
#42223=CARTESIAN_POINT('Ctrl Pts',(-46.3678153036492,4.36339716923192,-0.218723914653743));
#42224=CARTESIAN_POINT('Ctrl Pts',(-46.169342151921,2.55000073175133,3.54747392877952));
#42225=CARTESIAN_POINT('Ctrl Pts',(-45.970869000193,-1.59771238330974,4.06625013341793));
#42226=CARTESIAN_POINT('Ctrl Pts',(-45.7723958484648,-4.28285075637247,
0.862707601648684));
#42227=CARTESIAN_POINT('Ctrl Pts',(-45.5739226967367,-3.04739027481367,
-3.13057303385079));
#42228=CARTESIAN_POINT('Ctrl Pts',(-45.3754495450085,0.977706246068333,
-4.25807063160085));
#42229=CARTESIAN_POINT('Ctrl Pts',(-45.1769763932805,4.10779282928477,-1.48765354803437));
#42230=CARTESIAN_POINT('Ctrl Pts',(-44.9785032415523,3.47753174277359,2.644588434011));
#42231=CARTESIAN_POINT('Ctrl Pts',(-44.7800300898242,-0.336124643548603,
4.35592644925301));
#42232=CARTESIAN_POINT('Ctrl Pts',(-44.581556938096,-3.84208646672359,2.07977080216117));
#42233=CARTESIAN_POINT('Ctrl Pts',(-44.3830837863679,-3.83093301839846,
-2.1002445609612));
#42234=CARTESIAN_POINT('Ctrl Pts',(-44.1846106346398,-0.312874366403276,
-4.35765815985495));
#42235=CARTESIAN_POINT('Ctrl Pts',(-43.9861374829117,3.4915951255531,-2.62599285728587));
#42236=CARTESIAN_POINT('Ctrl Pts',(-43.7876643311835,4.09979544336713,1.50955368564645));
#42237=CARTESIAN_POINT('Ctrl Pts',(-43.5891911794554,0.954969042813313,
4.26322754900215));
#42238=CARTESIAN_POINT('Ctrl Pts',(-43.3907180277272,-3.06405324931624,
3.1142659958098));
#42239=CARTESIAN_POINT('Ctrl Pts',(-43.1922448759992,-4.2781859146255,-0.885550838293665));
#42240=CARTESIAN_POINT('Ctrl Pts',(-42.993771724271,-1.57599000561263,-4.07471845769885));
#42241=CARTESIAN_POINT('Ctrl Pts',(-42.7952985725428,2.5688955889342,-3.53381528386206));
#42242=CARTESIAN_POINT('Ctrl Pts',(-42.5968254208148,4.36216781272975,0.242006158779532));
#42243=CARTESIAN_POINT('Ctrl Pts',(-42.3983522690865,2.1622329174566,3.79629079734019));
#42244=CARTESIAN_POINT('Ctrl Pts',(-42.1998791173585,-2.01704900199012,
3.87538234641091));
#42245=CARTESIAN_POINT('Ctrl Pts',(-42.0014059656303,-4.34988787292489,
0.406878974983359));
#42246=CARTESIAN_POINT('Ctrl Pts',(-41.8029328139022,-2.70076090324605,
-3.43408875115367));
#42247=CARTESIAN_POINT('Ctrl Pts',(-41.6044596621741,1.4206913250513,-4.13142967581763));
#42248=CARTESIAN_POINT('Ctrl Pts',(-41.4059865104459,4.24161708193722,-1.04678533497605));
#42249=CARTESIAN_POINT('Ctrl Pts',(-41.2075133587178,3.17969003372768,2.99610518785898));
#42250=CARTESIAN_POINT('Ctrl Pts',(-41.0090402069897,-0.792982640099472,
4.2963069652672));
#42251=CARTESIAN_POINT('Ctrl Pts',(-40.8105670552616,-4.03974469799334,
1.66359183165144));
#42252=CARTESIAN_POINT('Ctrl Pts',(-40.6120939035334,-3.58845157328471,
-2.49200527958776));
#42253=CARTESIAN_POINT('Ctrl Pts',(-40.4136207518053,0.147774865327506,
-4.36637579652508));
#42254=CARTESIAN_POINT('Ctrl Pts',(-40.2151476000772,3.74872552602871,-2.24368713010601));
#42255=CARTESIAN_POINT('Ctrl Pts',(-40.016674448349,3.91802520478279,1.93291321636264));
#42256=CARTESIAN_POINT('Ctrl Pts',(-39.8182012966209,0.500693921112148,
4.34008993048116));
#42257=CARTESIAN_POINT('Ctrl Pts',(-39.6197281448928,-3.37498161158642,
2.77427001727592));
#42258=CARTESIAN_POINT('Ctrl Pts',(-39.4212549931647,-4.16113808479721,
-1.33116672380013));
#42259=CARTESIAN_POINT('Ctrl Pts',(-39.2227818414366,-1.1381136789162,-4.21802942867477));
#42260=CARTESIAN_POINT('Ctrl Pts',(-39.0243086897083,2.92676052276938,-3.24363189182457));
#42261=CARTESIAN_POINT('Ctrl Pts',(-38.8258355379803,4.3124253365845,0.700044801199802));
#42262=CARTESIAN_POINT('Ctrl Pts',(-38.6273623862521,1.75041819146013,4.00288785282676));
#42263=CARTESIAN_POINT('Ctrl Pts',(-38.428889234524,-2.41395334759883,3.64141514289692));
#42264=CARTESIAN_POINT('Ctrl Pts',(-38.2304160827959,-4.36854843913065,
-0.0534746881410977));
#42265=CARTESIAN_POINT('Ctrl Pts',(-38.0319429310678,-2.32409547106562,
-3.69941282485139));
#42266=CARTESIAN_POINT('Ctrl Pts',(-37.8334697793396,1.84787642311034,-3.95884171598405));
#42267=CARTESIAN_POINT('Ctrl Pts',(-37.6349966276115,4.32826889973387,-0.594275473916914));
#42268=CARTESIAN_POINT('Ctrl Pts',(-37.4365234758834,2.84648593385764,3.31430125903684));
#42269=CARTESIAN_POINT('Ctrl Pts',(-37.2380503241552,-1.24102161286549,
4.18890682203643));
#42270=CARTESIAN_POINT('Ctrl Pts',(-37.0395771724271,-4.1924755843569,1.22891150286507));
#42271=CARTESIAN_POINT('Ctrl Pts',(-36.841104020699,-3.30606176426067,-2.85605157835015));
#42272=CARTESIAN_POINT('Ctrl Pts',(-36.6426308689708,0.606780643612692,
-4.32653351516425));
#42273=CARTESIAN_POINT('Ctrl Pts',(-36.4441577172427,3.96416510263855,-1.83642861182384));
#42274=CARTESIAN_POINT('Ctrl Pts',(-36.2456845655146,3.69268130427524,2.33477617607313));
#42275=CARTESIAN_POINT('Ctrl Pts',(-36.0472114137865,0.040850415721449,
4.36868472779142));
#42276=CARTESIAN_POINT('Ctrl Pts',(-35.8487382620583,-3.64837568041693,
2.40342045881384));
#42277=CARTESIAN_POINT('Ctrl Pts',(-35.6502651103302,-3.9978128538176,-1.76197826126017));
#42278=CARTESIAN_POINT('Ctrl Pts',(-35.4517919586021,-0.68758001131886,
-4.31443029093499));
#42279=CARTESIAN_POINT('Ctrl Pts',(-35.2533188068739,3.25207597902751,-2.91737499028409));
#42280=CARTESIAN_POINT('Ctrl Pts',(-35.0548456551459,4.21472294342388,1.15029801246422));
#42281=CARTESIAN_POINT('Ctrl Pts',(-34.8563725034176,1.31913648235043,4.16496746064537));
#42282=CARTESIAN_POINT('Ctrl Pts',(-34.6578993516896,-2.7840113148488,3.36695054999275));
#42283=CARTESIAN_POINT('Ctrl Pts',(-34.4594261999614,-4.33862492462412,
-0.513233641466429));
#42284=CARTESIAN_POINT('Ctrl Pts',(-34.2609530482333,-1.92158299986923,
-3.92359449764067));
#42285=CARTESIAN_POINT('Ctrl Pts',(-34.0624798965052,2.25451067263522,-3.74222616022556));
#42286=CARTESIAN_POINT('Ctrl Pts',(-33.864006744777,4.36678459897784,-0.135156477582659));
#42287=CARTESIAN_POINT('Ctrl Pts',(-33.6655335930489,2.48162511682313,3.59563788316554));
#42288=CARTESIAN_POINT('Ctrl Pts',(-33.4670604413208,-1.67525877135726,
4.03492045228817));
#42289=CARTESIAN_POINT('Ctrl Pts',(-33.2685872895926,-4.29858055480978,
0.78056404036699));
#42290=CARTESIAN_POINT('Ctrl Pts',(-33.0701141378645,-2.98690414235031,
-3.18833477723296));
#42291=CARTESIAN_POINT('Ctrl Pts',(-32.8716409861363,1.0590382124698,-4.23857441503996));
#42292=CARTESIAN_POINT('Ctrl Pts',(-32.6731678344083,4.13551788016929,-1.40874655992579));
#42293=CARTESIAN_POINT('Ctrl Pts',(-32.4746946826801,3.42626986633934,2.71067331309355));
#42294=CARTESIAN_POINT('Ctrl Pts',(-32.276221530952,-0.419447400734403,
4.34869392867786));
#42295=CARTESIAN_POINT('Ctrl Pts',(-32.0777483792239,-3.88119494940355,
2.00584166175373));
#42296=CARTESIAN_POINT('Ctrl Pts',(-31.8792752274957,-3.79002661592259,
-2.17319425222436));
#42297=CARTESIAN_POINT('Ctrl Pts',(-31.6808020757676,-0.229399537641264,
-4.36284893841544));
#42298=CARTESIAN_POINT('Ctrl Pts',(-31.4823289240394,3.54122401627932,-2.55867299079608));
#42299=CARTESIAN_POINT('Ctrl Pts',(-31.2838557723114,4.07014721407014,1.58775837680034));
#42300=CARTESIAN_POINT('Ctrl Pts',(-31.0853826205832,0.873184217512199,
4.28072707954971));
#42301=CARTESIAN_POINT('Ctrl Pts',(-30.8869094688551,-3.12310736595907,
3.05504097975702));
#42302=CARTESIAN_POINT('Ctrl Pts',(-30.688436317127,-4.26045011876644,-0.967284752699883));
#42303=CARTESIAN_POINT('Ctrl Pts',(-30.4899631653988,-1.49769996477461,
-4.10414057054783));
#42304=CARTESIAN_POINT('Ctrl Pts',(-30.2914900136707,2.63607175884002,-3.48399206221092));
#42305=CARTESIAN_POINT('Ctrl Pts',(-30.0930168619426,4.35673583376276,0.325465638908587));
#42306=CARTESIAN_POINT('Ctrl Pts',(-29.8945437102144,2.08916532116829,3.83698622204075));
#42307=CARTESIAN_POINT('Ctrl Pts',(-29.6960705584864,-2.09086481965406,
3.8360603896753));
#42308=CARTESIAN_POINT('Ctrl Pts',(-29.4975974067581,-4.35687958067188,
0.323535665463647));
#42309=CARTESIAN_POINT('Ctrl Pts',(-29.2991242550301,-2.63452816565838,
-3.48515944422279));
#42310=CARTESIAN_POINT('Ctrl Pts',(-29.1006511033019,1.49951786499866,-4.10347671857079));
#42311=CARTESIAN_POINT('Ctrl Pts',(-28.9021779515738,4.2608781873688,-0.965397368811076));
#42312=CARTESIAN_POINT('Ctrl Pts',(-28.7037047998456,3.12175374121783,3.05642415029312));
#42313=CARTESIAN_POINT('Ctrl Pts',(-28.5052316481175,-0.875080403086531,
4.28033985746888));
#42314=CARTESIAN_POINT('Ctrl Pts',(-28.3067584963894,-4.07085015799139,
1.58595523218163));
#42315=CARTESIAN_POINT('Ctrl Pts',(-28.1082853446612,-3.54009023099919,
-2.56024142683588));
#42316=CARTESIAN_POINT('Ctrl Pts',(-27.9098121929331,0.231332164621206,
-4.36274689122739));
#42317=CARTESIAN_POINT('Ctrl Pts',(-27.711339041205,3.79098892299601,-2.17151513764563));
#42318=CARTESIAN_POINT('Ctrl Pts',(-27.5128658894769,3.8803060233133,2.00756075194279));
#42319=CARTESIAN_POINT('Ctrl Pts',(-27.3143927377488,0.417520980461716,
4.34887930830195));
#42320=CARTESIAN_POINT('Ctrl Pts',(-27.1159195860206,-3.42747030091991,
2.70915528230011));
#42321=CARTESIAN_POINT('Ctrl Pts',(-26.9174464342925,-4.13489342958415,
-1.41057836835976));
#42322=CARTESIAN_POINT('Ctrl Pts',(-26.7189732825644,-1.05716051005105,
-4.2390431306241));
#42323=CARTESIAN_POINT('Ctrl Pts',(-26.5205001308362,2.98831621393063,-3.18701132926479));
#42324=CARTESIAN_POINT('Ctrl Pts',(-26.3220269791081,4.29823435975001,0.782468143739444));
#42325=CARTESIAN_POINT('Ctrl Pts',(-26.12355382738,1.67347122286134,4.0356621604834));
#42326=CARTESIAN_POINT('Ctrl Pts',(-25.9250806756518,-2.48321766461065,
3.59453822311966));
#42327=CARTESIAN_POINT('Ctrl Pts',(-25.7266075239237,-4.36672429907916,
-0.13709085722334));
#42328=CARTESIAN_POINT('Ctrl Pts',(-25.5281343721955,-2.25285272466553,
-3.7432244934374));
#42329=CARTESIAN_POINT('Ctrl Pts',(-25.3296612204675,1.92332088042537,-3.92274289218939));
#42330=CARTESIAN_POINT('Ctrl Pts',(-25.1311880687393,4.33885185055037,-0.511311672346996));
#42331=CARTESIAN_POINT('Ctrl Pts',(-24.9327149170112,2.78251955405799,3.36818347757181));
#42332=CARTESIAN_POINT('Ctrl Pts',(-24.734241765283,-1.32098134511574,4.16438270253336));
#42333=CARTESIAN_POINT('Ctrl Pts',(-24.5357686135549,-4.21523208750278,
1.14843086678717));
#42334=CARTESIAN_POINT('Ctrl Pts',(-24.3372954618268,-3.25078332474412,
-2.91881530468582));
#42335=CARTESIAN_POINT('Ctrl Pts',(-24.1388223100987,0.689491144911088,
-4.31412528427163));
#42336=CARTESIAN_POINT('Ctrl Pts',(-23.9403491583705,3.99859298054725,-1.76020714213438));
#42337=CARTESIAN_POINT('Ctrl Pts',(-23.7418760066424,3.64731065820044,2.40503637599935));
#42338=CARTESIAN_POINT('Ctrl Pts',(-23.5434028549143,-0.0427856463317108,
4.36866620329026));
#42339=CARTESIAN_POINT('Ctrl Pts',(-23.3449297031862,-3.69371519826275,
2.33314016754789));
#42340=CARTESIAN_POINT('Ctrl Pts',(-23.146456551458,-3.96335121479337,-1.83818447265194));
#42341=CARTESIAN_POINT('Ctrl Pts',(-22.9479833997299,-0.604864021552577,
-4.32680188161348));
#42342=CARTESIAN_POINT('Ctrl Pts',(-22.7495102480017,3.30732661012167,-2.85458678293089));
#42343=CARTESIAN_POINT('Ctrl Pts',(-22.5510370962736,4.19193079129697,1.23076855999775));
#42344=CARTESIAN_POINT('Ctrl Pts',(-22.3525639445455,1.23916589428106,4.18945615727784));
#42345=CARTESIAN_POINT('Ctrl Pts',(-22.1540907928174,-2.84795381969309,
3.31304000099578));
#42346=CARTESIAN_POINT('Ctrl Pts',(-21.9556176410892,-4.32800522364261,
-0.596192746873735));
#42347=CARTESIAN_POINT('Ctrl Pts',(-21.7571444893611,-1.84612255894362,
-3.95965989760005));
#42348=CARTESIAN_POINT('Ctrl Pts',(-21.558671337633,2.32573400440593,-3.69838293691345));
#42349=CARTESIAN_POINT('Ctrl Pts',(-21.3601981859049,4.36857169866203,-0.0515395086490985));
#42350=CARTESIAN_POINT('Ctrl Pts',(-21.1617250341767,2.41234004112657,3.64248411572105));
#42351=CARTESIAN_POINT('Ctrl Pts',(-20.9632518824486,-1.75219121408373,
4.00211206197311));
#42352=CARTESIAN_POINT('Ctrl Pts',(-20.7647787307204,-4.31273501846039,
0.698134419612753));
#42353=CARTESIAN_POINT('Ctrl Pts',(-20.5663055789923,-2.92532337552109,
-3.24492806637258));
#42354=CARTESIAN_POINT('Ctrl Pts',(-20.3678324272642,1.1399820647682,-4.21752485461668));
#42355=CARTESIAN_POINT('Ctrl Pts',(-20.1693592755361,4.16172735513416,-1.32932329733237));
#42356=CARTESIAN_POINT('Ctrl Pts',(-19.970886123808,3.37375233771011,2.77576479030521));
#42357=CARTESIAN_POINT('Ctrl Pts',(-19.7724129720798,-0.502616439716474,
4.3398677078719));
#42358=CARTESIAN_POINT('Ctrl Pts',(-19.5739398203517,-3.91888105989819,
1.93117742470076));
#42359=CARTESIAN_POINT('Ctrl Pts',(-19.3754666686235,-3.747731252441,-2.24534751581572));
#42360=CARTESIAN_POINT('Ctrl Pts',(-19.1769935168955,-0.145840639017714,
-4.36644082924682));
#42361=CARTESIAN_POINT('Ctrl Pts',(-18.9785203651673,3.58955512665475,-2.49041542719466));
#42362=CARTESIAN_POINT('Ctrl Pts',(-18.7800472134392,4.03900736575815,1.66538118959415));
#42363=CARTESIAN_POINT('Ctrl Pts',(-18.581574061711,0.791079389490325,4.29665781821478));
#42364=CARTESIAN_POINT('Ctrl Pts',(-18.3831009099829,-3.18101693276428,
2.99469635869308));
#42365=CARTESIAN_POINT('Ctrl Pts',(-18.1846277582548,-4.24115296208294,
-1.04866417861854));
#42366=CARTESIAN_POINT('Ctrl Pts',(-17.9861546065267,-1.41886104999451,
-4.1320586065678));
#42367=CARTESIAN_POINT('Ctrl Pts',(-17.7876814547985,2.7022818666961,-3.43289203445551));
#42368=CARTESIAN_POINT('Ctrl Pts',(-17.5892083030704,4.34970720738444,0.40880584307295));
#42369=CARTESIAN_POINT('Ctrl Pts',(-17.3907351513423,2.01533209195444,3.87627547607769));
#42370=CARTESIAN_POINT('Ctrl Pts',(-17.1922619996141,-2.16391438156393,
3.79533260157307));
#42371=CARTESIAN_POINT('Ctrl Pts',(-16.993788847886,-4.36227458832746,0.240073787271785));
#42372=CARTESIAN_POINT('Ctrl Pts',(-16.7953156961578,-2.56732993171374,
-3.53495290336793));
#42373=CARTESIAN_POINT('Ctrl Pts',(-16.5968425444297,1.57779486478368,-4.074019927782));
#42374=CARTESIAN_POINT('Ctrl Pts',(-16.3983693927016,4.27857777509826,-0.88365560584303));
#42375=CARTESIAN_POINT('Ctrl Pts',(-16.1998962409735,3.06267339494391,3.11562300081466));
#42376=CARTESIAN_POINT('Ctrl Pts',(-16.0014230892454,-0.956857468442627,
4.26280409969637));
#42377=CARTESIAN_POINT('Ctrl Pts',(-15.8029499375172,-4.10046374136095,
1.50773741516452));
#42378=CARTESIAN_POINT('Ctrl Pts',(-15.6044767857891,-3.49043152387025,
-2.62753930217525));
#42379=CARTESIAN_POINT('Ctrl Pts',(-15.4060036340609,0.31480468578838,-4.35751913559863));
#42380=CARTESIAN_POINT('Ctrl Pts',(-15.2075304823328,3.83186300629334,-2.09854733287175));
#42381=CARTESIAN_POINT('Ctrl Pts',(-15.0090573306047,3.84116479543024,2.08147256086886));
#42382=CARTESIAN_POINT('Ctrl Pts',(-14.8105841788766,0.334195027597992,
4.35607491795439));
#42383=CARTESIAN_POINT('Ctrl Pts',(-14.6121110271484,-3.47870289812566,
2.64304770177813));
#42384=CARTESIAN_POINT('Ctrl Pts',(-14.4136378754203,-4.10713342729877,
-1.48947306711724));
#42385=CARTESIAN_POINT('Ctrl Pts',(-14.2151647236922,-0.975819915219347,
-4.25850331693705));
#42386=CARTESIAN_POINT('Ctrl Pts',(-14.016691571964,3.04877675323287,-3.12922279747697));
#42387=CARTESIAN_POINT('Ctrl Pts',(-13.8182184202359,4.28246817500175,0.864604728994704));
#42388=CARTESIAN_POINT('Ctrl Pts',(-13.6197452685078,1.59591096403841,4.06695748713514));
#42389=CARTESIAN_POINT('Ctrl Pts',(-13.4212721167797,-2.55157193722059,
3.54634398451292));
#42390=CARTESIAN_POINT('Ctrl Pts',(-13.2227989650515,-4.36329985106452,
-0.220656785535732));
#42391=CARTESIAN_POINT('Ctrl Pts',(-13.0243258133234,-2.18078435752364,
-3.78566435296142));
#42392=CARTESIAN_POINT('Ctrl Pts',(-12.8258526615952,1.99806048313776,-3.88520646980645));
#42393=CARTESIAN_POINT('Ctrl Pts',(-12.6273795098672,4.34784470804019,-0.428160486347726));
#42394=CARTESIAN_POINT('Ctrl Pts',(-12.428906358139,2.71753344232774,3.42083133128965));
#42395=CARTESIAN_POINT('Ctrl Pts',(-12.2304332064109,-1.40045696689287,
4.13833242879109));
#42396=CARTESIAN_POINT('Ctrl Pts',(-12.0319600546827,-4.23644380123351,
1.06752935617385));
#42397=CARTESIAN_POINT('Ctrl Pts',(-11.8334869029546,-3.19431354497235,
-2.98050934971));
#42398=CARTESIAN_POINT('Ctrl Pts',(-11.6350137512265,0.771948962940714,
-4.30013602179249));
#42399=CARTESIAN_POINT('Ctrl Pts',(-11.4365405994984,4.03155546248635,-1.68334059542301));
#42400=CARTESIAN_POINT('Ctrl Pts',(-11.2380674477702,3.60060335336482,2.47441518323838));
#42401=CARTESIAN_POINT('Ctrl Pts',(-11.0395942960421,-0.126406028390937,
4.36704665916097));
#42402=CARTESIAN_POINT('Ctrl Pts',(-10.841121144314,-3.73770105110923,2.26200483196645));
#42403=CARTESIAN_POINT('Ctrl Pts',(-10.6426479925859,-3.92743709512795,
-1.91371703005316));
#42404=CARTESIAN_POINT('Ctrl Pts',(-10.4441748408577,-0.521926362488377,
-4.3375877950126));
#42405=CARTESIAN_POINT('Ctrl Pts',(-10.2457016891296,3.36136517909586,-2.79075243260033));
#42406=CARTESIAN_POINT('Ctrl Pts',(-10.0472285374015,4.16760238916512,1.31078805805055));
#42407=CARTESIAN_POINT('Ctrl Pts',(-9.84875538567332,1.15874117929357,4.212409510804));
#42408=CARTESIAN_POINT('Ctrl Pts',(-9.65028223394519,-2.91085261239433,
3.25791529604742));
#42409=CARTESIAN_POINT('Ctrl Pts',(-9.45180908221706,-4.31579940438351,
-0.678933360813514));
#42410=CARTESIAN_POINT('Ctrl Pts',(-9.25333593048893,-1.76998555489433,
-3.99427416970442));
#42411=CARTESIAN_POINT('Ctrl Pts',(-9.05486277876081,2.39610500605629,-3.65318433797894));
#42412=CARTESIAN_POINT('Ctrl Pts',(-8.85638962703267,4.36875781335193,0.0320963483755011));
#42413=CARTESIAN_POINT('Ctrl Pts',(-8.65791647530455,2.34217089611098,3.68799545833686));
#42414=CARTESIAN_POINT('Ctrl Pts',(-8.45944332357642,-1.82848151744868,
3.9678369860229));
#42415=CARTESIAN_POINT('Ctrl Pts',(-8.26097017184828,-4.32530896002622,
0.615448948020644));
#42416=CARTESIAN_POINT('Ctrl Pts',(-8.06249702012015,-2.86267054231623,
-3.30033216107977));
#42417=CARTESIAN_POINT('Ctrl Pts',(-7.86402386839203,1.22050813883025,-4.19492966452973));
#42418=CARTESIAN_POINT('Ctrl Pts',(-7.66555071666389,4.18641164898603,-1.24941286712486));
#42419=CARTESIAN_POINT('Ctrl Pts',(-7.46707756493577,3.31999840339956,2.83983901105795));
#42420=CARTESIAN_POINT('Ctrl Pts',(-7.26860441320764,-0.585601280879622,
4.32945102144992));
#42421=CARTESIAN_POINT('Ctrl Pts',(-7.07013126147951,-3.95513098708112,
1.85580545379544));
#42422=CARTESIAN_POINT('Ctrl Pts',(-6.87165810975138,-3.7040624282691,-2.3166779091587));
#42423=CARTESIAN_POINT('Ctrl Pts',(-6.67318495802324,-0.0622282930241267,
-4.36843251599986));
#42424=CARTESIAN_POINT('Ctrl Pts',(-6.47471180629512,3.63657074439811,-2.42124518137171));
#42425=CARTESIAN_POINT('Ctrl Pts',(-6.27623865456699,4.00638731049232,1.74239367698454));
#42426=CARTESIAN_POINT('Ctrl Pts',(-6.07776550283886,0.708684648362605,
4.31101392672931));
#42427=CARTESIAN_POINT('Ctrl Pts',(-5.87929235111072,-3.2377607271739,2.93325424759644));
#42428=CARTESIAN_POINT('Ctrl Pts',(-5.68081919938259,-4.22030151652084,
-1.1296592923042));
#42429=CARTESIAN_POINT('Ctrl Pts',(-5.48234604765447,-1.33950215406073,
-4.15846233438502));
#42430=CARTESIAN_POINT('Ctrl Pts',(-5.28387289592634,2.76750164809137,-3.38053392768505));
#42431=CARTESIAN_POINT('Ctrl Pts',(-5.08539974419822,4.34108450918146,0.491996229040367));
#42432=CARTESIAN_POINT('Ctrl Pts',(-4.88692659247008,1.94076028853959,3.91414416059468));
#42433=CARTESIAN_POINT('Ctrl Pts',(-4.68845344074195,-2.23617091758218,
3.75321390834575));
#42434=CARTESIAN_POINT('Ctrl Pts',(-4.48998028901382,-4.36607091699489,
0.156523926563516));
#42435=CARTESIAN_POINT('Ctrl Pts',(-4.29150713728569,-2.49919083141846,
-3.58345087889809));
#42436=CARTESIAN_POINT('Ctrl Pts',(-4.09303398555755,1.65549364400027,-4.04307010156087));
#42437=CARTESIAN_POINT('Ctrl Pts',(-3.89456083382943,4.29470934640759,-0.801589997177687));
#42438=CARTESIAN_POINT('Ctrl Pts',(-3.6960876821013,3.00247066989856,3.17368003394153));
#42439=CARTESIAN_POINT('Ctrl Pts',(-3.49761453037318,-1.03828391133824,
4.2437061383287));
#42440=CARTESIAN_POINT('Ctrl Pts',(-3.29914137864504,-4.12857450997301,
1.42896700762253));
#42441=CARTESIAN_POINT('Ctrl Pts',(-3.10066822691691,-3.4394938140484,-2.693874169598));
#42442=CARTESIAN_POINT('Ctrl Pts',(-2.90219507518879,0.398162150355857,
-4.35069458476621));
#42443=CARTESIAN_POINT('Ctrl Pts',(-2.70372192346066,3.87133219910116,-2.02481019052676));
#42444=CARTESIAN_POINT('Ctrl Pts',(-2.50524877173252,3.80061700796258,2.15462104672691));
#42445=CARTESIAN_POINT('Ctrl Pts',(-2.3067756200044,0.250744414810584,4.36167509654208));
#42446=CARTESIAN_POINT('Ctrl Pts',(-2.10830246827627,-3.52865644924059,
2.57596963970611));
#42447=CARTESIAN_POINT('Ctrl Pts',(-1.90982931654813,-4.07787624219031,
-1.56781834409616));
#42448=CARTESIAN_POINT('Ctrl Pts',(-1.71135616482,-0.894106422019328,-4.27640966953572));
#42449=CARTESIAN_POINT('Ctrl Pts',(-1.51288301309188,3.10809075750666,-3.07027444400813));
#42450=CARTESIAN_POINT('Ctrl Pts',(-1.31440986136373,4.26518845267467,0.946399535345616));
#42451=CARTESIAN_POINT('Ctrl Pts',(-1.11593670963561,1.51765894786496,4.09681002284487));
#42452=CARTESIAN_POINT('Ctrl Pts',(-0.917463557907481,-2.61878668638777,
3.49675893979982));
#42453=CARTESIAN_POINT('Ctrl Pts',(-0.718990406179359,-4.35866736123758,
-0.303967491095578));
#42454=CARTESIAN_POINT('Ctrl Pts',(-0.52051725445122,-2.10716851112986,
-3.82705064996035));
#42455=CARTESIAN_POINT('Ctrl Pts',(-0.322044102723092,2.07063247843363,
-3.84560467727572));
#42456=CARTESIAN_POINT('Ctrl Pts',(-0.123570950994966,4.35802801706137,
-0.346107461111702));
#42457=CARTESIAN_POINT('Ctrl Pts',(0.0749022007331604,2.64588156589855,
3.47487588324251));
#42458=CARTESIAN_POINT('Ctrl Pts',(0.207217635218587,-0.0950992885905953,
3.89410803063403));
#42459=CARTESIAN_POINT('Ctrl Pts',(0.273375352461297,-1.25165011272755,
3.47787809703117));
#42460=CARTESIAN_POINT('Ctrl Pts',(-54.567,-1.74869447533071,3.52286199445108));
#42461=CARTESIAN_POINT('Ctrl Pts',(-54.5008422827573,-2.92020446772555,
2.9413424643865));
#42462=CARTESIAN_POINT('Ctrl Pts',(-54.3685268482719,-4.6172274129017,0.527769072056658));
#42463=CARTESIAN_POINT('Ctrl Pts',(-54.1700536965438,-2.9442570596054,-3.60142813193026));
#42464=CARTESIAN_POINT('Ctrl Pts',(-53.9715805448156,1.42782374076287,-4.42261113343342));
#42465=CARTESIAN_POINT('Ctrl Pts',(-53.7731073930875,4.49085494087165,-1.2008466490418));
#42466=CARTESIAN_POINT('Ctrl Pts',(-53.5746342413593,3.44391503517721,3.12308779992807));
#42467=CARTESIAN_POINT('Ctrl Pts',(-53.3761610896313,-0.756189411504974,
4.58658181113279));
#42468=CARTESIAN_POINT('Ctrl Pts',(-53.1776879379031,-4.26378076653011,
1.85222502157982));
#42469=CARTESIAN_POINT('Ctrl Pts',(-52.979214786175,-3.86837859842421,-2.57810446123634));
#42470=CARTESIAN_POINT('Ctrl Pts',(-52.7807416344468,0.0682846871540122,
-4.64817492172454));
#42471=CARTESIAN_POINT('Ctrl Pts',(-52.5822684827187,3.94239838556798,-2.46333497443955));
#42472=CARTESIAN_POINT('Ctrl Pts',(-52.3837953309906,4.2075906767663,1.97654522392122));
#42473=CARTESIAN_POINT('Ctrl Pts',(-52.1853221792624,0.621067460305235,
4.60702942724974));
#42474=CARTESIAN_POINT('Ctrl Pts',(-51.9868490275344,-3.5339863170476,3.02017189553276));
#42475=CARTESIAN_POINT('Ctrl Pts',(-51.7883758758061,-4.4539682903228,-1.33141391106648));
#42476=CARTESIAN_POINT('Ctrl Pts',(-51.5899027240781,-1.29670574585495,
-4.46419499324869));
#42477=CARTESIAN_POINT('Ctrl Pts',(-51.3914295723499,3.0475838049597,-3.51037373970853));
#42478=CARTESIAN_POINT('Ctrl Pts',(-51.1929564206218,4.60206058888503,0.656908175550339));
#42479=CARTESIAN_POINT('Ctrl Pts',(-50.9944832688937,1.94372785161201,4.22284386453272));
#42480=CARTESIAN_POINT('Ctrl Pts',(-50.7960101171655,-2.49392831173375,
3.92311241991201));
#42481=CARTESIAN_POINT('Ctrl Pts',(-50.5975369654375,-4.64859756442089,
0.032092912022845));
#42482=CARTESIAN_POINT('Ctrl Pts',(-50.3990638137092,-2.54785670310451,
-3.88830493645013));
#42483=CARTESIAN_POINT('Ctrl Pts',(-50.2005906619813,1.8852381363435,-4.24927833946838));
#42484=CARTESIAN_POINT('Ctrl Pts',(-50.0021175102529,4.59255198071539,-0.720385659383156));
#42485=CARTESIAN_POINT('Ctrl Pts',(-49.803644358525,3.09576087736483,3.46796103779234));
#42486=CARTESIAN_POINT('Ctrl Pts',(-49.6051712067967,-1.23494558517625,
4.48167363791002));
#42487=CARTESIAN_POINT('Ctrl Pts',(-49.4066980550687,-4.43516057912403,
1.39278132691336));
#42488=CARTESIAN_POINT('Ctrl Pts',(-49.2082249033404,-3.57534955803026,
-2.97108813779842));
#42489=CARTESIAN_POINT('Ctrl Pts',(-49.0097517516124,0.557400955467083,
-4.61516991703562));
#42490=CARTESIAN_POINT('Ctrl Pts',(-48.8112785998842,4.1798965777469,-2.03444188569328));
#42491=CARTESIAN_POINT('Ctrl Pts',(-48.6128054481562,3.97603945794876,2.40865095344619));
#42492=CARTESIAN_POINT('Ctrl Pts',(-48.414332296428,0.132444081719959,4.64682125247059));
#42493=CARTESIAN_POINT('Ctrl Pts',(-48.2158591446998,-3.83239299652962,
2.63120753782877));
#42494=CARTESIAN_POINT('Ctrl Pts',(-48.0173859929717,-4.28898838077306,
-1.79306102979217));
#42495=CARTESIAN_POINT('Ctrl Pts',(-47.8189128412436,-0.819366418289231,
-4.57592917991651));
#42496=CARTESIAN_POINT('Ctrl Pts',(-47.6204396895155,3.40031834670907,-3.16990919870439));
#42497=CARTESIAN_POINT('Ctrl Pts',(-47.4219665377873,4.50729034775482,1.13790285527143));
#42498=CARTESIAN_POINT('Ctrl Pts',(-47.2234933860592,1.48820744283477,4.40405810521368));
#42499=CARTESIAN_POINT('Ctrl Pts',(-47.025020234331,-2.89320740585849,3.63865910655113));
#42500=CARTESIAN_POINT('Ctrl Pts',(-46.826547082603,-4.62612799527478,-0.457634087822847));
#42501=CARTESIAN_POINT('Ctrl Pts',(-46.6280739308748,-2.12420755208681,
-4.13500078145832));
#42502=CARTESIAN_POINT('Ctrl Pts',(-46.4296007791468,2.32225080975237,-4.02711315505378));
#42503=CARTESIAN_POINT('Ctrl Pts',(-46.2311276274185,4.64287888172855,-0.232733488355147));
#42504=CARTESIAN_POINT('Ctrl Pts',(-46.0326544756905,2.71333185741701,3.77469461261823));
#42505=CARTESIAN_POINT('Ctrl Pts',(-45.8341813239623,-1.7000481037694,4.32669916123979));
#42506=CARTESIAN_POINT('Ctrl Pts',(-45.6357081722342,-4.55717335808265,
0.917965234300663));
#42507=CARTESIAN_POINT('Ctrl Pts',(-45.437235020506,-3.24257989877357,-3.33109063027));
#42508=CARTESIAN_POINT('Ctrl Pts',(-45.238761868778,1.04032970329042,-4.5308060315417));
#42509=CARTESIAN_POINT('Ctrl Pts',(-45.0402887170497,4.37090272508006,-1.5829398456324));
#42510=CARTESIAN_POINT('Ctrl Pts',(-44.8418155653217,3.70027253143814,2.81397803475566));
#42511=CARTESIAN_POINT('Ctrl Pts',(-44.6433424135935,-0.357653898701961,
4.6349296516502));
#42512=CARTESIAN_POINT('Ctrl Pts',(-44.4448692618655,-4.0881774970914,2.21298304089265));
#42513=CARTESIAN_POINT('Ctrl Pts',(-44.2463961101372,-4.07630965474763,
-2.23476817267793));
#42514=CARTESIAN_POINT('Ctrl Pts',(-44.0479229584092,-0.332914408674636,
-4.63677228074658));
#42515=CARTESIAN_POINT('Ctrl Pts',(-43.8494498066809,3.71523669362209,-2.79419138524314));
#42516=CARTESIAN_POINT('Ctrl Pts',(-43.6509766549529,4.36239309537038,1.6062427177945));
#42517=CARTESIAN_POINT('Ctrl Pts',(-43.4525035032247,1.01613615025615,4.53629325674009));
#42518=CARTESIAN_POINT('Ctrl Pts',(-43.2540303514966,-3.26031016017885,
3.3137391035562));
#42519=CARTESIAN_POINT('Ctrl Pts',(-43.0555571997685,-4.55220972667487,
-0.942271612312327));
#42520=CARTESIAN_POINT('Ctrl Pts',(-42.8570840480404,-1.6769343772943,-4.33570989357585));
#42521=CARTESIAN_POINT('Ctrl Pts',(-42.6586108963122,2.73343695672062,-3.76016111232444));
#42522=CARTESIAN_POINT('Ctrl Pts',(-42.4601377445842,4.64157078321707,0.257506992892894));
#42523=CARTESIAN_POINT('Ctrl Pts',(-42.2616645928559,2.30072697040417,4.03944855081209));
#42524=CARTESIAN_POINT('Ctrl Pts',(-42.0631914411279,-2.14624382139399,
4.12360602460166));
#42525=CARTESIAN_POINT('Ctrl Pts',(-41.8647182893996,-4.62850429603346,
0.432940144364989));
#42526=CARTESIAN_POINT('Ctrl Pts',(-41.6662451376716,-2.87374842948024,
-3.65404695523508));
#42527=CARTESIAN_POINT('Ctrl Pts',(-41.4677719859434,1.5116885982894,-4.39605354480638));
#42528=CARTESIAN_POINT('Ctrl Pts',(-41.2692988342153,4.51329860893046,-1.11383340479144));
#42529=CARTESIAN_POINT('Ctrl Pts',(-41.0708256824872,3.38335364292205,3.1880099300236));
#42530=CARTESIAN_POINT('Ctrl Pts',(-40.8723525307591,-0.843774291109008,
4.57149145604215));
#42531=CARTESIAN_POINT('Ctrl Pts',(-40.6738793790309,-4.29849601547731,
1.77014722323563));
#42532=CARTESIAN_POINT('Ctrl Pts',(-40.4754062273028,-3.81829693276388,
-2.65162171514888));
#42533=CARTESIAN_POINT('Ctrl Pts',(-40.2769330755747,0.157240052846411,
-4.64604829428018));
#42534=CARTESIAN_POINT('Ctrl Pts',(-40.0784599238465,3.98883665711766,-2.38739843969065));
#42535=CARTESIAN_POINT('Ctrl Pts',(-39.8799867721184,4.16898021789935,2.05671902061676));
#42536=CARTESIAN_POINT('Ctrl Pts',(-39.6815136203903,0.532764069457865,
4.61807878162528));
#42537=CARTESIAN_POINT('Ctrl Pts',(-39.4830404686622,-3.59115392042467,
2.95196590543005));
#42538=CARTESIAN_POINT('Ctrl Pts',(-39.284567316934,-4.42766481907536,-1.41642982068484));
#42539=CARTESIAN_POINT('Ctrl Pts',(-39.0860941652059,-1.21101145733567,
-4.48820013337248));
#42540=CARTESIAN_POINT('Ctrl Pts',(-38.8876210134777,3.11422364181328,-3.45139106676922));
#42541=CARTESIAN_POINT('Ctrl Pts',(-38.6891478617497,4.58864223166364,0.744883653194257));
#42542=CARTESIAN_POINT('Ctrl Pts',(-38.4906747100215,1.86253493324648,4.25927843765109));
#42543=CARTESIAN_POINT('Ctrl Pts',(-38.2922015582934,-2.56857044737412,
3.87465289334144));
#42544=CARTESIAN_POINT('Ctrl Pts',(-38.0937284065652,-4.64836009769383,
-0.0568998169656816));
#42545=CARTESIAN_POINT('Ctrl Pts',(-37.8952552548371,-2.47295704773775,
-3.93636540822205));
#42546=CARTESIAN_POINT('Ctrl Pts',(-37.696782103109,1.9662355014118,-4.21241108392697));
#42547=CARTESIAN_POINT('Ctrl Pts',(-37.4983089513809,4.60550059726841,-0.63233965205675));
#42548=CARTESIAN_POINT('Ctrl Pts',(-37.2998357996527,3.02880735282022,3.52658690613249));
#42549=CARTESIAN_POINT('Ctrl Pts',(-37.1013626479246,-1.32051078888074,
4.45721218290677));
#42550=CARTESIAN_POINT('Ctrl Pts',(-36.9028894961964,-4.4610095294625,1.30762500933861));
#42551=CARTESIAN_POINT('Ctrl Pts',(-36.7044163444683,-3.51781966015203,
-3.03898569026757));
#42552=CARTESIAN_POINT('Ctrl Pts',(-36.5059431927402,0.64564579542217,-4.60365405888156));
#42553=CARTESIAN_POINT('Ctrl Pts',(-36.3074700410121,4.2180754409679,-1.95405444174575));
#42554=CARTESIAN_POINT('Ctrl Pts',(-36.1089968892839,3.92920272430553,2.48432186689104));
#42555=CARTESIAN_POINT('Ctrl Pts',(-35.9105237375558,0.0434669421797721,
4.64850511583461));
#42556=CARTESIAN_POINT('Ctrl Pts',(-35.7120505858277,-3.88205926305851,
2.55736291227986));
#42557=CARTESIAN_POINT('Ctrl Pts',(-35.5135774340995,-4.25387837783278,
-1.8748354417414));
#42558=CARTESIAN_POINT('Ctrl Pts',(-35.3151042823715,-0.731620476027489,
-4.59077560615418));
#42559=CARTESIAN_POINT('Ctrl Pts',(-35.1166311306433,3.46037600960852,-3.10423695279999));
#42560=CARTESIAN_POINT('Ctrl Pts',(-34.9181579789152,4.48468186310071,1.22397621454777));
#42561=CARTESIAN_POINT('Ctrl Pts',(-34.7196848271871,1.40362902538621,4.431739471821));
#42562=CARTESIAN_POINT('Ctrl Pts',(-34.5212116754589,-2.96233114678408,
3.58260845806457));
#42563=CARTESIAN_POINT('Ctrl Pts',(-34.3227385237308,-4.61651994008701,
-0.546106976499942));
#42564=CARTESIAN_POINT('Ctrl Pts',(-34.1242653720026,-2.04466308785533,
-4.17490623178112));
#42565=CARTESIAN_POINT('Ctrl Pts',(-33.9257922202745,2.39891524530935,-3.98192099781315));
#42566=CARTESIAN_POINT('Ctrl Pts',(-33.7273190685464,4.64648328110378,-0.143813439656987));
#42567=CARTESIAN_POINT('Ctrl Pts',(-33.5288459168183,2.64057668839093,3.82594353587835));
#42568=CARTESIAN_POINT('Ctrl Pts',(-33.3303727650901,-1.7825614468038,4.29336277006403));
#42569=CARTESIAN_POINT('Ctrl Pts',(-33.131899613362,-4.57391067218585,0.830560262634542));
#42570=CARTESIAN_POINT('Ctrl Pts',(-32.9334264616339,-3.17821954463672,
-3.39255209438148));
#42571=CARTESIAN_POINT('Ctrl Pts',(-32.7349533099057,1.12687109628521,-4.51006105494813));
#42572=CARTESIAN_POINT('Ctrl Pts',(-32.5364801581776,4.40040360438443,-1.49897875419349));
#42573=CARTESIAN_POINT('Ctrl Pts',(-32.3380070064495,3.64572725987484,2.88429574309024));
#42574=CARTESIAN_POINT('Ctrl Pts',(-32.1395338547213,-0.446313595424793,
4.62723387798174));
#42575=CARTESIAN_POINT('Ctrl Pts',(-31.9410607029933,-4.12979093297379,
2.13431863528631));
#42576=CARTESIAN_POINT('Ctrl Pts',(-31.7425875512651,-4.03278313978311,
-2.3123903940477));
#42577=CARTESIAN_POINT('Ctrl Pts',(-31.544114399537,-0.244092899977717,
-4.64229553595886));
#42578=CARTESIAN_POINT('Ctrl Pts',(-31.3456412478088,3.76804438445096,-2.72255958682465));
#42579=CARTESIAN_POINT('Ctrl Pts',(-31.1471680960807,4.33084585537712,1.68945652917313));
#42580=CARTESIAN_POINT('Ctrl Pts',(-30.9486949443526,0.92911289211364,4.55491365677892));
#42581=CARTESIAN_POINT('Ctrl Pts',(-30.7502217926244,-3.32314677587213,
3.25072064210593));
#42582=CARTESIAN_POINT('Ctrl Pts',(-30.5517486408963,-4.53333792819974,
-1.02924069864568));
#42583=CARTESIAN_POINT('Ctrl Pts',(-30.3532754891682,-1.59362974946449,
-4.36701653404526));
#42584=CARTESIAN_POINT('Ctrl Pts',(-30.15480233744,2.80491585458726,-3.70714664340217));
#42585=CARTESIAN_POINT('Ctrl Pts',(-29.956329185712,4.63579087837372,0.346312169855375));
#42586=CARTESIAN_POINT('Ctrl Pts',(-29.7578560339838,2.22297929202692,4.08275057457869));
#42587=CARTESIAN_POINT('Ctrl Pts',(-29.5593828822557,-2.22478764577608,
4.08176544135075));
#42588=CARTESIAN_POINT('Ctrl Pts',(-29.3609097305275,-4.63594383247414,
0.344258578902418));
#42589=CARTESIAN_POINT('Ctrl Pts',(-29.1624365787994,-2.80327339209578,
-3.70838879787041));
#42590=CARTESIAN_POINT('Ctrl Pts',(-28.9639634270712,1.59556408874945,-4.36631016141731));
#42591=CARTESIAN_POINT('Ctrl Pts',(-28.7654902753432,4.53379341519692,-1.0272324251697));
#42592=CARTESIAN_POINT('Ctrl Pts',(-28.567017123615,3.32170644956629,3.25219240665626));
#42593=CARTESIAN_POINT('Ctrl Pts',(-28.3685439718869,-0.931130531035452,
4.55450163258032));
#42594=CARTESIAN_POINT('Ctrl Pts',(-28.1700708201587,-4.33159382384316,
1.68753789061073));
#42595=CARTESIAN_POINT('Ctrl Pts',(-27.9715976684306,-3.76683797863228,
-2.72422848339423));
#42596=CARTESIAN_POINT('Ctrl Pts',(-27.7731245167025,0.24614931442832,-4.64218695250519));
#42597=CARTESIAN_POINT('Ctrl Pts',(-27.5746513649744,4.03380708397526,-2.31060372982344));
#42598=CARTESIAN_POINT('Ctrl Pts',(-27.3761782132462,4.12884506991978,2.13614783561486));
#42599=CARTESIAN_POINT('Ctrl Pts',(-27.1777050615181,0.44426378522975,4.62743113143094));
#42600=CARTESIAN_POINT('Ctrl Pts',(-26.9792319097899,-3.64700458397518,
2.88268048029381));
#42601=CARTESIAN_POINT('Ctrl Pts',(-26.7807587580619,-4.39973915686285,
-1.50092789252875));
#42602=CARTESIAN_POINT('Ctrl Pts',(-26.5822856063337,-1.12487312439103,
-4.51055979242331));
#42603=CARTESIAN_POINT('Ctrl Pts',(-26.3838124546056,3.1797220613837,-3.39114387771338));
#42604=CARTESIAN_POINT('Ctrl Pts',(-26.1853393028775,4.57354230284658,0.832586326500559));
#42605=CARTESIAN_POINT('Ctrl Pts',(-25.9868661511493,1.78065940331774,4.29415198571022));
#42606=CARTESIAN_POINT('Ctrl Pts',(-25.7883929994211,-2.64227124109951,
3.82477344106307));
#42607=CARTESIAN_POINT('Ctrl Pts',(-25.5899198476931,-4.64641911891196,
-0.145871719028707));
#42608=CARTESIAN_POINT('Ctrl Pts',(-25.3914466959649,-2.39715110344515,
-3.98298327566846));
#42609=CARTESIAN_POINT('Ctrl Pts',(-25.1929735442368,2.04651228210034,-4.17400007980539));
#42610=CARTESIAN_POINT('Ctrl Pts',(-24.9945003925087,4.61676140093734,-0.544061902560779));
#42611=CARTESIAN_POINT('Ctrl Pts',(-24.7960272407805,2.96074383662082,3.58392035638559));
#42612=CARTESIAN_POINT('Ctrl Pts',(-24.5975540890525,-1.40559205420105,
4.43111725913116));
#42613=CARTESIAN_POINT('Ctrl Pts',(-24.3990809373243,-4.48522361857249,
1.22198947556942));
#42614=CARTESIAN_POINT('Ctrl Pts',(-24.2006077855961,-3.45900055900394,
-3.10576952136075));
#42615=CARTESIAN_POINT('Ctrl Pts',(-24.002134633868,0.733654020408733,-4.59045106338594));
#42616=CARTESIAN_POINT('Ctrl Pts',(-23.8036614821399,4.25470847277443,-1.8729508799497));
#42617=CARTESIAN_POINT('Ctrl Pts',(-23.6051883304118,3.88092602467422,2.55908233122917));
#42618=CARTESIAN_POINT('Ctrl Pts',(-23.4067151786836,-0.0455261270268758,
4.64848540481315));
#42619=CARTESIAN_POINT('Ctrl Pts',(-23.2082420269555,-3.93030284065408,
2.48258106972349));
#42620=CARTESIAN_POINT('Ctrl Pts',(-23.0097688752274,-4.21720942246388,
-1.95592276792438));
#42621=CARTESIAN_POINT('Ctrl Pts',(-22.8112957234993,-0.643606411028971,
-4.60393961457854));
#42622=CARTESIAN_POINT('Ctrl Pts',(-22.6128225717711,3.51916552116573,-3.03742707264574));
#42623=CARTESIAN_POINT('Ctrl Pts',(-22.414349420043,4.46042984164243,1.30960101358717));
#42624=CARTESIAN_POINT('Ctrl Pts',(-22.2158762683148,1.31853620891633,4.45779670384143));
#42625=CARTESIAN_POINT('Ctrl Pts',(-22.0174031165868,-3.03036925880373,
3.52524486274362));
#42626=CARTESIAN_POINT('Ctrl Pts',(-21.8189299648586,-4.60522003235342,
-0.634379729037498));
#42627=CARTESIAN_POINT('Ctrl Pts',(-21.6204568131305,-1.96436929978352,
-4.21328167122386));
#42628=CARTESIAN_POINT('Ctrl Pts',(-21.4219836614024,2.47470053143833,-3.93526955451616));
#42629=CARTESIAN_POINT('Ctrl Pts',(-21.2235105096742,4.64838484703084,-0.0548406865110448));
#42630=CARTESIAN_POINT('Ctrl Pts',(-21.0250373579461,2.56685380635791,3.87579033537536));
#42631=CARTESIAN_POINT('Ctrl Pts',(-20.8265642062179,-1.86442152045769,
4.25845295630437));
#42632=CARTESIAN_POINT('Ctrl Pts',(-20.6280910544898,-4.58897174909836,
0.742850908985189));
#42633=CARTESIAN_POINT('Ctrl Pts',(-20.4296179027617,-3.11269444326658,
-3.45277026311631));
#42634=CARTESIAN_POINT('Ctrl Pts',(-20.2311447510336,1.21299951592391,-4.48766324063775));
#42635=CARTESIAN_POINT('Ctrl Pts',(-20.0326715993054,4.42829183300448,-1.41446832016443));
#42636=CARTESIAN_POINT('Ctrl Pts',(-19.8341984475773,3.5898459098312,2.9535564207699));
#42637=CARTESIAN_POINT('Ctrl Pts',(-19.6357252958492,-0.534809728077204,
4.617842325346));
#42638=CARTESIAN_POINT('Ctrl Pts',(-19.4372521441211,-4.16989089173616,
2.05487204906261));
#42639=CARTESIAN_POINT('Ctrl Pts',(-19.2387789923929,-3.98777869891112,
-2.38916517543554));
#42640=CARTESIAN_POINT('Ctrl Pts',(-19.0403058406648,-0.155181936626634,
-4.64611749243903));
#42641=CARTESIAN_POINT('Ctrl Pts',(-18.8418326889366,3.8194711702762,-2.64993003047852));
#42642=CARTESIAN_POINT('Ctrl Pts',(-18.6433595372085,4.29771145607754,1.77205119206607));
#42643=CARTESIAN_POINT('Ctrl Pts',(-18.4448863854804,0.841749134626984,
4.57186478161348));
#42644=CARTESIAN_POINT('Ctrl Pts',(-18.2464132337522,-3.38476553170436,
3.18651086337221));
#42645=CARTESIAN_POINT('Ctrl Pts',(-18.0479400820241,-4.51280476154808,
-1.11583259100634));
#42646=CARTESIAN_POINT('Ctrl Pts',(-17.849466930296,-1.50974109154628,-4.39672275945386));
#42647=CARTESIAN_POINT('Ctrl Pts',(-17.6509937785679,2.87536681277406,-3.65277358715271));
#42648=CARTESIAN_POINT('Ctrl Pts',(-17.4525206268397,4.62831205861156,0.434990431060229));
#42649=CARTESIAN_POINT('Ctrl Pts',(-17.2540474751116,2.1444169408607,4.12455636047718));
#42650=CARTESIAN_POINT('Ctrl Pts',(-17.0555743233835,-2.30251613464764,
4.03842898126119));
#42651=CARTESIAN_POINT('Ctrl Pts',(-16.8571011716554,-4.64168439794168,
0.255450850277838));
#42652=CARTESIAN_POINT('Ctrl Pts',(-16.6586280199272,-2.73177101695766,
-3.7613715979564));
#42653=CARTESIAN_POINT('Ctrl Pts',(-16.4601548681991,1.67885484022851,-4.33496662183739));
#42654=CARTESIAN_POINT('Ctrl Pts',(-16.261681716471,4.55262668636092,-0.94025498756312));
#42655=CARTESIAN_POINT('Ctrl Pts',(-16.0632085647428,3.25884192419725,3.31518302663628));
#42656=CARTESIAN_POINT('Ctrl Pts',(-15.8647354130147,-1.01814553219758,
4.53584268491193));
#42657=CARTESIAN_POINT('Ctrl Pts',(-15.6662622612865,-4.3631041987887,1.60431011263891));
#42658=CARTESIAN_POINT('Ctrl Pts',(-15.4677891095584,-3.71399856161824,
-2.79583688209824));
#42659=CARTESIAN_POINT('Ctrl Pts',(-15.2693159578303,0.33496836772571,-4.63662435179152));
#42660=CARTESIAN_POINT('Ctrl Pts',(-15.0708428061022,4.07729920967249,-2.23296223474716));
#42661=CARTESIAN_POINT('Ctrl Pts',(-14.872369654374,4.08719679145807,2.21479379963412));
#42662=CARTESIAN_POINT('Ctrl Pts',(-14.6738965026459,0.35560068814135,4.63508762998029));
#42663=CARTESIAN_POINT('Ctrl Pts',(-14.4754233509178,-3.70151870093434,
2.81233861646075));
#42664=CARTESIAN_POINT('Ctrl Pts',(-14.2769501991897,-4.37020108747133,
-1.58487590746636));
#42665=CARTESIAN_POINT('Ctrl Pts',(-14.0784770474615,-1.03832255030294,
-4.53126643098101));
#42666=CARTESIAN_POINT('Ctrl Pts',(-13.8800038957334,3.24405518308156,-3.32965390936127));
#42667=CARTESIAN_POINT('Ctrl Pts',(-13.6815307440053,4.55676627183815,0.919983875315956));
#42668=CARTESIAN_POINT('Ctrl Pts',(-13.4830575922771,1.69813130106531,4.32745182195541));
#42669=CARTESIAN_POINT('Ctrl Pts',(-13.284584440549,-2.71500370080188,3.77349229383538));
#42670=CARTESIAN_POINT('Ctrl Pts',(-13.0861112888209,-4.64277533019594,
-0.234790162330059));
#42671=CARTESIAN_POINT('Ctrl Pts',(-12.8876381370927,-2.32046665624351,
-4.02814146775719));
#42672=CARTESIAN_POINT('Ctrl Pts',(-12.6891649853646,2.12603906125972,-4.13405939688834));
#42673=CARTESIAN_POINT('Ctrl Pts',(-12.4906918336365,4.62633026357041,-0.455584766399773));
#42674=CARTESIAN_POINT('Ctrl Pts',(-12.2922186819084,2.89159527322953,3.63994037902266));
#42675=CARTESIAN_POINT('Ctrl Pts',(-12.0937455301802,-1.49015820109303,
4.40339842879546));
#42676=CARTESIAN_POINT('Ctrl Pts',(-11.8952723784521,-4.50779397233723,
1.13590610966014));
#42677=CARTESIAN_POINT('Ctrl Pts',(-11.696799226724,-3.39891381058531,-3.1714151565532));
#42678=CARTESIAN_POINT('Ctrl Pts',(-11.4983260749959,0.821393377408535,
-4.57556576901178));
#42679=CARTESIAN_POINT('Ctrl Pts',(-11.2998529232677,4.28978224794291,-1.79116092304315));
#42680=CARTESIAN_POINT('Ctrl Pts',(-11.1013797715396,3.83122705141254,2.6329049484415));
#42681=CARTESIAN_POINT('Ctrl Pts',(-10.9029066198114,-0.134502511913974,
4.64676212660943));
#42682=CARTESIAN_POINT('Ctrl Pts',(-10.7044334680833,-3.97710604910729,
2.40688941606321));
#42683=CARTESIAN_POINT('Ctrl Pts',(-10.5059603163552,-4.17899495303025,
-2.03629329163328));
#42684=CARTESIAN_POINT('Ctrl Pts',(-10.3074871646271,-0.55535647850289,
-4.61541638086834));
#42685=CARTESIAN_POINT('Ctrl Pts',(-10.1090140128989,3.57666533632311,-2.96950404258823));
#42686=CARTESIAN_POINT('Ctrl Pts',(-9.91054086117082,4.43454317121036,1.39474587279358));
#42687=CARTESIAN_POINT('Ctrl Pts',(-9.71206770944268,1.23296017806185,4.4822202518748));
#42688=CARTESIAN_POINT('Ctrl Pts',(-9.51359455771455,-3.09729680745274,
3.46658934307858));
#42689=CARTESIAN_POINT('Ctrl Pts',(-9.31512140598642,-4.59223241324053,
-0.722419995422388));
#42690=CARTESIAN_POINT('Ctrl Pts',(-9.11664825425829,-1.88335561377043,
-4.2501130360359));
#42691=CARTESIAN_POINT('Ctrl Pts',(-8.91817510253017,2.54957889450653,-3.88717592188593));
#42692=CARTESIAN_POINT('Ctrl Pts',(-8.71970195080204,4.64858288262784,0.0341521645346766));
#42693=CARTESIAN_POINT('Ctrl Pts',(-8.52122879907389,2.49219022912522,3.92421674335857));
#42694=CARTESIAN_POINT('Ctrl Pts',(-8.32275564734577,-1.94559832482275,
4.22198251363622));
#42695=CARTESIAN_POINT('Ctrl Pts',(-8.12428249561764,-4.60235106926837,
0.654869316892727));
#42696=CARTESIAN_POINT('Ctrl Pts',(-7.92580934388951,-3.04602860816486,
-3.51172306784635));
#42697=CARTESIAN_POINT('Ctrl Pts',(-7.72733619216139,1.29868339804392,-4.46362079691452));
#42698=CARTESIAN_POINT('Ctrl Pts',(-7.52886304043324,4.45455719052072,-1.32943951475187));
#42699=CARTESIAN_POINT('Ctrl Pts',(-7.33038988870513,3.53264896058713,3.02173468528678));
#42700=CARTESIAN_POINT('Ctrl Pts',(-7.131916736977,-0.623109864781879,4.60675843553939));
#42701=CARTESIAN_POINT('Ctrl Pts',(-6.93344358524887,-4.2084626776301,1.97467239764006));
#42702=CARTESIAN_POINT('Ctrl Pts',(-6.73497043352073,-3.94131282526402,
-2.46506438058074));
#42703=CARTESIAN_POINT('Ctrl Pts',(-6.5364972817926,-0.066214102526462,
-4.64823674952382));
#42704=CARTESIAN_POINT('Ctrl Pts',(-6.33802413006447,3.86949820432006,-2.57632933333366));
#42705=CARTESIAN_POINT('Ctrl Pts',(-6.13955097833635,4.26300204049134,1.85399643735695));
#42706=CARTESIAN_POINT('Ctrl Pts',(-5.94107782660821,0.754076894693181,
4.58714041902643));
#42707=CARTESIAN_POINT('Ctrl Pts',(-5.74260467488009,-3.44514384578296,
3.12113329882894));
#42708=CARTESIAN_POINT('Ctrl Pts',(-5.54413152315195,-4.49061775163378,
-1.20201555539611));
#42709=CARTESIAN_POINT('Ctrl Pts',(-5.34565837142384,-1.42529914695175,
-4.42481768309406));
#42710=CARTESIAN_POINT('Ctrl Pts',(-5.14718521969569,2.94476401270036,-3.59706187016166));
#42711=CARTESIAN_POINT('Ctrl Pts',(-4.94871206796758,4.61913706448716,0.523509278002365));
#42712=CARTESIAN_POINT('Ctrl Pts',(-4.75023891623944,2.06506870877937,4.16485058738426));
#42713=CARTESIAN_POINT('Ctrl Pts',(-4.55176576451131,-2.37940080320625,
3.9936125266212));
#42714=CARTESIAN_POINT('Ctrl Pts',(-4.35329261278318,-4.64572388678821,
0.1665495037332));
#42715=CARTESIAN_POINT('Ctrl Pts',(-4.15481946105504,-2.65926751165869,
-3.81297593688373));
#42716=CARTESIAN_POINT('Ctrl Pts',(-3.95634630932691,1.76153033530024,-4.30203441581027));
#42717=CARTESIAN_POINT('Ctrl Pts',(-3.75787315759879,4.56979150745246,-0.852932961487828));
#42718=CARTESIAN_POINT('Ctrl Pts',(-3.55940000587066,3.19478313012126,3.37695869421504));
#42719=CARTESIAN_POINT('Ctrl Pts',(-3.36092685414253,-1.10478745303856,
4.51552147231563));
#42720=CARTESIAN_POINT('Ctrl Pts',(-3.16245370241439,-4.39301550158241,
1.52049434994359));
#42721=CARTESIAN_POINT('Ctrl Pts',(-2.96398055068627,-3.6597982199938,-2.86642059087705));
#42722=CARTESIAN_POINT('Ctrl Pts',(-2.76550739895815,0.423664994886726,
-4.62936267890035));
#42723=CARTESIAN_POINT('Ctrl Pts',(-2.56703424723001,4.11929645967266,-2.15450212494862));
#42724=CARTESIAN_POINT('Ctrl Pts',(-2.36856109550188,4.04405186129635,2.29262754867159));
#42725=CARTESIAN_POINT('Ctrl Pts',(-2.17008794377375,0.266804946486184,
4.64104650786609));
#42726=CARTESIAN_POINT('Ctrl Pts',(-1.97161479204563,-3.75467184710545,
2.74096411037234));
#42727=CARTESIAN_POINT('Ctrl Pts',(-1.77314164031749,-4.33906993859569,
-1.66823930938942));
#42728=CARTESIAN_POINT('Ctrl Pts',(-1.57466848858935,-0.951375193182703,
-4.55031971059427));
#42729=CARTESIAN_POINT('Ctrl Pts',(-1.37619533686123,3.30716833257329,-3.26692983112172));
#42730=CARTESIAN_POINT('Ctrl Pts',(-1.17772218513309,4.5383797590448,1.00701775380853));
#42731=CARTESIAN_POINT('Ctrl Pts',(-0.979249033404966,1.6148671334332,4.35921645447386));
#42732=CARTESIAN_POINT('Ctrl Pts',(-0.780775881676836,-2.78652364898572,
3.72073125741831));
#42733=CARTESIAN_POINT('Ctrl Pts',(-0.582302729948716,-4.63784612289411,
-0.323437035503383));
#42734=CARTESIAN_POINT('Ctrl Pts',(-0.383829578220575,-2.24213561157208,
-4.07217861516247));
#42735=CARTESIAN_POINT('Ctrl Pts',(-0.185356426492449,2.20325939470542,
-4.0919210539669));
#42736=CARTESIAN_POINT('Ctrl Pts',(0.0131167252356776,4.63716582782614,
-0.368276129740102));
#42737=CARTESIAN_POINT('Ctrl Pts',(0.211589876963804,2.81535399355526,3.69744656037688));
#42738=CARTESIAN_POINT('Ctrl Pts',(0.343905311449231,-0.101190531491979,
4.14353111517988));
#42739=CARTESIAN_POINT('Ctrl Pts',(0.41006302869194,-1.3318200590755,3.70064107017205));
#42740=CARTESIAN_POINT('',(0.,3.89175630324288,-0.568086152066163));
#42741=CARTESIAN_POINT('Ctrl Pts',(1.36557432028894E-14,3.8984675804681,
-0.567744983796988));
#42742=CARTESIAN_POINT('Ctrl Pts',(1.22189337746952E-14,3.90378079301249,
-0.48168157494731));
#42743=CARTESIAN_POINT('Ctrl Pts',(1.81248313162765E-15,3.90605201893254,
-0.395549047494557));
#42744=CARTESIAN_POINT('Ctrl Pts',(2.1094237467878E-15,3.9051901940657,
-0.30946516814072));
#42745=CARTESIAN_POINT('Ctrl Pts',(2.53269562981551E-15,3.90397348654204,
-0.187933627678834));
#42746=CARTESIAN_POINT('Ctrl Pts',(-1.73372847453606E-15,3.89651412242738,
-0.0664981433266434));
#42747=CARTESIAN_POINT('Ctrl Pts',(-3.44169137633799E-15,3.88304410532436,
0.0544558887272117));
#42748=CARTESIAN_POINT('Ctrl Pts',(-4.42827767156581E-15,3.87526329564968,
0.124323676985952));
#42749=CARTESIAN_POINT('Ctrl Pts',(-5.99827845040638E-15,3.86547596069021,
0.194030594989938));
#42750=CARTESIAN_POINT('Ctrl Pts',(-8.54871728961371E-15,3.85371957233101,
0.263499450080404));
#42751=CARTESIAN_POINT('Ctrl Pts',(-1.02912501597371E-14,3.84568727105213,
0.310962561755177));
#42752=CARTESIAN_POINT('Ctrl Pts',(9.54271907070366E-15,3.83673570538044,
0.358314497435108));
#42753=CARTESIAN_POINT('Ctrl Pts',(1.0769163338864E-14,3.82687555339248,
0.405529836552379));
#42754=CARTESIAN_POINT('Ctrl Pts',(1.14030656965669E-14,3.82177921615585,
0.429933648093749));
#42755=CARTESIAN_POINT('Ctrl Pts',(3.36346654511152E-15,3.81643949818047,
0.454303276137411));
#42756=CARTESIAN_POINT('Ctrl Pts',(3.77475828372553E-15,3.81086326754485,
0.478612579049032));
#42757=CARTESIAN_POINT('Ctrl Pts',(5.8076671888918E-15,3.78330139879781,
0.598767188849739));
#42758=CARTESIAN_POINT('Ctrl Pts',(-8.81286749205166E-15,3.74994210044639,
0.717568668278516));
#42759=CARTESIAN_POINT('Ctrl Pts',(-6.66133814775094E-15,3.71102535385896,
0.834613822750009));
#42760=CARTESIAN_POINT('Ctrl Pts',(-4.77874997148781E-15,3.67697320059496,
0.937028332912565));
#42761=CARTESIAN_POINT('Ctrl Pts',(-1.19256951314485E-14,3.63866504086141,
1.03809826459941));
#42762=CARTESIAN_POINT('Ctrl Pts',(-1.80411241501588E-14,3.59623186452301,
1.13753521681003));
#42763=CARTESIAN_POINT('Ctrl Pts',(-2.07166243458445E-14,3.57766734987495,
1.18103888340217));
#42764=CARTESIAN_POINT('Ctrl Pts',(7.25282410556592E-15,3.55831295269719,
1.22422972408107));
#42765=CARTESIAN_POINT('Ctrl Pts',(6.38378239159465E-15,3.53817820767951,
1.26708221387324));
#42766=CARTESIAN_POINT('Ctrl Pts',(5.86343967720961E-15,3.52612243669922,
1.29274033879192));
#42767=CARTESIAN_POINT('Ctrl Pts',(-1.21504972407371E-14,3.5137868896413,
1.31827714523396));
#42768=CARTESIAN_POINT('Ctrl Pts',(-1.25455201782643E-14,3.50117347886088,
1.34368698778094));
#42769=CARTESIAN_POINT('Ctrl Pts',(-1.28529383185491E-14,3.49135736208285,
1.36346165349941));
#42770=CARTESIAN_POINT('Ctrl Pts',(-1.07293940314999E-15,3.48137159065754,
1.38316187499542));
#42771=CARTESIAN_POINT('Ctrl Pts',(-1.49880108324396E-15,3.47122829643433,
1.40276372527097));
#42772=CARTESIAN_POINT('Ctrl Pts',(-3.7927871000821E-15,3.41658948716747,
1.50835286967661));
#42773=CARTESIAN_POINT('Ctrl Pts',(-1.78861038778567E-14,3.3573208681292,
1.61121938665418));
#42774=CARTESIAN_POINT('Ctrl Pts',(-1.51545442861334E-14,3.29363279258605,
1.71100480040831));
#42775=CARTESIAN_POINT('Ctrl Pts',(-1.24429888430173E-14,3.23041112668357,
1.81005945132219));
#42776=CARTESIAN_POINT('Ctrl Pts',(-5.91093669341422E-15,3.16283391779207,
1.90607864354505));
#42777=CARTESIAN_POINT('Ctrl Pts',(7.21644966006352E-16,3.09106889768542,
1.99867770501885));
#42778=CARTESIAN_POINT('Ctrl Pts',(7.15828444958648E-15,3.02142398629525,
2.08854117083508));
#42779=CARTESIAN_POINT('Ctrl Pts',(-1.113421031979E-15,2.94783444879763,
2.17518402768862));
#42780=CARTESIAN_POINT('Ctrl Pts',(-2.692290834716E-15,2.87042640391083,
2.25821467895789));
#42781=CARTESIAN_POINT('Ctrl Pts',(-3.75588572577925E-15,2.81828100159452,
2.31414771177578));
#42782=CARTESIAN_POINT('Ctrl Pts',(1.06053239849839E-14,2.76440223430484,
2.36844071851178));
#42783=CARTESIAN_POINT('Ctrl Pts',(1.08246744900953E-14,2.70882332088636,
2.42096180237772));
#42784=CARTESIAN_POINT('Ctrl Pts',(1.09325239104711E-14,2.68149649255625,
2.44678516872728));
#42785=CARTESIAN_POINT('Ctrl Pts',(-3.0607682060388E-15,2.65375860355061,
2.47218002031012));
#42786=CARTESIAN_POINT('Ctrl Pts',(-4.05231403988182E-15,2.62561329981337,
2.49712970045525));
#42787=CARTESIAN_POINT('Ctrl Pts',(-4.49139428739187E-15,2.61314988510334,
2.50817801648817));
#42788=CARTESIAN_POINT('Ctrl Pts',(9.44721820786953E-15,2.60061273947681,
2.51913353665884));
#42789=CARTESIAN_POINT('Ctrl Pts',(9.07607322631065E-15,2.58800583701869,
2.5299921641494));
#42790=CARTESIAN_POINT('Ctrl Pts',(6.58226895225797E-15,2.50329730317145,
2.60295365626651));
#42791=CARTESIAN_POINT('Ctrl Pts',(-5.44922795401061E-15,2.41539203436312,
2.67158814314046));
#42792=CARTESIAN_POINT('Ctrl Pts',(-3.88578058618805E-15,2.3244377116327,
2.7355533676673));
#42793=CARTESIAN_POINT('Ctrl Pts',(-3.00127507940947E-15,2.27298116696346,
2.77174108623125));
#42794=CARTESIAN_POINT('Ctrl Pts',(1.68198853175566E-14,2.22054821616337,
2.80643359943742));
#42795=CARTESIAN_POINT('Ctrl Pts',(1.35724764760425E-14,2.16716210631343,
2.83956236070516));
#42796=CARTESIAN_POINT('Ctrl Pts',(7.66563464323506E-15,2.07094770881052,
2.89926822454041));
#42797=CARTESIAN_POINT('Ctrl Pts',(8.40867004919118E-15,1.97163780542389,
2.95389782223386));
#42798=CARTESIAN_POINT('Ctrl Pts',(9.63118473862323E-15,1.8696483294102,
3.00342377340144));
#42799=CARTESIAN_POINT('Ctrl Pts',(1.08588687776138E-14,1.76722759538598,
3.05315914287378));
#42800=CARTESIAN_POINT('Ctrl Pts',(-1.80644630904049E-15,1.66210361371026,
3.09774762574349));
#42801=CARTESIAN_POINT('Ctrl Pts',(-5.4678483962789E-15,1.55469419618438,
3.13710949192373));
#42802=CARTESIAN_POINT('Ctrl Pts',(-6.61135484369508E-15,1.52114875142644,
3.14940274644399));
#42803=CARTESIAN_POINT('Ctrl Pts',(9.392172699074E-15,1.4873804182791,3.16118581633617));
#42804=CARTESIAN_POINT('Ctrl Pts',(8.85402862138562E-15,1.45340208653369,
3.17245523646713));
#42805=CARTESIAN_POINT('Ctrl Pts',(8.61943655830772E-15,1.43858998086425,
3.17736789206964));
#42806=CARTESIAN_POINT('Ctrl Pts',(-3.17134925512025E-15,1.42373964752971,
3.182182318915));
#42807=CARTESIAN_POINT('Ctrl Pts',(-3.02535774210355E-15,1.40886346011089,
3.18689486353806));
#42808=CARTESIAN_POINT('Ctrl Pts',(-1.98365783949599E-15,1.30271672140575,
3.22052049816183));
#42809=CARTESIAN_POINT('Ctrl Pts',(3.26982359098091E-15,1.19509672053443,
3.24901613967402));
#42810=CARTESIAN_POINT('Ctrl Pts',(5.10702591327572E-15,1.0864059213934,
3.27238984682911));
#42811=CARTESIAN_POINT('Ctrl Pts',(6.94588490287831E-15,0.977617112092361,
3.29578463084439));
#42812=CARTESIAN_POINT('Ctrl Pts',(1.14510993419572E-14,0.867754622283836,
3.31404818378446));
#42813=CARTESIAN_POINT('Ctrl Pts',(8.67361737988404E-15,0.757218921225994,
3.32713646231221));
#42814=CARTESIAN_POINT('Ctrl Pts',(5.93036099161788E-15,0.648045298426994,
3.34006346028121));
#42815=CARTESIAN_POINT('Ctrl Pts',(2.18853355113062E-14,0.538214089575848,
3.34794178778571));
#42816=CARTESIAN_POINT('Ctrl Pts',(2.32869279415127E-14,0.428121599625193,
3.35067992093372));
#42817=CARTESIAN_POINT('Ctrl Pts',(2.41195983244399E-14,0.362716882969348,
3.35230661520498));
#42818=CARTESIAN_POINT('Ctrl Pts',(-8.15105557746918E-15,0.297220211304994,
3.35211819703499));
#42819=CARTESIAN_POINT('Ctrl Pts',(-8.50708392619026E-15,0.231718325657212,
3.35008743341715));
#42820=CARTESIAN_POINT('Ctrl Pts',(-8.62454349224495E-15,0.21010818396038,
3.34941745133801));
#42821=CARTESIAN_POINT('Ctrl Pts',(9.54989894362464E-15,0.188497502383238,
3.34854689142872));
#42822=CARTESIAN_POINT('Ctrl Pts',(1.00336405850499E-14,0.166889483364383,
3.34747463388988));
#42823=CARTESIAN_POINT('Ctrl Pts',(1.05189742785417E-14,0.145210349749661,
3.3463988474222));
#42824=CARTESIAN_POINT('Ctrl Pts',(-2.12730678030541E-16,0.123528723474772,
3.34511958286768));
#42825=CARTESIAN_POINT('Ctrl Pts',(3.05311331771918E-16,0.101878773581793,
3.34363804214106));
#42826=CARTESIAN_POINT('Ctrl Pts',(2.87320079637429E-15,-0.00543815668135161,
3.33629417281912));
#42827=CARTESIAN_POINT('Ctrl Pts',(-8.51767506189532E-15,-0.112104853391998,
3.32398025711894));
#42828=CARTESIAN_POINT('Ctrl Pts',(-4.6074255521944E-15,-0.217758135893045,
3.306659700895));
#42829=CARTESIAN_POINT('Ctrl Pts',(-7.51373278920776E-16,-0.321947032063546,
3.2895792127993));
#42830=CARTESIAN_POINT('Ctrl Pts',(1.11424313353336E-14,-0.425151170945409,
3.26762971614554));
#42831=CARTESIAN_POINT('Ctrl Pts',(8.67361737988404E-15,-0.527005212035941,
3.24072940055987));
#42832=CARTESIAN_POINT('Ctrl Pts',(6.28095158031733E-15,-0.625717664680271,
3.21465879894271));
#42833=CARTESIAN_POINT('Ctrl Pts',(4.47067010218622E-15,-0.723162567288633,
3.18393779064207));
#42834=CARTESIAN_POINT('Ctrl Pts',(5.68295410730002E-15,-0.818981858554579,
3.14845138915928));
#42835=CARTESIAN_POINT('Ctrl Pts',(6.85203894076324E-15,-0.911386674340049,
3.11422952894112));
#42836=CARTESIAN_POINT('Ctrl Pts',(8.30932818362312E-15,-1.00228004599708,
3.07557558113778));
#42837=CARTESIAN_POINT('Ctrl Pts',(8.88178419700125E-15,-1.09131022003164,
3.0323521507494));
#42838=CARTESIAN_POINT('Ctrl Pts',(-0.596163522034944,-3.93875600852084,
-0.00157175874070594));
#42839=CARTESIAN_POINT('Ctrl Pts',(-0.591543258006201,-3.93922783435017,
-0.0925476617549403));
#42840=CARTESIAN_POINT('Ctrl Pts',(-0.586922993977456,-3.93634370691034,
-0.183493527674194));
#42841=CARTESIAN_POINT('Ctrl Pts',(-0.582302729948712,-3.93000729202238,
-0.274199249959615));
#42842=CARTESIAN_POINT('Ctrl Pts',(-0.516145012706005,-3.83927595245344,
-1.57301756205636));
#42843=CARTESIAN_POINT('Ctrl Pts',(-0.449987295463298,-3.04070578201288,
-2.82259808860928));
#42844=CARTESIAN_POINT('Ctrl Pts',(-0.383829578220589,-1.9005215290797,
-3.45067875835325));
#42845=CARTESIAN_POINT('Ctrl Pts',(-0.317671860977876,-0.760337276146452,
-4.07875942809726));
#42846=CARTESIAN_POINT('Ctrl Pts',(-0.251514143735159,0.72146105927955,
-4.08534024103211));
#42847=CARTESIAN_POINT('Ctrl Pts',(-0.185356426492449,1.86801129917929,
-3.46802316012836));
#42848=CARTESIAN_POINT('Ctrl Pts',(-0.12357095099497,2.93878814436674,-2.89150342870496));
#42849=CARTESIAN_POINT('Ctrl Pts',(-0.0617854754974978,3.71716450840878,
-1.77082536565068));
#42850=CARTESIAN_POINT('Ctrl Pts',(-2.03309591384482E-14,3.898467580468,
-0.567744983797649));
#42851=CARTESIAN_POINT('',(-54.567,-1.8715865317393,-2.62360084935039));
#42852=CARTESIAN_POINT('Ctrl Pts',(-54.567,-1.87559511676541,-2.6273759996692));
#42853=CARTESIAN_POINT('Ctrl Pts',(-54.567,-1.93789333947134,-2.59269552998053));
#42854=CARTESIAN_POINT('Ctrl Pts',(-54.567,-1.99885539889533,-2.55586353911646));
#42855=CARTESIAN_POINT('Ctrl Pts',(-54.567,-2.05835614585776,-2.51690310931682));
#42856=CARTESIAN_POINT('Ctrl Pts',(-54.567,-2.14425612316253,-2.46065675601161));
#42857=CARTESIAN_POINT('Ctrl Pts',(-54.567,-2.22711174078161,-2.39997677567503));
#42858=CARTESIAN_POINT('Ctrl Pts',(-54.567,-2.30683028545471,-2.33525511370045));
#42859=CARTESIAN_POINT('Ctrl Pts',(-54.567,-2.35703865932115,-2.29449208403147));
#42860=CARTESIAN_POINT('Ctrl Pts',(-54.567,-2.40600232074533,-2.25212477113805));
#42861=CARTESIAN_POINT('Ctrl Pts',(-54.567,-2.45369396016998,-2.20824155898267));
#42862=CARTESIAN_POINT('Ctrl Pts',(-54.567,-2.48399487183792,-2.18036033386087));
#42863=CARTESIAN_POINT('Ctrl Pts',(-54.567,-2.51378223757325,-2.15186704269938));
#42864=CARTESIAN_POINT('Ctrl Pts',(-54.567,-2.54304824257815,-2.12278299439938));
#42865=CARTESIAN_POINT('Ctrl Pts',(-54.567,-2.55735314842029,-2.10856702702118));
#42866=CARTESIAN_POINT('Ctrl Pts',(-54.567,-2.57152812272356,-2.09421517294112));
#42867=CARTESIAN_POINT('Ctrl Pts',(-54.567,-2.58556785894575,-2.07973508475119));
#42868=CARTESIAN_POINT('Ctrl Pts',(-54.567,-2.65948482112199,-2.00349974000504));
#42869=CARTESIAN_POINT('Ctrl Pts',(-54.567,-2.72969587957797,-1.92367319141114));
#42870=CARTESIAN_POINT('Ctrl Pts',(-54.567,-2.79610010548891,-1.84066258236708));
#42871=CARTESIAN_POINT('Ctrl Pts',(-54.567,-2.85914867889807,-1.76184680812596));
#42872=CARTESIAN_POINT('Ctrl Pts',(-54.567,-2.91876562057248,-1.68015980669411));
#42873=CARTESIAN_POINT('Ctrl Pts',(-54.567,-2.9748433696887,-1.59591432401766));
#42874=CARTESIAN_POINT('Ctrl Pts',(-54.567,-2.99960770630907,-1.55871091402662));
#42875=CARTESIAN_POINT('Ctrl Pts',(-54.567,-3.02368153939547,-1.52100814673485));
#42876=CARTESIAN_POINT('Ctrl Pts',(-54.567,-3.04705405758258,-1.48283118015269));
#42877=CARTESIAN_POINT('Ctrl Pts',(-54.567,-3.05696360798717,-1.4666447952877));
#42878=CARTESIAN_POINT('Ctrl Pts',(-54.567,-3.06674707634774,-1.45037315554266));
#42879=CARTESIAN_POINT('Ctrl Pts',(-54.567,-3.07640358148389,-1.43401812748205));
#42880=CARTESIAN_POINT('Ctrl Pts',(-54.567,-3.08610983773139,-1.41757883696721));
#42881=CARTESIAN_POINT('Ctrl Pts',(-54.567,-3.09568363424083,-1.40106231376754));
#42882=CARTESIAN_POINT('Ctrl Pts',(-54.567,-3.10512111622586,-1.38447657626704));
#42883=CARTESIAN_POINT('Ctrl Pts',(-54.567,-3.16019365145779,-1.28769031333241));
#42884=CARTESIAN_POINT('Ctrl Pts',(-54.567,-3.21066290690797,-1.18848927937393));
#42885=CARTESIAN_POINT('Ctrl Pts',(-54.567,-3.25641980079756,-1.08730183953019));
#42886=CARTESIAN_POINT('Ctrl Pts',(-54.567,-3.30287797646003,-0.98456357529316));
#42887=CARTESIAN_POINT('Ctrl Pts',(-54.567,-3.34447882586322,-0.87977687522081));
#42888=CARTESIAN_POINT('Ctrl Pts',(-54.567,-3.38107398738024,-0.773348853617018));
#42889=CARTESIAN_POINT('Ctrl Pts',(-54.567,-3.41755338310152,-0.667257508341412));
#42890=CARTESIAN_POINT('Ctrl Pts',(-54.567,-3.44905921083244,-0.559534393146257));
#42891=CARTESIAN_POINT('Ctrl Pts',(-54.567,-3.47540277351408,-0.450553507956699));
#42892=CARTESIAN_POINT('Ctrl Pts',(-54.567,-3.49233717958551,-0.380497434443491));
#42893=CARTESIAN_POINT('Ctrl Pts',(-54.567,-3.50713752571676,-0.309921054712288));
#42894=CARTESIAN_POINT('Ctrl Pts',(-54.567,-3.51974304811656,-0.238919698740827));
#42895=CARTESIAN_POINT('Ctrl Pts',(-54.567,-3.52344450058597,-0.218071047169208));
#42896=CARTESIAN_POINT('Ctrl Pts',(-54.567,-3.52695665008924,-0.197185738634729));
#42897=CARTESIAN_POINT('Ctrl Pts',(-54.567,-3.53027780775631,-0.176266156451971));
#42898=CARTESIAN_POINT('Ctrl Pts',(-54.567,-3.53256308803807,-0.16187144428919));
#42899=CARTESIAN_POINT('Ctrl Pts',(-54.567,-3.53475742989087,-0.147463468338002));
#42900=CARTESIAN_POINT('Ctrl Pts',(-54.567,-3.53685927013624,-0.133051340231281));
#42901=CARTESIAN_POINT('Ctrl Pts',(-54.567,-3.55357701763763,-0.018419260473514));
#42902=CARTESIAN_POINT('Ctrl Pts',(-54.567,-3.56447071696453,0.0966256754745031));
#42903=CARTESIAN_POINT('Ctrl Pts',(-54.567,-3.56939469418434,0.211658829454915));
#42904=CARTESIAN_POINT('Ctrl Pts',(-54.567,-3.5721437137338,0.275880976514499));
#42905=CARTESIAN_POINT('Ctrl Pts',(-54.567,-3.57303128839785,0.340100030441642));
#42906=CARTESIAN_POINT('Ctrl Pts',(-54.567,-3.57202588112357,0.404245521614954));
#42907=CARTESIAN_POINT('Ctrl Pts',(-54.567,-3.57028656986049,0.515214457416961));
#42908=CARTESIAN_POINT('Ctrl Pts',(-54.567,-3.56288525045421,0.625962966574239));
#42909=CARTESIAN_POINT('Ctrl Pts',(-54.567,-3.55008625998367,0.73620625076776));
#42910=CARTESIAN_POINT('Ctrl Pts',(-54.567,-3.53704492605657,0.848536944793815));
#42911=CARTESIAN_POINT('Ctrl Pts',(-54.567,-3.51839948040439,0.960343777988608));
#42912=CARTESIAN_POINT('Ctrl Pts',(-54.567,-3.49437547908036,1.07132868702773));
#42913=CARTESIAN_POINT('Ctrl Pts',(-54.567,-3.48660681757375,1.10721797037555));
#42914=CARTESIAN_POINT('Ctrl Pts',(-54.567,-3.47827531871655,1.14302128727563));
#42915=CARTESIAN_POINT('Ctrl Pts',(-54.567,-3.46938746150371,1.17872844162552));
#42916=CARTESIAN_POINT('Ctrl Pts',(-54.567,-3.4641078129644,1.19993954130812));
#42917=CARTESIAN_POINT('Ctrl Pts',(-54.567,-3.45863056337528,1.22112107217551));
#42918=CARTESIAN_POINT('Ctrl Pts',(-54.567,-3.45296480785638,1.24224278150716));
#42919=CARTESIAN_POINT('Ctrl Pts',(-54.567,-3.42342725283962,1.35235760191379));
#42920=CARTESIAN_POINT('Ctrl Pts',(-54.567,-3.38873905323224,1.46098133704825));
#42921=CARTESIAN_POINT('Ctrl Pts',(-54.567,-3.34920122580605,1.56782019179735));
#42922=CARTESIAN_POINT('Ctrl Pts',(-54.567,-3.30839441336409,1.67808808943033));
#42923=CARTESIAN_POINT('Ctrl Pts',(-54.567,-3.26242164280839,1.78645539462761));
#42924=CARTESIAN_POINT('Ctrl Pts',(-54.567,-3.21155853814977,1.89260246649006));
#42925=CARTESIAN_POINT('Ctrl Pts',(-54.567,-3.16022236311832,1.99973679690069));
#42926=CARTESIAN_POINT('Ctrl Pts',(-54.567,-3.10390419869295,2.1046102041018));
#42927=CARTESIAN_POINT('Ctrl Pts',(-54.567,-3.04283453234895,2.20688591053918));
#42928=CARTESIAN_POINT('Ctrl Pts',(-54.567,-3.00304595452076,2.27352136393423));
#42929=CARTESIAN_POINT('Ctrl Pts',(-54.567,-2.96123934929021,2.33905393291921));
#42930=CARTESIAN_POINT('Ctrl Pts',(-54.567,-2.91746739595464,2.40338613119922));
#42931=CARTESIAN_POINT('Ctrl Pts',(-54.567,-2.902844530786,2.42487754270281));
#42932=CARTESIAN_POINT('Ctrl Pts',(-54.567,-2.88800225968487,2.44623495342649));
#42933=CARTESIAN_POINT('Ctrl Pts',(-54.567,-2.87294234438241,2.4674546085744));
#42934=CARTESIAN_POINT('Ctrl Pts',(-54.567,-2.86355986312814,2.48067467074929));
#42935=CARTESIAN_POINT('Ctrl Pts',(-54.567,-2.8540929031093,2.49384126294727));
#42936=CARTESIAN_POINT('Ctrl Pts',(-54.567,-2.84454187121597,2.50695346356968));
#42937=CARTESIAN_POINT('Ctrl Pts',(-54.567,-2.8345065952103,2.52073046209268));
#42938=CARTESIAN_POINT('Ctrl Pts',(-54.567,-2.82438385780302,2.53444004293616));
#42939=CARTESIAN_POINT('Ctrl Pts',(-54.567,-2.81417640991632,2.54807871818807));
#42940=CARTESIAN_POINT('Ctrl Pts',(-54.567,-2.74073890385789,2.64620219700058));
#42941=CARTESIAN_POINT('Ctrl Pts',(-54.567,-2.66288925851384,2.74069993823569));
#42942=CARTESIAN_POINT('Ctrl Pts',(-54.567,-2.58091654790888,2.83123710890433));
#42943=CARTESIAN_POINT('Ctrl Pts',(-54.567,-2.49880880908221,2.92192341546302));
#42944=CARTESIAN_POINT('Ctrl Pts',(-54.567,-2.41256402764738,3.00863692299536));
#42945=CARTESIAN_POINT('Ctrl Pts',(-54.567,-2.32242287699813,3.09102490393745));
#42946=CARTESIAN_POINT('Ctrl Pts',(-54.567,-2.2339914908075,3.17185017971528));
#42947=CARTESIAN_POINT('Ctrl Pts',(-54.567,-2.14180963977267,3.24851316729089));
#42948=CARTESIAN_POINT('Ctrl Pts',(-54.567,-2.04606345312307,3.32065397851649));
#42949=CARTESIAN_POINT('Ctrl Pts',(-54.567,-1.95044552606602,3.3926981514176));
#42950=CARTESIAN_POINT('Ctrl Pts',(-54.567,-1.85127243673682,3.46023303947618));
#42951=CARTESIAN_POINT('Ctrl Pts',(-54.567,-1.74869447533108,3.5228619944509));
#42952=CARTESIAN_POINT('Ctrl Pts',(-54.567,-1.87559511676549,-2.62737599966915));
#42953=CARTESIAN_POINT('Ctrl Pts',(-54.5052145245025,-1.06132064244425,
-3.20258678468392));
#42954=CARTESIAN_POINT('Ctrl Pts',(-54.3772713317624,1.2252681129847,-3.56578698204833));
#42955=CARTESIAN_POINT('Ctrl Pts',(-54.1831704217794,3.67986340215961,-0.983988949453548));
#42956=CARTESIAN_POINT('Ctrl Pts',(-53.9846972700513,2.8219875869866,2.55909768807962));
#42957=CARTESIAN_POINT('Ctrl Pts',(-53.7862241183231,-0.619631178725218,
3.75830321175399));
#42958=CARTESIAN_POINT('Ctrl Pts',(-53.6267338785483,-2.92926965772152,
1.95781535064456));
#42959=CARTESIAN_POINT('Ctrl Pts',(-53.5334013560163,-3.22000259141683,
0.443210257437656));
#42960=CARTESIAN_POINT('Ctrl Pts',(-53.5062265507269,-3.21814301605221,
0.00152842760642868));
#42961=CARTESIAN_POINT('Origin',(-54.567,-5.160062080289E-16,2.1385152528819E-16));
#42962=CARTESIAN_POINT('',(-54.567,-3.933,-4.81653586104654E-16));
#42963=CARTESIAN_POINT('Origin',(-54.567,0.,0.));
#42964=CARTESIAN_POINT('Origin',(-54.567,0.,0.));
#42965=CARTESIAN_POINT('',(-54.567,1.87158653173894,-2.62360084935064));
#42966=CARTESIAN_POINT('Ctrl Pts',(-54.567,1.75279620618125,3.52818484004951));
#42967=CARTESIAN_POINT('Ctrl Pts',(-54.567,1.82657430789191,3.48355378460627));
#42968=CARTESIAN_POINT('Ctrl Pts',(-54.567,1.89867731497302,3.43638255044532));
#42969=CARTESIAN_POINT('Ctrl Pts',(-54.567,1.96895656450102,3.38666332265823));
#42970=CARTESIAN_POINT('Ctrl Pts',(-54.567,2.06817543877299,3.31647068622802));
#42971=CARTESIAN_POINT('Ctrl Pts',(-54.567,2.16376116540805,3.24120063054011));
#42972=CARTESIAN_POINT('Ctrl Pts',(-54.567,2.25552899767464,3.16126330551513));
#42973=CARTESIAN_POINT('Ctrl Pts',(-54.567,2.30853769233681,3.11508837526235));
#42974=CARTESIAN_POINT('Ctrl Pts',(-54.567,2.36027174475663,3.06735546330207));
#42975=CARTESIAN_POINT('Ctrl Pts',(-54.567,2.41068902882149,3.01813932376916));
#42976=CARTESIAN_POINT('Ctrl Pts',(-54.567,2.44513556400026,2.98451344500101));
#42977=CARTESIAN_POINT('Ctrl Pts',(-54.567,2.47896732919389,2.95019513230726));
#42978=CARTESIAN_POINT('Ctrl Pts',(-54.567,2.51216950552106,2.91520763695931));
#42979=CARTESIAN_POINT('Ctrl Pts',(-54.567,2.5293304452325,2.89712393387901));
#42980=CARTESIAN_POINT('Ctrl Pts',(-54.567,2.54632471679035,2.87885960856721));
#42981=CARTESIAN_POINT('Ctrl Pts',(-54.567,2.56313473931103,2.86043519067462));
#42982=CARTESIAN_POINT('Ctrl Pts',(-54.567,2.64622234210827,2.76936804821556));
#42983=CARTESIAN_POINT('Ctrl Pts',(-54.567,2.72489683748954,2.67430520513737));
#42984=CARTESIAN_POINT('Ctrl Pts',(-54.567,2.79896338868084,2.57567350309106));
#42985=CARTESIAN_POINT('Ctrl Pts',(-54.567,2.86377162097323,2.48937076380055));
#42986=CARTESIAN_POINT('Ctrl Pts',(-54.567,2.92505136680962,2.40033466336044));
#42987=CARTESIAN_POINT('Ctrl Pts',(-54.567,2.98264010850768,2.30883708534923));
#42988=CARTESIAN_POINT('Ctrl Pts',(-54.567,3.00783518300059,2.26880689496932));
#42989=CARTESIAN_POINT('Ctrl Pts',(-54.567,3.03232337259389,2.22830544226294));
#42990=CARTESIAN_POINT('Ctrl Pts',(-54.567,3.05608912160428,2.187355097956));
#42991=CARTESIAN_POINT('Ctrl Pts',(-54.567,3.07031897932052,2.16283588029263));
#42992=CARTESIAN_POINT('Ctrl Pts',(-54.567,3.08428981350088,2.13815572847739));
#42993=CARTESIAN_POINT('Ctrl Pts',(-54.567,3.09799807180379,2.1133194287978));
#42994=CARTESIAN_POINT('Ctrl Pts',(-54.567,3.108666220358,2.09399112839202));
#42995=CARTESIAN_POINT('Ctrl Pts',(-54.567,3.1191765774848,2.07456573812209));
#42996=CARTESIAN_POINT('Ctrl Pts',(-54.567,3.12951637983522,2.05506685410723));
#42997=CARTESIAN_POINT('Ctrl Pts',(-54.567,3.18521374551435,1.95003230542785));
#42998=CARTESIAN_POINT('Ctrl Pts',(-54.567,3.23603690595946,1.84274166201074));
#42999=CARTESIAN_POINT('Ctrl Pts',(-54.567,3.2818109194263,1.7335719482421));
#43000=CARTESIAN_POINT('Ctrl Pts',(-54.567,3.3272497182131,1.62520171190402));
#43001=CARTESIAN_POINT('Ctrl Pts',(-54.567,3.36771328199207,1.51497896136699));
#43002=CARTESIAN_POINT('Ctrl Pts',(-54.567,3.40298086689944,1.4032605963081));
#43003=CARTESIAN_POINT('Ctrl Pts',(-54.567,3.43720657024157,1.29484263600781));
#43004=CARTESIAN_POINT('Ctrl Pts',(-54.567,3.46653877479758,1.18501538926984));
#43005=CARTESIAN_POINT('Ctrl Pts',(-54.567,3.49072735193707,1.0741054881589));
#43006=CARTESIAN_POINT('Ctrl Pts',(-54.567,3.50702181451284,0.999391823832429));
#43007=CARTESIAN_POINT('Ctrl Pts',(-54.567,3.5209811379261,0.924186878286872));
#43008=CARTESIAN_POINT('Ctrl Pts',(-54.567,3.53251580228219,0.848593054092502));
#43009=CARTESIAN_POINT('Ctrl Pts',(-54.567,3.53818712754629,0.811425334969612));
#43010=CARTESIAN_POINT('Ctrl Pts',(-54.567,3.54327213639131,0.774163649634371));
#43011=CARTESIAN_POINT('Ctrl Pts',(-54.567,3.54775921107122,0.736820478666499));
#43012=CARTESIAN_POINT('Ctrl Pts',(-54.567,3.54974618674968,0.720284098560792));
#43013=CARTESIAN_POINT('Ctrl Pts',(-54.567,3.55161489769857,0.703739936148487));
#43014=CARTESIAN_POINT('Ctrl Pts',(-54.567,3.55336423854053,0.687193590734354));
#43015=CARTESIAN_POINT('Ctrl Pts',(-54.567,3.56511848569491,0.576014666173494));
#43016=CARTESIAN_POINT('Ctrl Pts',(-54.567,3.57149546524957,0.464671209704678));
#43017=CARTESIAN_POINT('Ctrl Pts',(-54.567,3.57229788708192,0.353479489050023));
#43018=CARTESIAN_POINT('Ctrl Pts',(-54.567,3.57275184924506,0.290573880059895));
#43019=CARTESIAN_POINT('Ctrl Pts',(-54.567,3.57142069612182,0.227716836591344));
#43020=CARTESIAN_POINT('Ctrl Pts',(-54.567,3.56826131091937,0.164966495916737));
#43021=CARTESIAN_POINT('Ctrl Pts',(-54.567,3.56256734722735,0.051875454917302));
#43022=CARTESIAN_POINT('Ctrl Pts',(-54.567,3.55093778082866,-0.0608703175100407));
#43023=CARTESIAN_POINT('Ctrl Pts',(-54.567,3.53358690749236,-0.172913290391381));
#43024=CARTESIAN_POINT('Ctrl Pts',(-54.567,3.51616267006857,-0.28543001063441));
#43025=CARTESIAN_POINT('Ctrl Pts',(-54.567,3.49296810100612,-0.397238776827455));
#43026=CARTESIAN_POINT('Ctrl Pts',(-54.567,3.46417552856231,-0.507950709219032));
#43027=CARTESIAN_POINT('Ctrl Pts',(-54.567,3.45518320814962,-0.54252758391528));
#43028=CARTESIAN_POINT('Ctrl Pts',(-54.567,3.44564456424833,-0.576997229641806));
#43029=CARTESIAN_POINT('Ctrl Pts',(-54.567,3.4355640867651,-0.611347076759574));
#43030=CARTESIAN_POINT('Ctrl Pts',(-54.567,3.43116972567637,-0.626321132485534));
#43031=CARTESIAN_POINT('Ctrl Pts',(-54.567,3.42667284595602,-0.6412706901372));
#43032=CARTESIAN_POINT('Ctrl Pts',(-54.567,3.42207748879482,-0.656183497321861));
#43033=CARTESIAN_POINT('Ctrl Pts',(-54.567,3.38928802295434,-0.762591544534128));
#43034=CARTESIAN_POINT('Ctrl Pts',(-54.567,3.35144238687093,-0.867290076268274));
#43035=CARTESIAN_POINT('Ctrl Pts',(-54.567,3.30877634235103,-0.96995281167844));
#43036=CARTESIAN_POINT('Ctrl Pts',(-54.567,3.26607183263496,-1.07270810177234));
#43037=CARTESIAN_POINT('Ctrl Pts',(-54.567,3.21853763250597,-1.17342467286773));
#43038=CARTESIAN_POINT('Ctrl Pts',(-54.567,3.16636553468308,-1.2717482204815));
#43039=CARTESIAN_POINT('Ctrl Pts',(-54.567,3.11483633831456,-1.36886015586578));
#43040=CARTESIAN_POINT('Ctrl Pts',(-54.567,3.05878222358417,-1.4636383033807));
#43041=CARTESIAN_POINT('Ctrl Pts',(-54.567,2.99835357830501,-1.5557047498662));
#43042=CARTESIAN_POINT('Ctrl Pts',(-54.567,2.96245358513743,-1.61040041256928));
#43043=CARTESIAN_POINT('Ctrl Pts',(-54.567,2.92500902671214,-1.66413826114627));
#43044=CARTESIAN_POINT('Ctrl Pts',(-54.567,2.88604689933135,-1.71683148033191));
#43045=CARTESIAN_POINT('Ctrl Pts',(-54.567,2.87319267374389,-1.73421581152415));
#43046=CARTESIAN_POINT('Ctrl Pts',(-54.567,2.86017324527383,-1.75148639042203));
#43047=CARTESIAN_POINT('Ctrl Pts',(-54.567,2.84698951658492,-1.76863994674457));
#43048=CARTESIAN_POINT('Ctrl Pts',(-54.567,2.83376235824213,-1.78585001007142));
#43049=CARTESIAN_POINT('Ctrl Pts',(-54.567,2.820366499874,-1.80294627458048));
#43050=CARTESIAN_POINT('Ctrl Pts',(-54.567,2.80682238333785,-1.81990133392153));
#43051=CARTESIAN_POINT('Ctrl Pts',(-54.567,2.7396855052284,-1.90394592621961));
#43052=CARTESIAN_POINT('Ctrl Pts',(-54.567,2.66883293323538,-1.98462632727596));
#43053=CARTESIAN_POINT('Ctrl Pts',(-54.567,2.59444135432091,-2.06162312908462));
#43054=CARTESIAN_POINT('Ctrl Pts',(-54.567,2.52108087456256,-2.13755272223168));
#43055=CARTESIAN_POINT('Ctrl Pts',(-54.567,2.44427822116883,-2.20990063504143));
#43056=CARTESIAN_POINT('Ctrl Pts',(-54.567,2.36417413831495,-2.27831994080785));
#43057=CARTESIAN_POINT('Ctrl Pts',(-54.567,2.28654079774992,-2.34462891129411));
#43058=CARTESIAN_POINT('Ctrl Pts',(-54.567,2.2058060012744,-2.40724817445458));
#43059=CARTESIAN_POINT('Ctrl Pts',(-54.567,2.1220790745464,-2.46581789968667));
#43060=CARTESIAN_POINT('Ctrl Pts',(-54.567,2.04133558314445,-2.52230061427447));
#43061=CARTESIAN_POINT('Ctrl Pts',(-54.567,1.95780896462242,-2.57501739905895));
#43062=CARTESIAN_POINT('Ctrl Pts',(-54.567,1.87158653173864,-2.62360084935085));
#43063=CARTESIAN_POINT('Origin',(-54.567,0.,0.));
#43064=CARTESIAN_POINT('Origin',(-56.8777734492732,0.,0.));
#43065=CARTESIAN_POINT('Ctrl Pts',(-54.567,1.87158653173864,-2.62360084935085));
#43066=CARTESIAN_POINT('Ctrl Pts',(-54.5008422827573,2.74405176481089,-2.00121418560501));
#43067=CARTESIAN_POINT('Ctrl Pts',(-54.3685268482719,3.80418105204897,0.171604520928937));
#43068=CARTESIAN_POINT('Ctrl Pts',(-54.1700536965438,1.91525344717721,3.29560071974874));
#43069=CARTESIAN_POINT('Ctrl Pts',(-53.9715805448156,-1.72862424686986,
3.39318099076701));
#43070=CARTESIAN_POINT('Ctrl Pts',(-53.8324871290587,-3.17271035699792,
1.28805258441639));
#43071=CARTESIAN_POINT('Ctrl Pts',(-53.7595514305446,-3.22738947633959,
0.111495431728052));
#43072=CARTESIAN_POINT('Ctrl Pts',(-53.7527734492731,-3.22663436289375,
0.00208142861643813));
#43073=CARTESIAN_POINT('Ctrl Pts',(-54.9770630286919,2.2840585926085,-3.20180657528391));
#43074=CARTESIAN_POINT('Ctrl Pts',(-54.9109053114492,3.34880322426559,-2.44225440756606));
#43075=CARTESIAN_POINT('Ctrl Pts',(-54.7785898769639,4.64257049963806,0.209423809111752));
#43076=CARTESIAN_POINT('Ctrl Pts',(-54.5801167252356,2.33734909867248,4.02190602149484));
#43077=CARTESIAN_POINT('Ctrl Pts',(-54.3816435735076,-2.1095893764457,4.14099164896006));
#43078=CARTESIAN_POINT('Ctrl Pts',(-54.1831704217793,-4.62428608899499,
0.475171829894237));
#43079=CARTESIAN_POINT('Ctrl Pts',(-53.9846972700514,-2.90639616515588,
-3.6286483864793));
#43080=CARTESIAN_POINT('Ctrl Pts',(-53.7862241183231,1.47235844481099,-4.40916304885659));
#43081=CARTESIAN_POINT('Ctrl Pts',(-53.5877509665951,4.5031341736765,-1.15427358412515));
#43082=CARTESIAN_POINT('Ctrl Pts',(-53.3892778148669,3.41174088157173,3.15768914610369));
#43083=CARTESIAN_POINT('Ctrl Pts',(-53.1908046631387,-0.80286404893351,
4.57882123411569));
#43084=CARTESIAN_POINT('Ctrl Pts',(-52.9923315114107,-4.28249053334774,
1.80853540431148));
#43085=CARTESIAN_POINT('Ctrl Pts',(-52.7938583596825,-3.8418595301935,-2.61737787780216));
#43086=CARTESIAN_POINT('Ctrl Pts',(-52.5953852079544,0.115685074092492,
-4.64726406566888));
#43087=CARTESIAN_POINT('Ctrl Pts',(-52.3969120562262,3.96732629995167,-2.42297769608721));
#43088=CARTESIAN_POINT('Ctrl Pts',(-52.1984389044981,4.18720711106116,2.01935496417796));
#43089=CARTESIAN_POINT('Ctrl Pts',(-51.99996575277,0.574042118338133,4.61312905987137));
#43090=CARTESIAN_POINT('Ctrl Pts',(-51.8014926010419,-3.56461093282257,
2.98396398628069));
#43091=CARTESIAN_POINT('Ctrl Pts',(-51.6030194493137,-4.44015505970837,
-1.37677681431043));
#43092=CARTESIAN_POINT('Ctrl Pts',(-51.4045462975856,-1.25110101055297,
-4.47719062196251));
#43093=CARTESIAN_POINT('Ctrl Pts',(-51.2060731458575,3.08323341148789,-3.47910369919806));
#43094=CARTESIAN_POINT('Ctrl Pts',(-51.0075999941293,4.59512037410658,0.703817700242058));
#43095=CARTESIAN_POINT('Ctrl Pts',(-50.8091268424013,1.90055122225936,4.24245158453203));
#43096=CARTESIAN_POINT('Ctrl Pts',(-50.610653690673,-2.53381679938504,3.89746879408851));
#43097=CARTESIAN_POINT('Ctrl Pts',(-50.412180538945,-4.64868321197714,-0.0153272752145113));
#43098=CARTESIAN_POINT('Ctrl Pts',(-50.2137073872168,-2.50806113711531,
-3.91409246682743));
#43099=CARTESIAN_POINT('Ctrl Pts',(-50.0152342354887,1.92848535238818,-4.22982680231204));
#43100=CARTESIAN_POINT('Ctrl Pts',(-49.8167610837606,4.59966155680488,-0.673501363724546));
#43101=CARTESIAN_POINT('Ctrl Pts',(-49.6182879320324,3.06022458354438,3.49935937277421));
#43102=CARTESIAN_POINT('Ctrl Pts',(-49.4198147803042,-1.28059718662182,
4.46884340414282));
#43103=CARTESIAN_POINT('Ctrl Pts',(-49.2213416285762,-4.44913718740654,
1.34746755487186));
#43104=CARTESIAN_POINT('Ctrl Pts',(-49.022868476848,-3.54485673436904,-3.007404405193));
#43105=CARTESIAN_POINT('Ctrl Pts',(-48.8243953251199,0.604449530452811,
-4.60924411256357));
#43106=CARTESIAN_POINT('Ctrl Pts',(-48.6259221733918,4.20043178948642,-1.99169859811178));
#43107=CARTESIAN_POINT('Ctrl Pts',(-48.4274490216636,3.9512630032017,2.44908374772434));
#43108=CARTESIAN_POINT('Ctrl Pts',(-48.2289758699355,0.0850367741389765,
4.64793064394765));
#43109=CARTESIAN_POINT('Ctrl Pts',(-48.0305027182074,-3.85903365222682,
2.59197796959199));
#43110=CARTESIAN_POINT('Ctrl Pts',(-47.8320295664792,-4.27047504771653,
-1.83671810322143));
#43111=CARTESIAN_POINT('Ctrl Pts',(-47.6335564147511,-0.772646535574469,
-4.58404928583278));
#43112=CARTESIAN_POINT('Ctrl Pts',(-47.435083263023,3.43247655551004,-3.13505904565577));
#43113=CARTESIAN_POINT('Ctrl Pts',(-47.2366101112949,4.49544867810111,1.18382080841386));
#43114=CARTESIAN_POINT('Ctrl Pts',(-47.0381369595668,1.44320597277678,4.41900973567803));
#43115=CARTESIAN_POINT('Ctrl Pts',(-46.8396638078386,-2.93017351870171,
3.60895742205062));
#43116=CARTESIAN_POINT('Ctrl Pts',(-46.6411906561104,-4.62121930425517,
-0.504799629412044));
#43117=CARTESIAN_POINT('Ctrl Pts',(-46.4427175043824,-2.08191756152741,
-4.15645399239292));
#43118=CARTESIAN_POINT('Ctrl Pts',(-46.2442443526542,2.36320907948709,-4.00321537898037));
#43119=CARTESIAN_POINT('Ctrl Pts',(-46.0457712009261,4.64501149154437,-0.185361180660728));
#43120=CARTESIAN_POINT('Ctrl Pts',(-45.847298049198,2.67468657781142,3.8021759867674));
#43121=CARTESIAN_POINT('Ctrl Pts',(-45.6488248974699,-1.74409468659784,
4.30913265612192));
#43122=CARTESIAN_POINT('Ctrl Pts',(-45.4503517457417,-4.56630020751363,
0.871431545639821));
#43123=CARTESIAN_POINT('Ctrl Pts',(-45.2518785940136,-3.20843213216912,
-3.36399372430151));
#43124=CARTESIAN_POINT('Ctrl Pts',(-45.0534054422854,1.08649260427824,-4.5199584450218));
#43125=CARTESIAN_POINT('Ctrl Pts',(-44.8549322905574,4.38682240800469,-1.5382716549762));
#43126=CARTESIAN_POINT('Ctrl Pts',(-44.6564591388291,3.67137583132355,2.85157676190709));
#43127=CARTESIAN_POINT('Ctrl Pts',(-44.4579859871011,-0.404914421209559,
4.63104036209702));
#43128=CARTESIAN_POINT('Ctrl Pts',(-44.2595128353729,-4.11053870700268,
2.17116606046336));
#43129=CARTESIAN_POINT('Ctrl Pts',(-44.0610396836449,-4.0533016970634,-2.27623282562621));
#43130=CARTESIAN_POINT('Ctrl Pts',(-43.8625665319166,-0.285599182974214,
-4.63992711478959));
#43131=CARTESIAN_POINT('Ctrl Pts',(-43.6640933801886,3.74354597605967,-2.75614840837764));
#43132=CARTESIAN_POINT('Ctrl Pts',(-43.4656202284604,4.34578160663879,1.65065827816515));
#43133=CARTESIAN_POINT('Ctrl Pts',(-43.2671470767323,0.969810346848859,
4.54642259529622));
#43134=CARTESIAN_POINT('Ctrl Pts',(-43.0686739250041,-3.29394280200141,
3.28030964102757));
#43135=CARTESIAN_POINT('Ctrl Pts',(-42.8702007732761,-4.54236127977997,
-0.988657942784552));
#43136=CARTESIAN_POINT('Ctrl Pts',(-42.6717276215479,-1.63262028765758,
-4.35259020816388));
#43137=CARTESIAN_POINT('Ctrl Pts',(-42.4732544698198,2.77165077192005,-3.73208286649562));
#43138=CARTESIAN_POINT('Ctrl Pts',(-42.2747813180916,4.63870270808269,0.304840466312254));
#43139=CARTESIAN_POINT('Ctrl Pts',(-42.0763081663635,2.25940249266056,4.06270733625183));
#43140=CARTESIAN_POINT('Ctrl Pts',(-41.8778350146354,-2.18819552923403,
4.10149861022962));
#43141=CARTESIAN_POINT('Ctrl Pts',(-41.6793618629072,-4.63267988371023,
0.38570405616468));
#43142=CARTESIAN_POINT('Ctrl Pts',(-41.4808887111792,-2.83632548869743,
-3.68317094988007));
#43143=CARTESIAN_POINT('Ctrl Pts',(-41.2824155594509,1.55645243234538,-4.38040481573579));
#43144=CARTESIAN_POINT('Ctrl Pts',(-41.0839424077229,4.52442571492474,-1.06773708093468));
#43145=CARTESIAN_POINT('Ctrl Pts',(-40.8854692559947,3.3506580672695,3.22235644212695));
#43146=CARTESIAN_POINT('Ctrl Pts',(-40.6869961042666,-0.890362428554528,
4.56264673952452));
#43147=CARTESIAN_POINT('Ctrl Pts',(-40.4885229525385,-4.31632909314358,
1.72620789117576));
#43148=CARTESIAN_POINT('Ctrl Pts',(-40.2900498008103,-3.79105022960651,
-2.69043280541915));
#43149=CARTESIAN_POINT('Ctrl Pts',(-40.0915766490822,0.204624413165435,
-4.64420277048838));
#43150=CARTESIAN_POINT('Ctrl Pts',(-39.8931034973541,4.01298217624216,-2.34658572761319));
#43151=CARTESIAN_POINT('Ctrl Pts',(-39.6946303456259,4.14778365198342,2.09913822799128));
#43152=CARTESIAN_POINT('Ctrl Pts',(-39.4961571938978,0.485629137374503,
4.62327317652853));
#43153=CARTESIAN_POINT('Ctrl Pts',(-39.2976840421697,-3.62107905142639,
2.91518044504901));
#43154=CARTESIAN_POINT('Ctrl Pts',(-39.0992108904416,-4.41298614415993,
-1.46152106222511));
#43155=CARTESIAN_POINT('Ctrl Pts',(-38.9007377387134,-1.16516610035691,
-4.50031982001882));
#43156=CARTESIAN_POINT('Ctrl Pts',(-38.7022645869853,3.14926801392388,-3.41944461869924));
#43157=CARTESIAN_POINT('Ctrl Pts',(-38.5037914352572,4.58080536839695,0.791651881031651));
#43158=CARTESIAN_POINT('Ctrl Pts',(-38.305318283529,1.81899084063146,4.27805596568979));
#43159=CARTESIAN_POINT('Ctrl Pts',(-38.106845131801,-2.60796072132454,3.84825043362611));
#43160=CARTESIAN_POINT('Ctrl Pts',(-37.9083719800727,-4.64753798551651,
-0.104312976452023));
#43161=CARTESIAN_POINT('Ctrl Pts',(-37.7098988283447,-2.43267512575256,
-3.9613864058458));
#43162=CARTESIAN_POINT('Ctrl Pts',(-37.5114256766164,2.00910243504338,-4.19213524702842));
#43163=CARTESIAN_POINT('Ctrl Pts',(-37.3129525248885,4.61171137808434,-0.585327847554368));
#43164=CARTESIAN_POINT('Ctrl Pts',(-37.1144793731602,2.99267652000514,3.55729922419876));
#43165=CARTESIAN_POINT('Ctrl Pts',(-36.9160062214322,-1.36590841908661,
4.44351040445992));
#43166=CARTESIAN_POINT('Ctrl Pts',(-36.7175330697039,-4.47411614729356,
1.26205198957974));
#43167=CARTESIAN_POINT('Ctrl Pts',(-36.5190599179759,-3.48663723117299,
-3.07471158681162));
#43168=CARTESIAN_POINT('Ctrl Pts',(-36.3205867662477,0.692572313122873,
-4.59682870193908));
#43169=CARTESIAN_POINT('Ctrl Pts',(-36.1221136145196,4.23778866642741,-1.91092588620662));
#43170=CARTESIAN_POINT('Ctrl Pts',(-35.9236404627915,3.90365681526734,2.52427296315037));
#43171=CARTESIAN_POINT('Ctrl Pts',(-35.7251673110634,-0.00395291531700801,
4.64870679849092));
#43172=CARTESIAN_POINT('Ctrl Pts',(-35.5266941593352,-3.90794407590074,
2.51763055739075));
#43173=CARTESIAN_POINT('Ctrl Pts',(-35.3282210076071,-4.23453272132453,
-1.91813011964965));
#43174=CARTESIAN_POINT('Ctrl Pts',(-35.129747855879,-0.684753713175434,
-4.59799987779117));
#43175=CARTESIAN_POINT('Ctrl Pts',(-34.9312747041509,3.49186119850797,-3.06877758956716));
#43176=CARTESIAN_POINT('Ctrl Pts',(-34.7328015524227,4.4719633680656,1.26965907178053));
#43177=CARTESIAN_POINT('Ctrl Pts',(-34.5343284006946,1.35834958624193,4.44582691132163));
#43178=CARTESIAN_POINT('Ctrl Pts',(-34.3358552489664,-2.99872191450223,
3.55220458354517));
#43179=CARTESIAN_POINT('Ctrl Pts',(-34.1373820972383,-4.61070927103869,
-0.593169909750221));
#43180=CARTESIAN_POINT('Ctrl Pts',(-33.9389089455102,-2.00197017332486,
-4.19554596554403));
#43181=CARTESIAN_POINT('Ctrl Pts',(-33.7404357937821,2.43940854108479,-3.95724354741501));
#43182=CARTESIAN_POINT('Ctrl Pts',(-33.5419626420539,4.64770866458143,-0.0964089884288398));
#43183=CARTESIAN_POINT('Ctrl Pts',(-33.3434894903258,2.60141242142668,3.85268009799961));
#43184=CARTESIAN_POINT('Ctrl Pts',(-33.1450163385977,-1.82626368761961,
4.27495631172498));
#43185=CARTESIAN_POINT('Ctrl Pts',(-32.9465431868696,-4.58214506712391,
0.783860387892622));
#43186=CARTESIAN_POINT('Ctrl Pts',(-32.7480700351414,-3.14344818000384,
-3.42479547761697));
#43187=CARTESIAN_POINT('Ctrl Pts',(-32.5495968834133,1.17281788595065,-4.4983317719205));
#43188=CARTESIAN_POINT('Ctrl Pts',(-32.3511237316851,4.41546529883954,-1.45401400220878));
#43189=CARTESIAN_POINT('Ctrl Pts',(-32.1526505799571,3.61611611226858,2.92133441880021));
#43190=CARTESIAN_POINT('Ctrl Pts',(-31.9541774282288,-0.49349100632212,
4.62244060541122));
#43191=CARTESIAN_POINT('Ctrl Pts',(-31.7557042765008,-4.15134755404042,
2.09208126262768));
#43192=CARTESIAN_POINT('Ctrl Pts',(-31.5572311247726,-4.00898565116478,
-2.35340701380574));
#43193=CARTESIAN_POINT('Ctrl Pts',(-31.3587579730445,-0.196725952115783,
-4.64454404905792));
#43194=CARTESIAN_POINT('Ctrl Pts',(-31.1602848213164,3.79562023287763,-2.68398166380569));
#43195=CARTESIAN_POINT('Ctrl Pts',(-30.9618116695882,4.31338717518866,1.7335459615462));
#43196=CARTESIAN_POINT('Ctrl Pts',(-30.7633385178601,0.88260167414833,4.56415433663957));
#43197=CARTESIAN_POINT('Ctrl Pts',(-30.564865366132,-3.3561333235221,3.2166534843871));
#43198=CARTESIAN_POINT('Ctrl Pts',(-30.3663922144039,-4.52260332466425,
-1.07543000312019));
#43199=CARTESIAN_POINT('Ctrl Pts',(-30.1679190626757,-1.54900064449623,
-4.38304546260082));
#43200=CARTESIAN_POINT('Ctrl Pts',(-29.9694459109476,2.8425851730912,-3.6783420256411));
#43201=CARTESIAN_POINT('Ctrl Pts',(-29.7709727592195,4.63201723661572,0.3935820671347));
#43202=CARTESIAN_POINT('Ctrl Pts',(-29.5724996074913,2.18121714975723,4.10521403455169));
#43203=CARTESIAN_POINT('Ctrl Pts',(-29.3740264557632,-2.26630847004096,
4.05885900746697));
#43204=CARTESIAN_POINT('Ctrl Pts',(-29.175553304035,-4.63921442707336,0.296951214022621));
#43205=CARTESIAN_POINT('Ctrl Pts',(-28.977080152307,-2.76529979572438,-3.73679107840429));
#43206=CARTESIAN_POINT('Ctrl Pts',(-28.7786070005788,1.64002016084422,-4.34980739756368));
#43207=CARTESIAN_POINT('Ctrl Pts',(-28.5801338488507,4.54403607253222,-0.980931544707037));
#43208=CARTESIAN_POINT('Ctrl Pts',(-28.3816606971225,3.2883593788168,3.2859067423807));
#43209=CARTESIAN_POINT('Ctrl Pts',(-28.1831875453944,-0.977540819649672,
4.54476671236201));
#43210=CARTESIAN_POINT('Ctrl Pts',(-27.9847143936663,-4.34858251477885,
1.6432652360574));
#43211=CARTESIAN_POINT('Ctrl Pts',(-27.7862412419382,-3.7388533176929,-2.76251088552642));
#43212=CARTESIAN_POINT('Ctrl Pts',(-27.58776809021,0.29348966371279,-4.63943470060404));
#43213=CARTESIAN_POINT('Ctrl Pts',(-27.3892949384819,4.05716691174368,-2.26933628493606));
#43214=CARTESIAN_POINT('Ctrl Pts',(-27.1908217867538,4.10684036836924,2.17815350988125));
#43215=CARTESIAN_POINT('Ctrl Pts',(-26.9923486350256,0.397038055173797,
4.63172228297628));
#43216=CARTESIAN_POINT('Ctrl Pts',(-26.7938754832975,-3.67622005718519,
2.84532891157148));
#43217=CARTESIAN_POINT('Ctrl Pts',(-26.5954023315694,-4.38420000193776,
-1.54572988160424));
#43218=CARTESIAN_POINT('Ctrl Pts',(-26.3969291798412,-1.07880416411046,
-4.52179965272383));
#43219=CARTESIAN_POINT('Ctrl Pts',(-26.1984560281132,3.21414846959147,-3.35853243832749));
#43220=CARTESIAN_POINT('Ctrl Pts',(-25.9999828763849,4.56481160377853,0.879195965575385));
#43221=CARTESIAN_POINT('Ctrl Pts',(-25.8015097246569,1.73676383642218,4.31209251992246));
#43222=CARTESIAN_POINT('Ctrl Pts',(-25.6030365729287,-2.68114888191185,
3.79762178170733));
#43223=CARTESIAN_POINT('Ctrl Pts',(-25.4045634212006,-4.64468953980158,
-0.193260453101312));
#43224=CARTESIAN_POINT('Ctrl Pts',(-25.2060902694725,-2.35639759233519,
-4.00722858228877));
#43225=CARTESIAN_POINT('Ctrl Pts',(-25.0076171177443,2.08898322585505,-4.15290736785344));
#43226=CARTESIAN_POINT('Ctrl Pts',(-24.8091439660162,4.6220711091526,-0.496939821117236));
#43227=CARTESIAN_POINT('Ctrl Pts',(-24.6106708142881,2.92403170659736,3.61393540377918));
#43228=CARTESIAN_POINT('Ctrl Pts',(-24.41219766256,-1.45071907627053,4.41654895655195));
#43229=CARTESIAN_POINT('Ctrl Pts',(-24.2137245108318,-4.49745544249288,
1.17617391004329));
#43230=CARTESIAN_POINT('Ctrl Pts',(-24.0152513591037,-3.4271399524689,-3.14089195453562));
#43231=CARTESIAN_POINT('Ctrl Pts',(-23.8167782073755,0.780441283340165,
-4.58272865519371));
#43232=CARTESIAN_POINT('Ctrl Pts',(-23.6183050556475,4.27359248746764,-1.82945286217911));
#43233=CARTESIAN_POINT('Ctrl Pts',(-23.4198319039193,3.85462002336901,2.59853708830907));
#43234=CARTESIAN_POINT('Ctrl Pts',(-23.2213587521912,-0.092941156116394,
4.64777930471908));
#43235=CARTESIAN_POINT('Ctrl Pts',(-23.022885600463,-3.95542232442586,2.44236048922118));
#43236=CARTESIAN_POINT('Ctrl Pts',(-22.8244124487349,-4.19703853226137,
-1.99883918377353));
#43237=CARTESIAN_POINT('Ctrl Pts',(-22.6259392970068,-0.596609943671765,
-4.61026540439779));
#43238=CARTESIAN_POINT('Ctrl Pts',(-22.4274661452787,3.54996615153713,-3.0013714943032));
#43239=CARTESIAN_POINT('Ctrl Pts',(-22.2289929935505,4.44683918227362,1.35503203315327));
#43240=CARTESIAN_POINT('Ctrl Pts',(-22.0305198418224,1.27299539459941,4.47101478964274));
#43241=CARTESIAN_POINT('Ctrl Pts',(-21.8320466900943,-3.06617134498456,
3.4941499405536));
#43242=CARTESIAN_POINT('Ctrl Pts',(-21.6335735383661,-4.59850951475821,
-0.681322806423914));
#43243=CARTESIAN_POINT('Ctrl Pts',(-21.435100386638,-1.92128910729172,-4.2331003638087));
#43244=CARTESIAN_POINT('Ctrl Pts',(-21.2366272349099,2.51471401335639,-3.90982147353356));
#43245=CARTESIAN_POINT('Ctrl Pts',(-21.0381540831818,4.64870255509436,-0.00742146443297473));
#43246=CARTESIAN_POINT('Ctrl Pts',(-20.8396809314536,2.5271849048734,3.90177228710943));
#43247=CARTESIAN_POINT('Ctrl Pts',(-20.6412077797255,-1.90776340335524,
4.23921329030442));
#43248=CARTESIAN_POINT('Ctrl Pts',(-20.4427346279974,-4.59631067181976,
0.696001962634392));
#43249=CARTESIAN_POINT('Ctrl Pts',(-20.2442614762692,-3.07731222354206,
-3.48434211906835));
#43250=CARTESIAN_POINT('Ctrl Pts',(-20.0457883245411,1.25871335578393,-4.47505655962543));
#43251=CARTESIAN_POINT('Ctrl Pts',(-19.847315172813,4.4424900192119,-1.36922348543914));
#43252=CARTESIAN_POINT('Ctrl Pts',(-19.6488420210848,3.55953116656451,2.99002147118228));
#43253=CARTESIAN_POINT('Ctrl Pts',(-19.4503688693567,-0.581886737885667,
4.61214682638659));
#43254=CARTESIAN_POINT('Ctrl Pts',(-19.2518957176286,-4.19063502393284,
2.01222976323844));
#43255=CARTESIAN_POINT('Ctrl Pts',(-19.0534225659004,-3.96320040061246,
-2.42971873031846));
#43256=CARTESIAN_POINT('Ctrl Pts',(-18.8549494141723,-0.107780625542997,
-4.64745886056377));
#43257=CARTESIAN_POINT('Ctrl Pts',(-18.6564762624442,3.84630347875288,-2.61083129926249));
#43258=CARTESIAN_POINT('Ctrl Pts',(-18.4580031107161,4.27941198265269,1.81579833863889));
#43259=CARTESIAN_POINT('Ctrl Pts',(-18.2595299589879,0.79506954743727,4.58021341627364));
#43260=CARTESIAN_POINT('Ctrl Pts',(-18.0610568072598,-3.417093896341,3.15181849532368));
#43261=CARTESIAN_POINT('Ctrl Pts',(-17.8625836555317,-4.50118793536699,
-1.16180794212383));
#43262=CARTESIAN_POINT('Ctrl Pts',(-17.6641105038036,-1.46481332682715,
-4.41189442772884));
#43263=CARTESIAN_POINT('Ctrl Pts',(-17.4656373520754,2.91247782960961,-3.62325315371527));
#43264=CARTESIAN_POINT('Ctrl Pts',(-17.2671642003473,4.62363423318624,0.482179428826549));
#43265=CARTESIAN_POINT('Ctrl Pts',(-17.0686910486191,2.1022324389674,4.14621626262165));
#43266=CARTESIAN_POINT('Ctrl Pts',(-16.870217896891,-2.34359085887269,4.01473192256763));
#43267=CARTESIAN_POINT('Ctrl Pts',(-16.6717447451629,-4.64404880086273,
0.208089545822435));
#43268=CARTESIAN_POINT('Ctrl Pts',(-16.4732715934348,-2.69326068148164,
-3.78904175557095));
#43269=CARTESIAN_POINT('Ctrl Pts',(-16.2747984417066,1.72298685819398,-4.317615871099));
#43270=CARTESIAN_POINT('Ctrl Pts',(-16.0763252899785,4.56198114132962,-0.893766518744185));
#43271=CARTESIAN_POINT('Ctrl Pts',(-15.8778521382504,3.22485557931545,3.34825283042266));
#43272=CARTESIAN_POINT('Ctrl Pts',(-15.6793789865222,-1.06436096363523,
4.52522112862619));
#43273=CARTESIAN_POINT('Ctrl Pts',(-15.4809058347941,-4.37924227701401,
1.55972036054167));
#43274=CARTESIAN_POINT('Ctrl Pts',(-15.282432683066,-3.68528619865666,-2.83357656643789));
#43275=CARTESIAN_POINT('Ctrl Pts',(-15.0839595313379,0.382247356783641,
-4.63296638042055));
#43276=CARTESIAN_POINT('Ctrl Pts',(-14.8854863796097,4.09986478522412,-2.19125518065658));
#43277=CARTESIAN_POINT('Ctrl Pts',(-14.6870132278816,4.06439201850983,2.25637054664095));
#43278=CARTESIAN_POINT('Ctrl Pts',(-14.4885400761535,0.308301467299323,
4.63847396555551));
#43279=CARTESIAN_POINT('Ctrl Pts',(-14.2900669244253,-3.73001380952726,
2.77443462792171));
#43280=CARTESIAN_POINT('Ctrl Pts',(-14.0915937726972,-4.3538071472935,-1.62937222513801));
#43281=CARTESIAN_POINT('Ctrl Pts',(-13.8931206209691,-0.992046869976568,
-4.54162234577525));
#43282=CARTESIAN_POINT('Ctrl Pts',(-13.6946474692409,3.2778510108686,-3.29638943003145));
#43283=CARTESIAN_POINT('Ctrl Pts',(-13.4961743175128,4.54714493657699,0.966417844225444));
#43284=CARTESIAN_POINT('Ctrl Pts',(-13.2977011657847,1.65390034664457,4.34454878753181));
#43285=CARTESIAN_POINT('Ctrl Pts',(-13.0992280140565,-2.75335446067982,
3.74560138532248));
#43286=CARTESIAN_POINT('Ctrl Pts',(-12.9007548623284,-4.64013891800504,
-0.282137104064989));
#43287=CARTESIAN_POINT('Ctrl Pts',(-12.7022817106003,-2.27925649127012,
-4.05160219800491));
#43288=CARTESIAN_POINT('Ctrl Pts',(-12.5038085588722,2.16809845047511,-4.11215753989588));
#43289=CARTESIAN_POINT('Ctrl Pts',(-12.305335407144,4.63073695329427,-0.408369677216674));
#43290=CARTESIAN_POINT('Ctrl Pts',(-12.1068622554159,2.85431530018207,3.66924715589203));
#43291=CARTESIAN_POINT('Ctrl Pts',(-11.9083891036878,-1.53499807696976,
4.38796894104485));
#43292=CARTESIAN_POINT('Ctrl Pts',(-11.7099159519597,-4.51914651965373,
1.08986478875911));
#43293=CARTESIAN_POINT('Ctrl Pts',(-11.5114428002315,-3.36638670270264,
-3.20592125476317));
#43294=CARTESIAN_POINT('Ctrl Pts',(-11.3129696485034,0.868024239072622,
-4.56694913966179));
#43295=CARTESIAN_POINT('Ctrl Pts',(-11.1144964967753,4.30783013129569,-1.74730938410351));
#43296=CARTESIAN_POINT('Ctrl Pts',(-10.9160233450471,3.80417059840855,2.67184890704529));
#43297=CARTESIAN_POINT('Ctrl Pts',(-10.717550193319,-0.181895336035743,
4.64514850253505));
#43298=CARTESIAN_POINT('Ctrl Pts',(-10.5190770415909,-4.00145099807289,
2.36619534990175));
#43299=CARTESIAN_POINT('Ctrl Pts',(-10.3206038898628,-4.15800622131905,
-2.07881571750535));
#43300=CARTESIAN_POINT('Ctrl Pts',(-10.1221307381346,-0.508247529807154,
-4.62084137060774));
#43301=CARTESIAN_POINT('Ctrl Pts',(-9.92365758640649,3.60677012041613,-2.93286546270854));
#43302=CARTESIAN_POINT('Ctrl Pts',(-9.72518443467835,4.4200853281841,1.43990840522821));
#43303=CARTESIAN_POINT('Ctrl Pts',(-9.52671128295023,1.18717467827454,4.49456413984039));
#43304=CARTESIAN_POINT('Ctrl Pts',(-9.32823813122209,-3.13249709142274,
3.43481476881992));
#43305=CARTESIAN_POINT('Ctrl Pts',(-9.12976497949398,-4.58462450635486,
-0.769226013344334));
#43306=CARTESIAN_POINT('Ctrl Pts',(-8.93129182776583,-1.83990393125596,
-4.26910342432976));
#43307=CARTESIAN_POINT('Ctrl Pts',(-8.73281867603771,2.58909789851022,-3.86096653647828));
#43308=CARTESIAN_POINT('Ctrl Pts',(-8.53434552430957,4.64799279884426,0.0815687793655434));
#43309=CARTESIAN_POINT('Ctrl Pts',(-8.33587237258145,2.45203123089627,3.94943456289434));
#43310=CARTESIAN_POINT('Ctrl Pts',(-8.13739922085332,-1.98856396595975,
4.20191669088779));
#43311=CARTESIAN_POINT('Ctrl Pts',(-7.93892606912519,-4.60879183022014,
0.607888468036587));
#43312=CARTESIAN_POINT('Ctrl Pts',(-7.74045291739705,-3.01004850015028,
-3.54261182612741));
#43313=CARTESIAN_POINT('Ctrl Pts',(-7.54197976566894,1.34414753498608,-4.45014133798747));
#43314=CARTESIAN_POINT('Ctrl Pts',(-7.34350661394079,4.46788666515927,-1.28393117851835));
#43315=CARTESIAN_POINT('Ctrl Pts',(-7.14503346221267,3.50164173134291,3.05761274676646));
#43316=CARTESIAN_POINT('Ctrl Pts',(-6.94656031048454,-0.670069220816254,
4.60016279746532));
#43317=CARTESIAN_POINT('Ctrl Pts',(-6.74808715875641,-4.22838671869335,
1.93164082610646));
#43318=CARTESIAN_POINT('Ctrl Pts',(-6.54961400702828,-3.91596272468331,
-2.50514000860802));
#43319=CARTESIAN_POINT('Ctrl Pts',(-6.35114085530016,-0.0187957997636384,
-4.64867048109021));
#43320=CARTESIAN_POINT('Ctrl Pts',(-6.15266770357202,3.89557713941664,-2.53672412274591));
#43321=CARTESIAN_POINT('Ctrl Pts',(-5.95419455184391,4.24386848014819,1.8973852657751));
#43322=CARTESIAN_POINT('Ctrl Pts',(-5.75572140011576,0.707246045382618,
4.59459394888022));
#43323=CARTESIAN_POINT('Ctrl Pts',(-5.55724824838764,-3.47680217990147,
3.08582843446728));
#43324=CARTESIAN_POINT('Ctrl Pts',(-5.35877509665951,-4.47812295987505,
-1.24776010426379));
#43325=CARTESIAN_POINT('Ctrl Pts',(-5.16030194493138,-1.38008918797814,
-4.43912653089702));
#43326=CARTESIAN_POINT('Ctrl Pts',(-4.96182879320324,2.98130312838602,-3.56683643984536));
#43327=CARTESIAN_POINT('Ctrl Pts',(-4.76335564147512,4.61355676801949,0.570600082934498));
#43328=CARTESIAN_POINT('Ctrl Pts',(-4.56488248974698,2.02247731019143,4.18569899305294));
#43329=CARTESIAN_POINT('Ctrl Pts',(-4.36640933801885,-2.42001438061241,
3.96913352904242));
#43330=CARTESIAN_POINT('Ctrl Pts',(-4.16793618629072,-4.64718121967184,
0.119151613750008));
#43331=CARTESIAN_POINT('Ctrl Pts',(-3.9694630345626,-2.62023457294503,-3.83990382567675));
#43332=CARTESIAN_POINT('Ctrl Pts',(-3.77098988283446,1.80532216910622,-4.2838420471841));
#43333=CARTESIAN_POINT('Ctrl Pts',(-3.57251673110634,4.57825424888385,-0.806273921550659));
#43334=CARTESIAN_POINT('Ctrl Pts',(-3.37404357937821,3.16017012504447,3.40937180891919));
#43335=CARTESIAN_POINT('Ctrl Pts',(-3.17557042765009,-1.15079139389106,
4.50401724481208));
#43336=CARTESIAN_POINT('Ctrl Pts',(-2.97709727592194,-4.40829647230588,
1.47560370320468));
#43337=CARTESIAN_POINT('Ctrl Pts',(-2.77862412419382,-3.6303697878378,-2.9036034622217));
#43338=CARTESIAN_POINT('Ctrl Pts',(-2.58015097246569,0.470867420796771,
-4.62480083442049));
#43339=CARTESIAN_POINT('Ctrl Pts',(-2.38167782073757,4.14105545114363,-2.11236977893991));
#43340=CARTESIAN_POINT('Ctrl Pts',(-2.18320466900942,4.02046314377869,2.33375828107032));
#43341=CARTESIAN_POINT('Ctrl Pts',(-1.98473151728131,0.219434708775458,
4.64353032567314));
#43342=CARTESIAN_POINT('Ctrl Pts',(-1.78625836555316,-3.78240772570626,
2.70251482356271));
#43343=CARTESIAN_POINT('Ctrl Pts',(-1.58778521382503,-4.32188158398657,
-1.71240070088942));
#43344=CARTESIAN_POINT('Ctrl Pts',(-1.3893120620969,-0.90480577337975,-4.55981265027423));
#43345=CARTESIAN_POINT('Ctrl Pts',(-1.19083891036878,3.34012231182713,-3.2329771300526));
#43346=CARTESIAN_POINT('Ctrl Pts',(-0.992365758640643,4.52825177242018,
1.05316839446738));
#43347=CARTESIAN_POINT('Ctrl Pts',(-0.793892606912516,1.5695887441549,4.37563724216484));
#43348=CARTESIAN_POINT('Ctrl Pts',(-0.595419455184388,-2.82293548626305,
3.69177659323615));
#43349=CARTESIAN_POINT('Ctrl Pts',(-0.396946303456266,-4.63702310608274,
-0.370061573871447));
#43350=CARTESIAN_POINT('Ctrl Pts',(-0.198473151728126,-2.19487812995514,
-4.09631897812866));
#43351=CARTESIAN_POINT('Ctrl Pts',(-0.0661577172427097,0.75551006232788,
-4.07532749258864));
#43352=CARTESIAN_POINT('Ctrl Pts',(0.,1.9005636551884,-3.44330463255532));
#43353=CARTESIAN_POINT('Ctrl Pts',(-54.8403753524613,2.14656790565188,-3.00907133330622));
#43354=CARTESIAN_POINT('Ctrl Pts',(-54.7742176352186,3.14721940444736,-2.29524100024571));
#43355=CARTESIAN_POINT('Ctrl Pts',(-54.6419022007332,4.36310735044169,0.19681737971748));
#43356=CARTESIAN_POINT('Ctrl Pts',(-54.443429049005,2.19665054817406,3.77980425424614));
#43357=CARTESIAN_POINT('Ctrl Pts',(-54.2449558972769,-1.98260099992042,
3.89172142956237));
#43358=CARTESIAN_POINT('Ctrl Pts',(-54.0464827455487,-4.34592358414638,
0.446568491290883));
#43359=CARTESIAN_POINT('Ctrl Pts',(-53.8480095938207,-2.7314433830302,-3.41021906903733));
#43360=CARTESIAN_POINT('Ctrl Pts',(-53.6495364420925,1.38372868081164,-4.14375004305525));
#43361=CARTESIAN_POINT('Ctrl Pts',(-53.4510632903644,4.23206450278455,-1.0847911861996));
#43362=CARTESIAN_POINT('Ctrl Pts',(-53.2525901386363,3.20636848042456,2.96760958715623));
#43363=CARTESIAN_POINT('Ctrl Pts',(-53.0541169869081,-0.754535021833214,
4.30319552163747));
#43364=CARTESIAN_POINT('Ctrl Pts',(-52.8556438351801,-4.02470267833369,
1.6996692062514));
#43365=CARTESIAN_POINT('Ctrl Pts',(-52.6571706834518,-3.61059580179964,
-2.45982277671647));
#43366=CARTESIAN_POINT('Ctrl Pts',(-52.4586975317238,0.108721320903615,
-4.36751838360758));
#43367=CARTESIAN_POINT('Ctrl Pts',(-52.2602243799956,3.72851000157542,-2.27712466543675));
#43368=CARTESIAN_POINT('Ctrl Pts',(-52.0617512282675,3.93515491590644,1.89779831841912));
#43369=CARTESIAN_POINT('Ctrl Pts',(-51.8632780765393,0.539487205671952,
4.33543816108556));
#43370=CARTESIAN_POINT('Ctrl Pts',(-51.6648049248112,-3.35003639980807,
2.80434194871354));
#43371=CARTESIAN_POINT('Ctrl Pts',(-51.4663317730831,-4.17287646566163,
-1.29390066104614));
#43372=CARTESIAN_POINT('Ctrl Pts',(-51.267858621355,-1.17579001023567,-4.20768264338388));
#43373=CARTESIAN_POINT('Ctrl Pts',(-51.0693854696268,2.89763577350922,-3.26967634074781));
#43374=CARTESIAN_POINT('Ctrl Pts',(-50.8709123178987,4.31851352219464,0.661450845288393));
#43375=CARTESIAN_POINT('Ctrl Pts',(-50.6724391661706,1.78614606032967,3.98707390524443));
#43376=CARTESIAN_POINT('Ctrl Pts',(-50.4739660144425,-2.38129172253409,
3.66285762271801));
#43377=CARTESIAN_POINT('Ctrl Pts',(-50.2754928627142,-4.36885210329787,
-0.0144046379382577));
#43378=CARTESIAN_POINT('Ctrl Pts',(-50.0770197109862,-2.35708644242635,
-3.6784806205214));
#43379=CARTESIAN_POINT('Ctrl Pts',(-49.878546559258,1.81239867372601,-3.9752090816288));
#43380=CARTESIAN_POINT('Ctrl Pts',(-49.68007340753,4.32278134486142,-0.632959424273409));
#43381=CARTESIAN_POINT('Ctrl Pts',(-49.4816002558018,2.87601197989481,3.28871270826757));
#43382=CARTESIAN_POINT('Ctrl Pts',(-49.2831271040736,-1.20351064099935,
4.19983789284593));
#43383=CARTESIAN_POINT('Ctrl Pts',(-49.0846539523456,-4.18131790718314,
1.26635569532051));
#43384=CARTESIAN_POINT('Ctrl Pts',(-48.8861808006174,-3.33147132072511,
-2.82637135334204));
#43385=CARTESIAN_POINT('Ctrl Pts',(-48.6877076488893,0.568064219917555,
-4.33178707120854));
#43386=CARTESIAN_POINT('Ctrl Pts',(-48.4892344971611,3.94758352450775,-1.8718067488612));
#43387=CARTESIAN_POINT('Ctrl Pts',(-48.290761345433,3.71341364749161,2.30165924295085));
#43388=CARTESIAN_POINT('Ctrl Pts',(-48.0922881937049,0.0799179192503589,
4.36814483668739));
#43389=CARTESIAN_POINT('Ctrl Pts',(-47.8938150419767,-3.62673611417318,
2.43595183577544));
#43390=CARTESIAN_POINT('Ctrl Pts',(-47.6953418902486,-4.01341047422385,
-1.72615542563737));
#43391=CARTESIAN_POINT('Ctrl Pts',(-47.4968687385206,-0.726136475239662,
-4.30810886670719));
#43392=CARTESIAN_POINT('Ctrl Pts',(-47.2983955867923,3.22585595431062,-2.94634172324065));
#43393=CARTESIAN_POINT('Ctrl Pts',(-47.0999224350642,4.22484164160472,1.11255979229578));
#43394=CARTESIAN_POINT('Ctrl Pts',(-46.9014492833361,1.35633106455037,4.15300400088985));
#43395=CARTESIAN_POINT('Ctrl Pts',(-46.702976131608,-2.75378944024938,3.39171341755782));
#43396=CARTESIAN_POINT('Ctrl Pts',(-46.5045029798798,-4.34304140690395,
-0.474412822327436));
#43397=CARTESIAN_POINT('Ctrl Pts',(-46.3060298281518,-1.95659491146608,
-3.90625300518234));
#43398=CARTESIAN_POINT('Ctrl Pts',(-46.1075566764235,2.22095386729056,-3.76223870952363));
#43399=CARTESIAN_POINT('Ctrl Pts',(-45.9090835246954,4.36540140493793,-0.17420321993839));
#43400=CARTESIAN_POINT('Ctrl Pts',(-45.7106103729674,2.513681734868,3.57330104019546));
#43401=CARTESIAN_POINT('Ctrl Pts',(-45.5121372212391,-1.63910754775918,
4.04974105776527));
#43402=CARTESIAN_POINT('Ctrl Pts',(-45.3136640695111,-4.29142820798936,
0.818975044640645));
#43403=CARTESIAN_POINT('Ctrl Pts',(-45.1151909177829,-3.01529805963144,
-3.16149550049559));
#43404=CARTESIAN_POINT('Ctrl Pts',(-44.9167177660548,1.02109033525629,-4.24787602400507));
#43405=CARTESIAN_POINT('Ctrl Pts',(-44.7182446143267,4.12275421448949,-1.44567419392479));
#43406=CARTESIAN_POINT('Ctrl Pts',(-44.5197714625986,3.45037450204169,2.67992387648073));
#43407=CARTESIAN_POINT('Ctrl Pts',(-44.3212983108704,-0.380540282073574,
4.35227127851542));
#43408=CARTESIAN_POINT('Ctrl Pts',(-44.1228251591423,-3.86310162617809,
2.04047102745693));
#43409=CARTESIAN_POINT('Ctrl Pts',(-43.9243520074141,-3.80931004265721,
-2.13921321681172));
#43410=CARTESIAN_POINT('Ctrl Pts',(-43.725878855686,-0.268407317586806,
-4.36062308620417));
#43411=CARTESIAN_POINT('Ctrl Pts',(-43.5274057039579,3.51820030867284,-2.59023990705981));
#43412=CARTESIAN_POINT('Ctrl Pts',(-43.3289325522297,4.08418389614513,1.55129561674739));
#43413=CARTESIAN_POINT('Ctrl Pts',(-43.1304594005017,0.911431857243973,
4.27274714413007));
#43414=CARTESIAN_POINT('Ctrl Pts',(-42.9319862487735,-3.09566134805425,
3.08284884582977));
#43415=CARTESIAN_POINT('Ctrl Pts',(-42.7335130970454,-4.26893030266636,
-0.92914490745409));
#43416=CARTESIAN_POINT('Ctrl Pts',(-42.5350399453172,-1.53434343713571,
-4.09058264859536));
#43417=CARTESIAN_POINT('Ctrl Pts',(-42.3365667935891,2.60480909374755,-3.50742722992238));
#43418=CARTESIAN_POINT('Ctrl Pts',(-42.138093641861,4.35947238361319,0.286490356879277));
#43419=CARTESIAN_POINT('Ctrl Pts',(-41.9396204901329,2.12339599885507,3.81814950206473));
#43420=CARTESIAN_POINT('Ctrl Pts',(-41.7411473384047,-2.05647539408362,
3.85460570507537));
#43421=CARTESIAN_POINT('Ctrl Pts',(-41.5426741866766,-4.35381210784742,
0.362486299923509));
#43422=CARTESIAN_POINT('Ctrl Pts',(-41.3442010349485,-2.66559066554748,
-3.46145960424458));
#43423=CARTESIAN_POINT('Ctrl Pts',(-41.1457278832203,1.46276056523167,-4.11672293418855));
#43424=CARTESIAN_POINT('Ctrl Pts',(-40.9472547314922,4.25207438311479,-1.00346381525687));
#43425=CARTESIAN_POINT('Ctrl Pts',(-40.748781579764,3.1489625937313,3.02838418489993));
#43426=CARTESIAN_POINT('Ctrl Pts',(-40.550308428036,-0.836766368305163,
4.28799466335307));
#43427=CARTESIAN_POINT('Ctrl Pts',(-40.3518352763078,-4.05650429965212,
1.62229746192699));
#43428=CARTESIAN_POINT('Ctrl Pts',(-40.1533621245797,-3.56284500665734,
-2.5284801060336));
#43429=CARTESIAN_POINT('Ctrl Pts',(-39.9548889728515,0.192306887150334,
-4.36464136547615));
#43430=CARTESIAN_POINT('Ctrl Pts',(-39.7564158211234,3.77141758681283,-2.20533117103754));
#43431=CARTESIAN_POINT('Ctrl Pts',(-39.5579426693953,3.89810458267071,1.97277896649182));
#43432=CARTESIAN_POINT('Ctrl Pts',(-39.3594695176672,0.456396312997958,
4.3449716447352));
#43433=CARTESIAN_POINT('Ctrl Pts',(-39.160996365939,-3.40310537600674,2.73969888634954));
#43434=CARTESIAN_POINT('Ctrl Pts',(-38.9625232142109,-4.14734300415746,
-1.37354366291613));
#43435=CARTESIAN_POINT('Ctrl Pts',(-38.7640500624828,-1.09502801892821,
-4.22941956133854));
#43436=CARTESIAN_POINT('Ctrl Pts',(-38.5655769107546,2.95969537159059,-3.21360848509214));
#43437=CARTESIAN_POINT('Ctrl Pts',(-38.3671037590266,4.30506021940944,0.743997779115886));
#43438=CARTESIAN_POINT('Ctrl Pts',(-38.1686306072984,1.70949526943414,4.02053505293178));
#43439=CARTESIAN_POINT('Ctrl Pts',(-37.9701574555703,-2.45097249331184,
3.61660199981967));
#43440=CARTESIAN_POINT('Ctrl Pts',(-37.7716843038421,-4.36777581463652,
-0.0980337755429264));
#43441=CARTESIAN_POINT('Ctrl Pts',(-37.573211152114,-2.28623835076616,-3.72292766402423));
#43442=CARTESIAN_POINT('Ctrl Pts',(-37.3747380003859,1.88816294826562,-3.93978639888863));
#43443=CARTESIAN_POINT('Ctrl Pts',(-37.1762648486577,4.33410581775851,-0.550093581623009));
#43444=CARTESIAN_POINT('Ctrl Pts',(-36.9777916969296,2.81253002468074,3.34316482518291));
#43445=CARTESIAN_POINT('Ctrl Pts',(-36.7793185452015,-1.28368649734259,
4.17602983282103));
#43446=CARTESIAN_POINT('Ctrl Pts',(-36.5808453934733,-4.20479323911358,
1.18608178654579));
#43447=CARTESIAN_POINT('Ctrl Pts',(-36.3823722417453,-3.2767563858946,-2.88962692671043));
#43448=CARTESIAN_POINT('Ctrl Pts',(-36.1838990900171,0.650882383010416,
-4.32011901590195));
#43449=CARTESIAN_POINT('Ctrl Pts',(-35.985425938289,3.98269167512894,-1.79589621329561));
#43450=CARTESIAN_POINT('Ctrl Pts',(-35.7869527865608,3.66867315113963,2.37232238495911));
#43451=CARTESIAN_POINT('Ctrl Pts',(-35.5884796348327,-0.00371496649886586,
4.36887427000306));
#43452=CARTESIAN_POINT('Ctrl Pts',(-35.3900064831046,-3.67270233677799,
2.36607982399083));
#43453=CARTESIAN_POINT('Ctrl Pts',(-35.1915333313765,-3.97963172417899,
-1.80266678229203));
#43454=CARTESIAN_POINT('Ctrl Pts',(-34.9930601796483,-0.643534429780106,
-4.3212196919109));
#43455=CARTESIAN_POINT('Ctrl Pts',(-34.7945870279202,3.28166589244464,-2.88405013105466));
#43456=CARTESIAN_POINT('Ctrl Pts',(-34.5961138761921,4.20277004810898,1.19323095450504));
#43457=CARTESIAN_POINT('Ctrl Pts',(-34.3976407244639,1.27658267433185,4.17820689574687));
#43458=CARTESIAN_POINT('Ctrl Pts',(-34.1991675727358,-2.8182115119447,3.33837686039389));
#43459=CARTESIAN_POINT('Ctrl Pts',(-34.0006944210077,-4.33316403332743,
-0.557463584773404));
#43460=CARTESIAN_POINT('Ctrl Pts',(-33.8022212692795,-1.88146001859966,
-3.94299180654511));
#43461=CARTESIAN_POINT('Ctrl Pts',(-33.6037481175514,2.29256644291489,-3.71903418818535));
#43462=CARTESIAN_POINT('Ctrl Pts',(-33.4052749658233,4.3679362195421,-0.0906055742386371));
#43463=CARTESIAN_POINT('Ctrl Pts',(-33.2068018140952,2.44481837342964,3.62076501709402));
#43464=CARTESIAN_POINT('Ctrl Pts',(-33.008328662367,-1.71633032172986,4.01762198505305));
#43465=CARTESIAN_POINT('Ctrl Pts',(-32.8098555106389,-4.30631927392746,
0.736675300978531));
#43466=CARTESIAN_POINT('Ctrl Pts',(-32.6113823589108,-2.95422586710896,
-3.21863724488722));
#43467=CARTESIAN_POINT('Ctrl Pts',(-32.4129092071827,1.10221919932485,-4.22755118534484));
#43468=CARTESIAN_POINT('Ctrl Pts',(-32.2144360554545,4.14967292418903,-1.36648849622798));
#43469=CARTESIAN_POINT('Ctrl Pts',(-32.0159629037264,3.39844118483932,2.7454824168548));
#43470=CARTESIAN_POINT('Ctrl Pts',(-31.8174897519983,-0.463784930617257,
4.34418919088514));
#43471=CARTESIAN_POINT('Ctrl Pts',(-31.6190166002701,-3.90145395286594,
1.96614680065802));
#43472=CARTESIAN_POINT('Ctrl Pts',(-31.420543448542,-3.7676616356771,-2.21174184459168));
#43473=CARTESIAN_POINT('Ctrl Pts',(-31.2220702968138,-0.184883880119101,
-4.36496210051622));
#43474=CARTESIAN_POINT('Ctrl Pts',(-31.0235971450857,3.56713991501999,-2.52241729591716));
#43475=CARTESIAN_POINT('Ctrl Pts',(-30.8251239933576,4.05373947274123,1.62919381143267));
#43476=CARTESIAN_POINT('Ctrl Pts',(-30.6266508416295,0.829472778558662,
4.28941150948485));
#43477=CARTESIAN_POINT('Ctrl Pts',(-30.4281776899014,-3.15410826266673,
3.02302452114573));
#43478=CARTESIAN_POINT('Ctrl Pts',(-30.2297045381732,-4.25036169305628,
-1.01069365599607));
#43479=CARTESIAN_POINT('Ctrl Pts',(-30.0312313864451,-1.45575734355953,
-4.11920462525759));
#43480=CARTESIAN_POINT('Ctrl Pts',(-29.8327582347169,2.67147354336079,-3.45692136086352));
#43481=CARTESIAN_POINT('Ctrl Pts',(-29.6342850829888,4.35318934931119,0.369890087883597));
#43482=CARTESIAN_POINT('Ctrl Pts',(-29.4358119312607,2.04991708359791,3.85809747653482));
#43483=CARTESIAN_POINT('Ctrl Pts',(-29.2373387795326,-2.129886265545,3.81453282643021));
#43484=CARTESIAN_POINT('Ctrl Pts',(-29.0388656278044,-4.35995329928042,
0.279076004279576));
#43485=CARTESIAN_POINT('Ctrl Pts',(-28.8403924760763,-2.59884041951351,
-3.51185202734594));
#43486=CARTESIAN_POINT('Ctrl Pts',(-28.6419193243482,1.54129786918891,-4.08796735144797));
#43487=CARTESIAN_POINT('Ctrl Pts',(-28.44344617262,4.27050427996367,-0.921883605930295));
#43488=CARTESIAN_POINT('Ctrl Pts',(-28.244973020892,3.09041402337959,3.08810902530494));
#43489=CARTESIAN_POINT('Ctrl Pts',(-28.0464998691637,-0.918696988209928,
4.27119093835957));
#43490=CARTESIAN_POINT('Ctrl Pts',(-27.8480267174357,-4.08681620143686,
1.54434760457097));
#43491=CARTESIAN_POINT('Ctrl Pts',(-27.6495535657075,-3.5137901285336,-2.59621938993813));
#43492=CARTESIAN_POINT('Ctrl Pts',(-27.4510804139794,0.275822824688006,
-4.36016031327428));
#43493=CARTESIAN_POINT('Ctrl Pts',(-27.2526072622512,3.81294258772753,-2.13273181876311));
#43494=CARTESIAN_POINT('Ctrl Pts',(-27.0541341105232,3.85962591192093,2.04703786191156));
#43495=CARTESIAN_POINT('Ctrl Pts',(-26.855660958795,0.373138040029648,4.35291215063591));
#43496=CARTESIAN_POINT('Ctrl Pts',(-26.6571878070669,-3.45492712595231,
2.67405212036522));
#43497=CARTESIAN_POINT('Ctrl Pts',(-26.4587146553387,-4.1202896661995,-1.45268346678852));
#43498=CARTESIAN_POINT('Ctrl Pts',(-26.2602415036106,-1.01386470673626,
-4.24960639877456));
#43499=CARTESIAN_POINT('Ctrl Pts',(-26.0617683518825,3.02067029766771,-3.15636296088693));
#43500=CARTESIAN_POINT('Ctrl Pts',(-25.8632952001544,4.29002921191622,0.826272079267115));
#43501=CARTESIAN_POINT('Ctrl Pts',(-25.6648220484262,1.63221798382302,4.05252275025762));
#43502=CARTESIAN_POINT('Ctrl Pts',(-25.4663488966981,-2.51975503553682,
3.56902097905823));
#43503=CARTESIAN_POINT('Ctrl Pts',(-25.26787574497,-4.36509883333121,-0.181626989518244));
#43504=CARTESIAN_POINT('Ctrl Pts',(-25.0694025932418,-2.21455240291618,
-3.76601033493126));
#43505=CARTESIAN_POINT('Ctrl Pts',(-24.8709294415137,1.96323525262301,-3.90291987247102));
#43506=CARTESIAN_POINT('Ctrl Pts',(-24.6724562897855,4.34384193674173,-0.467026141318341));
#43507=CARTESIAN_POINT('Ctrl Pts',(-24.4739831380575,2.74801733931117,3.39639174579671));
#43508=CARTESIAN_POINT('Ctrl Pts',(-24.2755099863293,-1.3633919109241,4.15069135028104));
#43509=CARTESIAN_POINT('Ctrl Pts',(-24.0770368346012,-4.22672760724999,
1.1053732049321));
#43510=CARTESIAN_POINT('Ctrl Pts',(-23.878563682873,-3.22084059224854,-2.9518235156247));
#43511=CARTESIAN_POINT('Ctrl Pts',(-23.6800905311449,0.7334620120889,-4.30686773245864));
#43512=CARTESIAN_POINT('Ctrl Pts',(-23.4816173794168,4.01634025725961,-1.71932752144164));
#43513=CARTESIAN_POINT('Ctrl Pts',(-23.2831442276887,3.62258816714416,2.4421161232296));
#43514=CARTESIAN_POINT('Ctrl Pts',(-23.0846710759605,-0.0873464907944999,
4.36800260744161));
#43515=CARTESIAN_POINT('Ctrl Pts',(-22.8861979242324,-3.71732259513318,
2.29534069623296));
#43516=CARTESIAN_POINT('Ctrl Pts',(-22.6877247725042,-3.94439452704584,
-1.87851750140415));
#43517=CARTESIAN_POINT('Ctrl Pts',(-22.4892516207762,-0.560696543172442,
-4.33274688558486));
#43518=CARTESIAN_POINT('Ctrl Pts',(-22.290778469048,3.33627317254483,-2.82070159822491));
#43519=CARTESIAN_POINT('Ctrl Pts',(-22.0923053173199,4.17915823226011,1.27346482393652));
#43520=CARTESIAN_POINT('Ctrl Pts',(-21.8938321655917,1.19636644477205,4.20187857010344));
#43521=CARTESIAN_POINT('Ctrl Pts',(-21.6953590138636,-2.88160077139558,
3.28381686187937));
#43522=CARTESIAN_POINT('Ctrl Pts',(-21.4968858621355,-4.32169865088358,
-0.64031004913398));
#43523=CARTESIAN_POINT('Ctrl Pts',(-21.2984127104074,-1.8056356122114,-3.97828558853997));
#43524=CARTESIAN_POINT('Ctrl Pts',(-21.0999395586792,2.36333884359729,-3.67446672299738));
#43525=CARTESIAN_POINT('Ctrl Pts',(-20.9014664069511,4.36887028204107,-0.00697472359797444));
#43526=CARTESIAN_POINT('Ctrl Pts',(-20.702993255223,2.37505904008103,3.66690206362268));
#43527=CARTESIAN_POINT('Ctrl Pts',(-20.5045201034948,-1.79292409856378,
3.98403054266156));
#43528=CARTESIAN_POINT('Ctrl Pts',(-20.3060469517667,-4.31963216900934,
0.654105582097085));
#43529=CARTESIAN_POINT('Ctrl Pts',(-20.1075738000386,-2.89207101608637,
-3.27459942985154));
#43530=CARTESIAN_POINT('Ctrl Pts',(-19.9091006483104,1.1829441244129,-4.20567704259232));
#43531=CARTESIAN_POINT('Ctrl Pts',(-19.7106274965823,4.17507087045813,-1.28680201069282));
#43532=CARTESIAN_POINT('Ctrl Pts',(-19.5121543448542,3.34526241403874,2.81003479859068));
#43533=CARTESIAN_POINT('Ctrl Pts',(-19.3136811931261,-0.546859612232254,
4.33451505391088));
#43534=CARTESIAN_POINT('Ctrl Pts',(-19.1152080413979,-3.93837648289131,
1.89110202450305));
#43535=CARTESIAN_POINT('Ctrl Pts',(-18.9167348896698,-3.72463246396239,
-2.28345991785894));
#43536=CARTESIAN_POINT('Ctrl Pts',(-18.7182617379417,-0.101292686794748,
-4.36770145267196));
#43537=CARTESIAN_POINT('Ctrl Pts',(-18.5197885862136,3.61477224341217,-2.45367027457396));
#43538=CARTESIAN_POINT('Ctrl Pts',(-18.3213154344854,4.02180944339694,1.70649494258672));
#43539=CARTESIAN_POINT('Ctrl Pts',(-18.1228422827573,0.747209716429057,
4.30450390030546));
#43540=CARTESIAN_POINT('Ctrl Pts',(-17.9243691310291,-3.21139926629802,
2.96209232477511));
#43541=CARTESIAN_POINT('Ctrl Pts',(-17.725895979301,-4.23023541980685,-1.09187200764678));
#43542=CARTESIAN_POINT('Ctrl Pts',(-17.5274228275729,-1.37663774708501,
-4.14631700444764));
#43543=CARTESIAN_POINT('Ctrl Pts',(-17.3289496758448,2.7371589569525,-3.4051486065142));
#43544=CARTESIAN_POINT('Ctrl Pts',(-17.1304765241166,4.34531096730604,0.45315426234418));
#43545=CARTESIAN_POINT('Ctrl Pts',(-16.9320033723885,1.97568691902713,3.89663154353295));
#43546=CARTESIAN_POINT('Ctrl Pts',(-16.7335302206604,-2.20251658075459,
3.77306200579476));
#43547=CARTESIAN_POINT('Ctrl Pts',(-16.5350570689323,-4.36449666417209,
0.195563433446896));
#43548=CARTESIAN_POINT('Ctrl Pts',(-16.3365839172041,-2.53113775589293,
-3.56095743428143));
#43549=CARTESIAN_POINT('Ctrl Pts',(-16.138110765476,1.61927032153549,-4.05771361900581));
#43550=CARTESIAN_POINT('Ctrl Pts',(-15.9396376137479,4.28736913136016,-0.839965546633269));
#43551=CARTESIAN_POINT('Ctrl Pts',(-15.7411644620197,3.03073288457795,3.14670214199071));
#43552=CARTESIAN_POINT('Ctrl Pts',(-15.5426913102916,-1.00029092596905,
4.25282191626866));
#43553=CARTESIAN_POINT('Ctrl Pts',(-15.3442181585635,-4.11563037539103,
1.46583177794371));
#43554=CARTESIAN_POINT('Ctrl Pts',(-15.1457450068353,-3.46344752397278,
-2.66300721680542));
#43555=CARTESIAN_POINT('Ctrl Pts',(-14.9472718551072,0.359237679255288,
-4.35408135866501));
#43556=CARTESIAN_POINT('Ctrl Pts',(-14.7487987033791,3.85307022943922,-2.0593508674046));
#43557=CARTESIAN_POINT('Ctrl Pts',(-14.550325551651,3.81973277356145,2.12054656318871));
#43558=CARTESIAN_POINT('Ctrl Pts',(-14.3518523999228,0.289743020215,4.35925741042068));
#43559=CARTESIAN_POINT('Ctrl Pts',(-14.1533792481947,-3.50548272145052,
2.60742537336791));
#43560=CARTESIAN_POINT('Ctrl Pts',(-13.9549060964666,-4.0917263331258,-1.53129089427051));
#43561=CARTESIAN_POINT('Ctrl Pts',(-13.7564329447384,-0.932329835533015,
-4.26823584936986));
#43562=CARTESIAN_POINT('Ctrl Pts',(-13.5579597930103,3.08053821482908,-3.09796069940352));
#43563=CARTESIAN_POINT('Ctrl Pts',(-13.3594866412822,4.27342600351457,0.908243568959527));
#43564=CARTESIAN_POINT('Ctrl Pts',(-13.161013489554,1.55434252638836,4.08302528754496));
#43565=CARTESIAN_POINT('Ctrl Pts',(-12.9625403378259,-2.5876141432208,3.52013199097342));
#43566=CARTESIAN_POINT('Ctrl Pts',(-12.7640671860978,-4.36082213976002,
-0.265153641215291));
#43567=CARTESIAN_POINT('Ctrl Pts',(-12.5655940343697,-2.14205487054604,
-3.80771284626886));
#43568=CARTESIAN_POINT('Ctrl Pts',(-12.3671208826415,2.03758807464232,-3.86462301216384));
#43569=CARTESIAN_POINT('Ctrl Pts',(-12.1686477309134,4.35198613364198,-0.383787546252879));
#43570=CARTESIAN_POINT('Ctrl Pts',(-11.9701745791853,2.68249756631029,3.4483739638865));
#43571=CARTESIAN_POINT('Ctrl Pts',(-11.7717014274572,-1.44259767149734,
4.12383173107989));
#43572=CARTESIAN_POINT('Ctrl Pts',(-11.573228275729,-4.24711297311721,1.02425952846461));
#43573=CARTESIAN_POINT('Ctrl Pts',(-11.3747551240009,-3.16374443169717,
-3.0129383264475));
#43574=CARTESIAN_POINT('Ctrl Pts',(-11.1762819722727,0.815772843547351,
-4.29203807716119));
#43575=CARTESIAN_POINT('Ctrl Pts',(-10.9778088205446,4.04851693943592,-1.64212873404349));
#43576=CARTESIAN_POINT('Ctrl Pts',(-10.7793356688165,3.5751755846346,2.51101487990485));
#43577=CARTESIAN_POINT('Ctrl Pts',(-10.5808625170883,-0.170946004531315,
4.36553016844526));
#43578=CARTESIAN_POINT('Ctrl Pts',(-10.3823893653603,-3.76058053689973,
2.2237603768306));
#43579=CARTESIAN_POINT('Ctrl Pts',(-10.1839162136321,-3.9077117964787,-1.953679785362));
#43580=CARTESIAN_POINT('Ctrl Pts',(-9.98544306190399,-0.477653173671534,
-4.34268622326693));
#43581=CARTESIAN_POINT('Ctrl Pts',(-9.78696991017584,3.38965778224963,-2.75631934058907));
#43582=CARTESIAN_POINT('Ctrl Pts',(-9.58849675844771,4.15401484726687,1.35323199664997));
#43583=CARTESIAN_POINT('Ctrl Pts',(-9.3900236067196,1.11571177334673,4.22401034881386));
#43584=CARTESIAN_POINT('Ctrl Pts',(-9.19155045499144,-2.94393398783904,
3.22805341704829));
#43585=CARTESIAN_POINT('Ctrl Pts',(-8.99307730326333,-4.3086494613817,-0.722921854010561));
#43586=CARTESIAN_POINT('Ctrl Pts',(-8.79460415153519,-1.72914948027085,
-4.01212141677566));
#43587=CARTESIAN_POINT('Ctrl Pts',(-8.59613099980706,2.43324513281668,-3.62855264695096));
#43588=CARTESIAN_POINT('Ctrl Pts',(-8.39765784807894,4.36820325012155,0.0766586831246986));
#43589=CARTESIAN_POINT('Ctrl Pts',(-8.19918469635081,2.30442930007647,3.71169527157334));
#43590=CARTESIAN_POINT('Ctrl Pts',(-8.00071154462268,-1.86886080833417,
3.94897904111218));
#43591=CARTESIAN_POINT('Ctrl Pts',(-7.80223839289454,-4.33136201435319,
0.571296147973731));
#43592=CARTESIAN_POINT('Ctrl Pts',(-7.60376524116642,-2.828856284943,-3.32936154648439));
#43593=CARTESIAN_POINT('Ctrl Pts',(-7.40529208943829,1.26323552661883,-4.18226161213738));
#43594=CARTESIAN_POINT('Ctrl Pts',(-7.20681893771015,4.19893874551101,-1.2066439406557));
#43595=CARTESIAN_POINT('Ctrl Pts',(-7.00834578598203,3.29085767848375,2.87355736466697));
#43596=CARTESIAN_POINT('Ctrl Pts',(-6.80987263425389,-0.62973388188193,
4.32325241294972));
#43597=CARTESIAN_POINT('Ctrl Pts',(-6.61139948252577,-3.9738556849657,1.81536420124497));
#43598=CARTESIAN_POINT('Ctrl Pts',(-6.41292633079764,-3.68023829674828,
-2.35434115352581));
#43599=CARTESIAN_POINT('Ctrl Pts',(-6.21445317906951,-0.0176643719493505,
-4.3688401387566));
#43600=CARTESIAN_POINT('Ctrl Pts',(-6.01598002734139,3.66107983767315,-2.38402403729976));
#43601=CARTESIAN_POINT('Ctrl Pts',(-5.81750687561325,3.98840550972488,1.78317068106301));
#43602=CARTESIAN_POINT('Ctrl Pts',(-5.61903372388513,0.664672818521727,
4.31801878554499));
#43603=CARTESIAN_POINT('Ctrl Pts',(-5.42056057215698,-3.2675133631987,2.90007458705824));
#43604=CARTESIAN_POINT('Ctrl Pts',(-5.22208742042888,-4.20855885848927,
-1.17265021240391));
#43605=CARTESIAN_POINT('Ctrl Pts',(-5.02361426870072,-1.29701364379981,
-4.17190984994354));
#43606=CARTESIAN_POINT('Ctrl Pts',(-4.8251411169726,2.80184126323327,-3.35212794070143));
#43607=CARTESIAN_POINT('Ctrl Pts',(-4.62666796524447,4.33584012300842,0.536252366271593));
#43608=CARTESIAN_POINT('Ctrl Pts',(-4.42819481351634,1.90073271238126,3.9337375802369));
#43609=CARTESIAN_POINT('Ctrl Pts',(-4.2297216617882,-2.27433972904608,3.73020844310279));
#43610=CARTESIAN_POINT('Ctrl Pts',(-4.03124851006008,-4.36744052458988,
0.111979189505195));
#43611=CARTESIAN_POINT('Ctrl Pts',(-3.83277535833195,-2.46250751086917,
-3.60875782244023));
#43612=CARTESIAN_POINT('Ctrl Pts',(-3.63430220660381,1.69664939424318,-4.02597283674152));
#43613=CARTESIAN_POINT('Ctrl Pts',(-3.43582905487569,4.30266266652348,-0.757739634511082));
#43614=CARTESIAN_POINT('Ctrl Pts',(-3.23735590314757,2.96994122163641,3.20414201594641));
#43615=CARTESIAN_POINT('Ctrl Pts',(-3.03888275141944,-1.08151860912011,
4.23289441676501));
#43616=CARTESIAN_POINT('Ctrl Pts',(-2.8404095996913,-4.14293563075526,1.3867785883475));
#43617=CARTESIAN_POINT('Ctrl Pts',(-2.64193644796318,-3.41183684929971,
-2.72881878902532));
#43618=CARTESIAN_POINT('Ctrl Pts',(-2.44346329623505,0.442523189453244,
-4.34640734406986));
#43619=CARTESIAN_POINT('Ctrl Pts',(-2.24499014450692,3.89178139112368,-1.98521403391992));
#43620=CARTESIAN_POINT('Ctrl Pts',(-2.04651699277878,3.77844823167868,2.19327588263559));
#43621=CARTESIAN_POINT('Ctrl Pts',(-1.84804384105066,0.206225665474638,
4.36400939900059));
#43622=CARTESIAN_POINT('Ctrl Pts',(-1.64957068932251,-3.55472274501437,
2.53983483767964));
#43623=CARTESIAN_POINT('Ctrl Pts',(-1.45109753759439,-4.06172255398183,
-1.6093214062197));
#43624=CARTESIAN_POINT('Ctrl Pts',(-1.25262438586626,-0.850340284733118,
-4.28533117431376));
#43625=CARTESIAN_POINT('Ctrl Pts',(-1.05415123413814,3.13906104629816,-3.03836555223933));
#43626=CARTESIAN_POINT('Ctrl Pts',(-0.855678082409997,4.25567012809769,
0.989772102224669));
#43627=CARTESIAN_POINT('Ctrl Pts',(-0.657204930681874,1.47510612651486,
4.11224234842401));
#43628=CARTESIAN_POINT('Ctrl Pts',(-0.458731778953743,-2.65300668474432,
3.46954722419258));
#43629=CARTESIAN_POINT('Ctrl Pts',(-0.260258627225623,-4.35789388656455,
-0.347785429041922));
#43630=CARTESIAN_POINT('Ctrl Pts',(-0.0617854754974821,-2.06275573044676,
-3.84973786496513));
#43631=CARTESIAN_POINT('Ctrl Pts',(0.0705299589879341,0.710031545354443,
-3.83000997825599));
#43632=CARTESIAN_POINT('Ctrl Pts',(0.136687676230644,1.78615774484866,-3.23603222681993));
#43633=CARTESIAN_POINT('Ctrl Pts',(-54.7036876762306,2.00907721869526,-2.81633609132854));
#43634=CARTESIAN_POINT('Ctrl Pts',(-54.6375299589879,2.94563558462912,-2.14822759292536));
#43635=CARTESIAN_POINT('Ctrl Pts',(-54.5052145245025,4.08364420124533,0.184210950323209));
#43636=CARTESIAN_POINT('Ctrl Pts',(-54.3067413727744,2.05595199767563,3.53770248699744));
#43637=CARTESIAN_POINT('Ctrl Pts',(-54.1082682210462,-1.85561262339514,
3.64245121016469));
#43638=CARTESIAN_POINT('Ctrl Pts',(-53.9097950693181,-4.06756107929776,
0.417965152687526));
#43639=CARTESIAN_POINT('Ctrl Pts',(-53.7113219175901,-2.55649060090452,
-3.19178975159536));
#43640=CARTESIAN_POINT('Ctrl Pts',(-53.5128487658618,1.29509891681229,-3.87833703725392));
#43641=CARTESIAN_POINT('Ctrl Pts',(-53.3143756141338,3.9609948318926,-1.01530878827405));
#43642=CARTESIAN_POINT('Ctrl Pts',(-53.1159024624056,3.0009960792774,2.77753002820876));
#43643=CARTESIAN_POINT('Ctrl Pts',(-52.9174293106774,-0.706205994732919,
4.02756980915926));
#43644=CARTESIAN_POINT('Ctrl Pts',(-52.7189561589495,-3.76691482331964,
1.59080300819131));
#43645=CARTESIAN_POINT('Ctrl Pts',(-52.5204830072211,-3.37933207340578,
-2.30226767563077));
#43646=CARTESIAN_POINT('Ctrl Pts',(-52.3220098554932,0.101757567714737,
-4.08777270154628));
#43647=CARTESIAN_POINT('Ctrl Pts',(-52.1235367037649,3.48969370319916,-2.13127163478629));
#43648=CARTESIAN_POINT('Ctrl Pts',(-51.9250635520369,3.68310272075172,1.77624167266026));
#43649=CARTESIAN_POINT('Ctrl Pts',(-51.7265904003086,0.504932293005767,
4.05774726229975));
#43650=CARTESIAN_POINT('Ctrl Pts',(-51.5281172485807,-3.13546186679357,
2.62471991114639));
#43651=CARTESIAN_POINT('Ctrl Pts',(-51.3296440968524,-3.9055978716149,-1.21102450778185));
#43652=CARTESIAN_POINT('Ctrl Pts',(-51.1311709451244,-1.10047900991836,
-3.93817466480525));
#43653=CARTESIAN_POINT('Ctrl Pts',(-50.9326977933961,2.71203813553055,-3.06024898229756));
#43654=CARTESIAN_POINT('Ctrl Pts',(-50.734224641668,4.0419066702827,0.619083990334728));
#43655=CARTESIAN_POINT('Ctrl Pts',(-50.53575148994,1.67174089839997,3.73169622595682));
#43656=CARTESIAN_POINT('Ctrl Pts',(-50.3372783382118,-2.22876664568314,
3.4282464513475));
#43657=CARTESIAN_POINT('Ctrl Pts',(-50.1388051864837,-4.0890209946186,-0.0134820006620064));
#43658=CARTESIAN_POINT('Ctrl Pts',(-49.9403320347555,-2.20611174773739,
-3.44286877421536));
#43659=CARTESIAN_POINT('Ctrl Pts',(-49.7418588830274,1.69631199506383,-3.72059136094556));
#43660=CARTESIAN_POINT('Ctrl Pts',(-49.5433857312993,4.04590113291796,-0.59241748482227));
#43661=CARTESIAN_POINT('Ctrl Pts',(-49.3449125795711,2.69179937624523,3.07806604376094));
#43662=CARTESIAN_POINT('Ctrl Pts',(-49.146439427843,-1.12642409537688,3.93083238154904));
#43663=CARTESIAN_POINT('Ctrl Pts',(-48.9479662761149,-3.91349862695974,
1.18524383576916));
#43664=CARTESIAN_POINT('Ctrl Pts',(-48.7494931243867,-3.11808590708118,
-2.6453383014911));
#43665=CARTESIAN_POINT('Ctrl Pts',(-48.5510199726586,0.531678909382298,
-4.05433002985349));
#43666=CARTESIAN_POINT('Ctrl Pts',(-48.3525468209305,3.69473525952908,-1.75191489961062));
#43667=CARTESIAN_POINT('Ctrl Pts',(-48.1540736692024,3.47556429178153,2.15423473817737));
#43668=CARTESIAN_POINT('Ctrl Pts',(-47.9556005174742,0.074799064361738,
4.08835902942712));
#43669=CARTESIAN_POINT('Ctrl Pts',(-47.7571273657462,-3.39443857611954,
2.27992570195889));
#43670=CARTESIAN_POINT('Ctrl Pts',(-47.5586542140179,-3.75634590073117,
-1.61559274805332));
#43671=CARTESIAN_POINT('Ctrl Pts',(-47.3601810622899,-0.679626414904852,
-4.03216844758158));
#43672=CARTESIAN_POINT('Ctrl Pts',(-47.1617079105617,3.0192353531112,-2.75762440082553));
#43673=CARTESIAN_POINT('Ctrl Pts',(-46.9632347588336,3.95423460510833,1.04129877617769));
#43674=CARTESIAN_POINT('Ctrl Pts',(-46.7647616071054,1.26945615632396,3.88699826610166));
#43675=CARTESIAN_POINT('Ctrl Pts',(-46.5662884553774,-2.57740536179706,
3.17446941306502));
#43676=CARTESIAN_POINT('Ctrl Pts',(-46.3678153036492,-4.06486350955272,
-0.444026015242831));
#43677=CARTESIAN_POINT('Ctrl Pts',(-46.1693421519211,-1.83127226140475,
-3.65605201797175));
#43678=CARTESIAN_POINT('Ctrl Pts',(-45.970869000193,2.07869865509402,-3.52126204006689));
#43679=CARTESIAN_POINT('Ctrl Pts',(-45.7723958484648,4.08579131833148,-0.16304525921605));
#43680=CARTESIAN_POINT('Ctrl Pts',(-45.5739226967367,2.35267689192458,3.34442609362352));
#43681=CARTESIAN_POINT('Ctrl Pts',(-45.3754495450085,-1.53412040892052,
3.79034945940863));
#43682=CARTESIAN_POINT('Ctrl Pts',(-45.1769763932805,-4.01655620846509,
0.766518543641464));
#43683=CARTESIAN_POINT('Ctrl Pts',(-44.9785032415522,-2.82216398709376,
-2.95899727668966));
#43684=CARTESIAN_POINT('Ctrl Pts',(-44.7800300898242,0.955688066234348,
-3.97579360298834));
#43685=CARTESIAN_POINT('Ctrl Pts',(-44.581556938096,3.85868602097429,-1.35307673287339));
#43686=CARTESIAN_POINT('Ctrl Pts',(-44.3830837863679,3.22937317275983,2.50827099105437));
#43687=CARTESIAN_POINT('Ctrl Pts',(-44.1846106346398,-0.356166142937589,
4.07350219493382));
#43688=CARTESIAN_POINT('Ctrl Pts',(-43.9861374829116,-3.61566454535351,
1.9097759944505));
#43689=CARTESIAN_POINT('Ctrl Pts',(-43.7876643311835,-3.56531838825102,
-2.00219360799722));
#43690=CARTESIAN_POINT('Ctrl Pts',(-43.5891911794554,-0.251215452199397,
-4.08131905761874));
#43691=CARTESIAN_POINT('Ctrl Pts',(-43.3907180277272,3.29285464128601,-2.42433140574198));
#43692=CARTESIAN_POINT('Ctrl Pts',(-43.1922448759991,3.82258618565147,1.45193295532964));
#43693=CARTESIAN_POINT('Ctrl Pts',(-42.993771724271,0.853053367639089,3.99907169296392));
#43694=CARTESIAN_POINT('Ctrl Pts',(-42.7952985725428,-2.8973798941071,2.88538805063197));
#43695=CARTESIAN_POINT('Ctrl Pts',(-42.5968254208148,-3.99549932555275,
-0.869631872123631));
#43696=CARTESIAN_POINT('Ctrl Pts',(-42.3983522690866,-1.43606658661385,
-3.82857508902685));
#43697=CARTESIAN_POINT('Ctrl Pts',(-42.1998791173585,2.43796741557505,-3.28277159334914));
#43698=CARTESIAN_POINT('Ctrl Pts',(-42.0014059656304,4.08024205914369,0.268140247446303));
#43699=CARTESIAN_POINT('Ctrl Pts',(-41.8029328139022,1.98738950504959,3.57359166787763));
#43700=CARTESIAN_POINT('Ctrl Pts',(-41.6044596621741,-1.92475525893321,
3.60771279992113));
#43701=CARTESIAN_POINT('Ctrl Pts',(-41.405986510446,-4.0749443319846,0.339268543682336));
#43702=CARTESIAN_POINT('Ctrl Pts',(-41.2075133587178,-2.49485584239753,
-3.23974825860909));
#43703=CARTESIAN_POINT('Ctrl Pts',(-41.0090402069898,1.36906869811796,-3.85304105264131));
#43704=CARTESIAN_POINT('Ctrl Pts',(-40.8105670552615,3.97972305130484,-0.939190549579057));
#43705=CARTESIAN_POINT('Ctrl Pts',(-40.6120939035335,2.94726712019311,2.8344119276729));
#43706=CARTESIAN_POINT('Ctrl Pts',(-40.4136207518052,-0.783170308055804,
4.01334258718161));
#43707=CARTESIAN_POINT('Ctrl Pts',(-40.2151476000772,-3.79667950616066,
1.51838703267821));
#43708=CARTESIAN_POINT('Ctrl Pts',(-40.016674448349,-3.33463978370818,-2.36652740664806));
#43709=CARTESIAN_POINT('Ctrl Pts',(-39.818201296621,0.179989361135237,-4.08507996046391));
#43710=CARTESIAN_POINT('Ctrl Pts',(-39.6197281448927,3.52985299738349,-2.0640766144619));
#43711=CARTESIAN_POINT('Ctrl Pts',(-39.4212549931647,3.64842551335801,1.84641970499238));
#43712=CARTESIAN_POINT('Ctrl Pts',(-39.2227818414365,0.427163488621416,
4.06667011294186));
#43713=CARTESIAN_POINT('Ctrl Pts',(-39.0243086897084,-3.18513170058709,
2.56421732765008));
#43714=CARTESIAN_POINT('Ctrl Pts',(-38.8258355379803,-3.88169986415499,
-1.28556626360714));
#43715=CARTESIAN_POINT('Ctrl Pts',(-38.6273623862521,-1.02488993749952,
-3.95851930265825));
#43716=CARTESIAN_POINT('Ctrl Pts',(-38.428889234524,2.7701227292573,-3.00777235148504));
#43717=CARTESIAN_POINT('Ctrl Pts',(-38.2304160827959,4.02931507042192,0.696343677200124));
#43718=CARTESIAN_POINT('Ctrl Pts',(-38.0319429310678,1.59999969823682,3.76301414017378));
#43719=CARTESIAN_POINT('Ctrl Pts',(-37.8334697793396,-2.29398426529913,
3.38495356601323));
#43720=CARTESIAN_POINT('Ctrl Pts',(-37.6349966276115,-4.08801364375652,
-0.0917545746338272));
#43721=CARTESIAN_POINT('Ctrl Pts',(-37.4365234758833,-2.13980157577975,
-3.48446892220266));
#43722=CARTESIAN_POINT('Ctrl Pts',(-37.2380503241552,1.76722346148785,-3.68743755074885));
#43723=CARTESIAN_POINT('Ctrl Pts',(-37.0395771724271,4.05650025743267,-0.514859315691648));
#43724=CARTESIAN_POINT('Ctrl Pts',(-36.841104020699,2.63238352935634,3.12903042616705));
#43725=CARTESIAN_POINT('Ctrl Pts',(-36.6426308689709,-1.20146457559858,
3.90854926118213));
#43726=CARTESIAN_POINT('Ctrl Pts',(-36.4441577172427,-3.9354703309336,1.11011158351183));
#43727=CARTESIAN_POINT('Ctrl Pts',(-36.2456845655146,-3.06687554061621,
-2.70454226660923));
#43728=CARTESIAN_POINT('Ctrl Pts',(-36.0472114137865,0.609192452897957,
-4.04340932986483));
#43729=CARTESIAN_POINT('Ctrl Pts',(-35.8487382620583,3.72759468383047,-1.68086654038461));
#43730=CARTESIAN_POINT('Ctrl Pts',(-35.6502651103302,3.43368948701192,2.22037180676785));
#43731=CARTESIAN_POINT('Ctrl Pts',(-35.451791958602,-0.00347701768072103,
4.08904174151521));
#43732=CARTESIAN_POINT('Ctrl Pts',(-35.2533188068739,-3.43746059765524,
2.21452909059092));
#43733=CARTESIAN_POINT('Ctrl Pts',(-35.0548456551458,-3.72473072703346,
-1.68720344493443));
#43734=CARTESIAN_POINT('Ctrl Pts',(-34.8563725034176,-0.602315146384778,
-4.04443950603062));
#43735=CARTESIAN_POINT('Ctrl Pts',(-34.6578993516896,3.07147058638131,-2.69932267254216));
#43736=CARTESIAN_POINT('Ctrl Pts',(-34.4594261999614,3.93357672815235,1.11680283722956));
#43737=CARTESIAN_POINT('Ctrl Pts',(-34.2609530482334,1.19481576242177,3.91058688017211));
#43738=CARTESIAN_POINT('Ctrl Pts',(-34.0624798965051,-2.63770110938717,
3.1245491372426));
#43739=CARTESIAN_POINT('Ctrl Pts',(-33.864006744777,-4.05561879561619,-0.521757259796585));
#43740=CARTESIAN_POINT('Ctrl Pts',(-33.6655335930489,-1.76094986387445,
-3.69043764754619));
#43741=CARTESIAN_POINT('Ctrl Pts',(-33.4670604413208,2.14572434474499,-3.48082482895569));
#43742=CARTESIAN_POINT('Ctrl Pts',(-33.2685872895926,4.08816377450278,-0.0848021600484351));
#43743=CARTESIAN_POINT('Ctrl Pts',(-33.0701141378645,2.28822432543259,3.38884993618843));
#43744=CARTESIAN_POINT('Ctrl Pts',(-32.8716409861364,-1.60639695584012,
3.76028765838113));
#43745=CARTESIAN_POINT('Ctrl Pts',(-32.6731678344083,-4.030493480731,0.689490214064437));
#43746=CARTESIAN_POINT('Ctrl Pts',(-32.4746946826801,-2.76500355421408,
-3.01247901215746));
#43747=CARTESIAN_POINT('Ctrl Pts',(-32.276221530952,1.03162051269905,-3.95677059876919));
#43748=CARTESIAN_POINT('Ctrl Pts',(-32.0777483792238,3.88388054953854,-1.27896299024718));
#43749=CARTESIAN_POINT('Ctrl Pts',(-31.8792752274958,3.18076625741006,2.56963041490939));
#43750=CARTESIAN_POINT('Ctrl Pts',(-31.6808020757676,-0.434078854912396,
4.06593777635907));
#43751=CARTESIAN_POINT('Ctrl Pts',(-31.4823289240395,-3.65156035169144,
1.84021233868835));
#43752=CARTESIAN_POINT('Ctrl Pts',(-31.2838557723113,-3.52633762018943,
-2.07007667537761));
#43753=CARTESIAN_POINT('Ctrl Pts',(-31.0853826205832,-0.173041808122419,
-4.08538015197453));
#43754=CARTESIAN_POINT('Ctrl Pts',(-30.8869094688551,3.33865959716237,-2.36085292802862));
#43755=CARTESIAN_POINT('Ctrl Pts',(-30.6884363171269,3.79409177029381,1.52484166131915));
#43756=CARTESIAN_POINT('Ctrl Pts',(-30.4899631653989,0.776343882968993,
4.01466868233013));
#43757=CARTESIAN_POINT('Ctrl Pts',(-30.2914900136707,-2.95208320181135,
2.82939555790436));
#43758=CARTESIAN_POINT('Ctrl Pts',(-30.0930168619426,-3.9781200614483,-0.945957308871949));
#43759=CARTESIAN_POINT('Ctrl Pts',(-29.8945437102144,-1.36251404262283,
-3.85536378791437));
#43760=CARTESIAN_POINT('Ctrl Pts',(-29.6960705584863,2.50036191363037,-3.23550069608593));
#43761=CARTESIAN_POINT('Ctrl Pts',(-29.4975974067582,4.07436146200666,0.346198108632488));
#43762=CARTESIAN_POINT('Ctrl Pts',(-29.29912425503,1.91861701743858,3.61098091851795));
#43763=CARTESIAN_POINT('Ctrl Pts',(-29.1006511033019,-1.99346406104904,
3.57020664539346));
#43764=CARTESIAN_POINT('Ctrl Pts',(-28.9021779515738,-4.08069217148748,
0.261200794536527));
#43765=CARTESIAN_POINT('Ctrl Pts',(-28.7037047998456,-2.43238104330263,
-3.28691297628758));
#43766=CARTESIAN_POINT('Ctrl Pts',(-28.5052316481175,1.44257557753361,-3.82612730533229));
#43767=CARTESIAN_POINT('Ctrl Pts',(-28.3067584963894,3.99697248739513,-0.862835667153545));
#43768=CARTESIAN_POINT('Ctrl Pts',(-28.1082853446613,2.89246866794238,2.89031130822918));
#43769=CARTESIAN_POINT('Ctrl Pts',(-27.9098121929331,-0.859853156770183,
3.99761516435712));
#43770=CARTESIAN_POINT('Ctrl Pts',(-27.711339041205,-3.82504988809487,1.44542997308453));
#43771=CARTESIAN_POINT('Ctrl Pts',(-27.5128658894769,-3.2887269393743,-2.42992789434984));
#43772=CARTESIAN_POINT('Ctrl Pts',(-27.3143927377487,0.258155985663226,
-4.0808859259445));
#43773=CARTESIAN_POINT('Ctrl Pts',(-27.1159195860206,3.56871826371137,-1.99612735259016));
#43774=CARTESIAN_POINT('Ctrl Pts',(-26.9174464342925,3.61241145547262,1.91592221394187));
#43775=CARTESIAN_POINT('Ctrl Pts',(-26.7189732825643,0.349238024885499,
4.07410201829554));
#43776=CARTESIAN_POINT('Ctrl Pts',(-26.5205001308362,-3.23363419471944,
2.50277532915898));
#43777=CARTESIAN_POINT('Ctrl Pts',(-26.3220269791081,-3.85637933046123,
-1.35963705197279));
#43778=CARTESIAN_POINT('Ctrl Pts',(-26.12355382738,-0.948925249362072,-3.97741314482529));
#43779=CARTESIAN_POINT('Ctrl Pts',(-25.9250806756518,2.82719212574396,-2.95419348344638));
#43780=CARTESIAN_POINT('Ctrl Pts',(-25.7266075239237,4.0152468200539,0.773348192958842));
#43781=CARTESIAN_POINT('Ctrl Pts',(-25.5281343721956,1.52767213122385,3.79295298059278));
#43782=CARTESIAN_POINT('Ctrl Pts',(-25.3296612204674,-2.35836118916179,
3.34042017640912));
#43783=CARTESIAN_POINT('Ctrl Pts',(-25.1311880687393,-4.08550812686082,
-0.169993525935175));
#43784=CARTESIAN_POINT('Ctrl Pts',(-24.9327149170112,-2.07270721349718,
-3.52479208757375));
#43785=CARTESIAN_POINT('Ctrl Pts',(-24.734241765283,1.83748727939098,-3.65293237708858));
#43786=CARTESIAN_POINT('Ctrl Pts',(-24.5357686135549,4.06561276433087,-0.437112461519451));
#43787=CARTESIAN_POINT('Ctrl Pts',(-24.3372954618268,2.57200297202499,3.17884808781425));
#43788=CARTESIAN_POINT('Ctrl Pts',(-24.1388223100987,-1.27606474557768,
3.88483374401012));
#43789=CARTESIAN_POINT('Ctrl Pts',(-23.9403491583705,-3.95599977200709,
1.03457249982091));
#43790=CARTESIAN_POINT('Ctrl Pts',(-23.7418760066424,-3.01454123202818,
-2.76275507671378));
#43791=CARTESIAN_POINT('Ctrl Pts',(-23.5434028549142,0.686482740837633,
-4.03100680972357));
#43792=CARTESIAN_POINT('Ctrl Pts',(-23.3449297031862,3.75908802705159,-1.60920218070417));
#43793=CARTESIAN_POINT('Ctrl Pts',(-23.146456551458,3.39055631091931,2.28569515815013));
#43794=CARTESIAN_POINT('Ctrl Pts',(-22.9479833997299,-0.0817518254726031,
4.08822591016416));
#43795=CARTESIAN_POINT('Ctrl Pts',(-22.7495102480017,-3.47922286584052,
2.14832090324472));
#43796=CARTESIAN_POINT('Ctrl Pts',(-22.5510370962737,-3.69175052183031,
-1.75819581903476));
#43797=CARTESIAN_POINT('Ctrl Pts',(-22.3525639445455,-0.524783142673121,
-4.05522836677194));
#43798=CARTESIAN_POINT('Ctrl Pts',(-22.1540907928174,3.12258019355253,-2.64003170214662));
#43799=CARTESIAN_POINT('Ctrl Pts',(-21.9556176410892,3.91147728224659,1.19189761471977));
#43800=CARTESIAN_POINT('Ctrl Pts',(-21.7571444893611,1.11973749494471,3.93274235056415));
#43801=CARTESIAN_POINT('Ctrl Pts',(-21.558671337633,-2.69703019780661,3.07348378320514));
#43802=CARTESIAN_POINT('Ctrl Pts',(-21.3601981859049,-4.04488778700894,
-0.599297291844044));
#43803=CARTESIAN_POINT('Ctrl Pts',(-21.1617250341767,-1.68998211713108,
-3.72347081327125));
#43804=CARTESIAN_POINT('Ctrl Pts',(-20.9632518824486,2.2119636738382,-3.43911197246119));
#43805=CARTESIAN_POINT('Ctrl Pts',(-20.7647787307204,4.08903800898778,-0.00652798276298151));
#43806=CARTESIAN_POINT('Ctrl Pts',(-20.5663055789923,2.22293317528866,3.43203184013592));
#43807=CARTESIAN_POINT('Ctrl Pts',(-20.3678324272642,-1.67808479377233,
3.72884779501869));
#43808=CARTESIAN_POINT('Ctrl Pts',(-20.1693592755361,-4.04295366619892,
0.612209201559777));
#43809=CARTESIAN_POINT('Ctrl Pts',(-19.970886123808,-2.70682980863068,-3.06485674063472));
#43810=CARTESIAN_POINT('Ctrl Pts',(-19.7724129720798,1.10717489304186,-3.93629752555922));
#43811=CARTESIAN_POINT('Ctrl Pts',(-19.5739398203517,3.90765172170437,-1.2043805359465));
#43812=CARTESIAN_POINT('Ctrl Pts',(-19.3754666686235,3.13099366151297,2.63004812599908));
#43813=CARTESIAN_POINT('Ctrl Pts',(-19.1769935168954,-0.511832486578831,
4.05688328143518));
#43814=CARTESIAN_POINT('Ctrl Pts',(-18.9785203651673,-3.6861179418498,1.76997428576766));
#43815=CARTESIAN_POINT('Ctrl Pts',(-18.7800472134392,-3.48606452731231,
-2.13720110539941));
#43816=CARTESIAN_POINT('Ctrl Pts',(-18.581574061711,-0.0948047480465078,
-4.08794404478016));
#43817=CARTESIAN_POINT('Ctrl Pts',(-18.3831009099829,3.38324100807146,-2.29650924988542));
#43818=CARTESIAN_POINT('Ctrl Pts',(-18.1846277582548,3.7642069041412,1.59719154653454));
#43819=CARTESIAN_POINT('Ctrl Pts',(-17.9861546065267,0.69934988542084,4.02879438433728));
#43820=CARTESIAN_POINT('Ctrl Pts',(-17.7876814547985,-3.00570463625504,
2.77236615422654));
#43821=CARTESIAN_POINT('Ctrl Pts',(-17.5892083030704,-3.95928290424672,
-1.02193607316972));
#43822=CARTESIAN_POINT('Ctrl Pts',(-17.3907351513422,-1.28846216734285,
-3.88073958116644));
#43823=CARTESIAN_POINT('Ctrl Pts',(-17.1922619996141,2.56184008429538,-3.18704405931314));
#43824=CARTESIAN_POINT('Ctrl Pts',(-16.993788847886,4.06698770142585,0.424129095861815));
#43825=CARTESIAN_POINT('Ctrl Pts',(-16.7953156961579,1.84914139908685,3.64704682444424));
#43826=CARTESIAN_POINT('Ctrl Pts',(-16.5968425444297,-2.06144230263648,
3.53139208902191));
#43827=CARTESIAN_POINT('Ctrl Pts',(-16.3983693927016,-4.08494452748146,
0.183037321071356));
#43828=CARTESIAN_POINT('Ctrl Pts',(-16.1998962409735,-2.36901483030422,
-3.33287311299191));
#43829=CARTESIAN_POINT('Ctrl Pts',(-16.0014230892454,1.515553784877,-3.79781136691262));
#43830=CARTESIAN_POINT('Ctrl Pts',(-15.8029499375172,4.0127571213907,-0.786164574522354));
#43831=CARTESIAN_POINT('Ctrl Pts',(-15.6044767857891,2.83661018984044,2.94515145355875));
#43832=CARTESIAN_POINT('Ctrl Pts',(-15.406003634061,-0.936220888302868,
3.98042270391114));
#43833=CARTESIAN_POINT('Ctrl Pts',(-15.2075304823328,-3.85201847376804,
1.37194319534574));
#43834=CARTESIAN_POINT('Ctrl Pts',(-15.0090573306047,-3.24160884928891,
-2.49243786717293));
#43835=CARTESIAN_POINT('Ctrl Pts',(-14.8105841788766,0.336228001726943,
-4.07519633690948));
#43836=CARTESIAN_POINT('Ctrl Pts',(-14.6121110271485,3.60627567365431,-1.92744655415262));
#43837=CARTESIAN_POINT('Ctrl Pts',(-14.4136378754203,3.57507352861307,1.98472257973647));
#43838=CARTESIAN_POINT('Ctrl Pts',(-14.2151647236922,0.271184573130672,
4.08004085528584));
#43839=CARTESIAN_POINT('Ctrl Pts',(-14.016691571964,-3.28095163337376,2.44041611881411));
#43840=CARTESIAN_POINT('Ctrl Pts',(-13.8182184202359,-3.8296455189581,-1.43320956340302));
#43841=CARTESIAN_POINT('Ctrl Pts',(-13.6197452685078,-0.87261280108946,
-3.99484935296447));
#43842=CARTESIAN_POINT('Ctrl Pts',(-13.4212721167797,2.88322541878955,-2.8995319687756));
#43843=CARTESIAN_POINT('Ctrl Pts',(-13.2227989650515,3.99970707045215,0.850069293693618));
#43844=CARTESIAN_POINT('Ctrl Pts',(-13.0243258133234,1.45478470613215,3.82150178755809));
#43845=CARTESIAN_POINT('Ctrl Pts',(-12.8258526615953,-2.42187382576178,
3.29466259662437));
#43846=CARTESIAN_POINT('Ctrl Pts',(-12.6273795098671,-4.081505361515,-0.248170178365596));
#43847=CARTESIAN_POINT('Ctrl Pts',(-12.428906358139,-2.00485324982196,-3.56382349453281));
#43848=CARTESIAN_POINT('Ctrl Pts',(-12.2304332064109,1.90707769880952,-3.61708848443179));
#43849=CARTESIAN_POINT('Ctrl Pts',(-12.0319600546828,4.07323531398969,-0.359205415289091));
#43850=CARTESIAN_POINT('Ctrl Pts',(-11.8334869029546,2.51067983243849,3.22750077188098));
#43851=CARTESIAN_POINT('Ctrl Pts',(-11.6350137512265,-1.35019726602492,
3.85969452111492));
#43852=CARTESIAN_POINT('Ctrl Pts',(-11.4365405994984,-3.97507942658069,
0.958654268170109));
#43853=CARTESIAN_POINT('Ctrl Pts',(-11.2380674477702,-2.96110216069169,
-2.81995539813183));
#43854=CARTESIAN_POINT('Ctrl Pts',(-11.0395942960421,0.763521448022078,
-4.0171270146606));
#43855=CARTESIAN_POINT('Ctrl Pts',(-10.841121144314,3.78920374757617,-1.53694808398346));
#43856=CARTESIAN_POINT('Ctrl Pts',(-10.6426479925859,3.34618057086064,2.35018085276441));
#43857=CARTESIAN_POINT('Ctrl Pts',(-10.4441748408577,-0.15999667302688,
4.08591183435546));
#43858=CARTESIAN_POINT('Ctrl Pts',(-10.2457016891296,-3.51971007572659,
2.08132540375945));
#43859=CARTESIAN_POINT('Ctrl Pts',(-10.0472285374015,-3.65741737163835,
-1.82854385321865));
#43860=CARTESIAN_POINT('Ctrl Pts',(-9.84875538567335,-0.44705881753592,
-4.06453107592611));
#43861=CARTESIAN_POINT('Ctrl Pts',(-9.65028223394518,3.17254544408314,-2.5797732184696));
#43862=CARTESIAN_POINT('Ctrl Pts',(-9.45180908221709,3.88794436634965,1.26655558807174));
#43863=CARTESIAN_POINT('Ctrl Pts',(-9.25333593048893,1.04424886841893,3.95345655778733));
#43864=CARTESIAN_POINT('Ctrl Pts',(-9.05486277876082,-2.75537088425535,
3.02129206527667));
#43865=CARTESIAN_POINT('Ctrl Pts',(-8.85638962703267,-4.03267441640854,
-0.676617694676789));
#43866=CARTESIAN_POINT('Ctrl Pts',(-8.65791647530455,-1.61839502928575,
-3.75513940922157));
#43867=CARTESIAN_POINT('Ctrl Pts',(-8.45944332357642,2.27739236712315,-3.39613875742363));
#43868=CARTESIAN_POINT('Ctrl Pts',(-8.26097017184829,4.08841370139886,0.0717485868838491));
#43869=CARTESIAN_POINT('Ctrl Pts',(-8.06249702012017,2.15682736925666,3.47395598025235));
#43870=CARTESIAN_POINT('Ctrl Pts',(-7.86402386839202,-1.74915765070859,
3.69604139133657));
#43871=CARTESIAN_POINT('Ctrl Pts',(-7.66555071666391,-4.05393219848626,
0.534703827910877));
#43872=CARTESIAN_POINT('Ctrl Pts',(-7.46707756493577,-2.64766406973572,
-3.11611126684138));
#43873=CARTESIAN_POINT('Ctrl Pts',(-7.26860441320765,1.18232351825157,-3.91438188628729));
#43874=CARTESIAN_POINT('Ctrl Pts',(-7.07013126147951,3.92999082586276,-1.12935670279306));
#43875=CARTESIAN_POINT('Ctrl Pts',(-6.87165810975138,3.08007362562457,2.68950198256747));
#43876=CARTESIAN_POINT('Ctrl Pts',(-6.67318495802325,-0.5893985429476,4.04634202843412));
#43877=CARTESIAN_POINT('Ctrl Pts',(-6.47471180629512,-3.71932465123805,
1.69908757638346));
#43878=CARTESIAN_POINT('Ctrl Pts',(-6.276238654567,-3.44451386881323,-2.20354229844359));
#43879=CARTESIAN_POINT('Ctrl Pts',(-6.07776550283886,-0.0165329441350717,
-4.08900979642298));
#43880=CARTESIAN_POINT('Ctrl Pts',(-5.87929235111075,3.42658253592967,-2.23132395185361));
#43881=CARTESIAN_POINT('Ctrl Pts',(-5.68081919938261,3.73294253930156,1.66895609635091));
#43882=CARTESIAN_POINT('Ctrl Pts',(-5.48234604765447,0.622099591660842,
4.04144362220976));
#43883=CARTESIAN_POINT('Ctrl Pts',(-5.28387289592636,-3.05822454649594,
2.71432073964919));
#43884=CARTESIAN_POINT('Ctrl Pts',(-5.08539974419822,-3.93899475710348,
-1.09754032054403));
#43885=CARTESIAN_POINT('Ctrl Pts',(-4.88692659247009,-1.21393809962148,
-3.90469316899007));
#43886=CARTESIAN_POINT('Ctrl Pts',(-4.68845344074195,2.62237939808053,-3.13741944155749));
#43887=CARTESIAN_POINT('Ctrl Pts',(-4.48998028901383,4.05812347799734,0.501904649608686));
#43888=CARTESIAN_POINT('Ctrl Pts',(-4.29150713728569,1.77898811457109,3.68177616742087));
#43889=CARTESIAN_POINT('Ctrl Pts',(-4.09303398555757,-2.12866507747974,
3.49128335716317));
#43890=CARTESIAN_POINT('Ctrl Pts',(-3.89456083382944,-4.08769982950793,
0.104806765260383));
#43891=CARTESIAN_POINT('Ctrl Pts',(-3.69608768210131,-2.30478044879331,
-3.37761181920371));
#43892=CARTESIAN_POINT('Ctrl Pts',(-3.49761453037318,1.58797661938014,-3.76810362629895));
#43893=CARTESIAN_POINT('Ctrl Pts',(-3.29914137864505,4.02707108416311,-0.709205347471504));
#43894=CARTESIAN_POINT('Ctrl Pts',(-3.10066822691692,2.77971231822834,2.99891222297364));
#43895=CARTESIAN_POINT('Ctrl Pts',(-2.9021950751888,-1.01224582434915,3.96177158871793));
#43896=CARTESIAN_POINT('Ctrl Pts',(-2.70372192346066,-3.87757478920465,
1.29795347349033));
#43897=CARTESIAN_POINT('Ctrl Pts',(-2.50524877173254,-3.19330391076162,
-2.55403411582895));
#43898=CARTESIAN_POINT('Ctrl Pts',(-2.3067756200044,0.414178958109714,-4.06801385371924));
#43899=CARTESIAN_POINT('Ctrl Pts',(-2.10830246827628,3.64250733110373,-1.85805828889993));
#43900=CARTESIAN_POINT('Ctrl Pts',(-1.90982931654813,3.53643331957866,2.05279348420085));
#43901=CARTESIAN_POINT('Ctrl Pts',(-1.71135616482002,0.193016622173817,
4.08448847232805));
#43902=CARTESIAN_POINT('Ctrl Pts',(-1.51288301309187,-3.32703776432247,
2.37715485179658));
#43903=CARTESIAN_POINT('Ctrl Pts',(-1.31440986136375,-3.80156352397709,
-1.50624211154998));
#43904=CARTESIAN_POINT('Ctrl Pts',(-1.11593670963562,-0.795874796086486,
-4.0108496983533));
#43905=CARTESIAN_POINT('Ctrl Pts',(-0.917463557907495,2.93799978076921,
-2.84375397442605));
#43906=CARTESIAN_POINT('Ctrl Pts',(-0.718990406179355,3.98308848377519,
0.926375809981952));
#43907=CARTESIAN_POINT('Ctrl Pts',(-0.520517254451229,1.38062350887484,
3.84884745468318));
#43908=CARTESIAN_POINT('Ctrl Pts',(-0.3220441027231,-2.4830778832256,3.247317855149));
#43909=CARTESIAN_POINT('Ctrl Pts',(-0.123570950994979,-4.07876466704636,
-0.325509284212394));
#43910=CARTESIAN_POINT('Ctrl Pts',(0.0749022007331616,-1.93063333093837,
-3.60315675180159));
#43911=CARTESIAN_POINT('Ctrl Pts',(0.207217635218578,0.664553028381002,
-3.58469246392335));
#43912=CARTESIAN_POINT('Ctrl Pts',(0.273375352461288,1.67175183450892,-3.02875982108454));
#43913=CARTESIAN_POINT('Ctrl Pts',(-54.567,1.87158653173864,-2.62360084935085));
#43914=CARTESIAN_POINT('Ctrl Pts',(-54.5008422827573,2.74405176481089,-2.00121418560501));
#43915=CARTESIAN_POINT('Ctrl Pts',(-54.3685268482719,3.80418105204897,0.171604520928937));
#43916=CARTESIAN_POINT('Ctrl Pts',(-54.1700536965438,1.91525344717721,3.29560071974874));
#43917=CARTESIAN_POINT('Ctrl Pts',(-53.9715805448156,-1.72862424686986,
3.39318099076701));
#43918=CARTESIAN_POINT('Ctrl Pts',(-53.7731073930875,-3.78919857444914,
0.38936181408417));
#43919=CARTESIAN_POINT('Ctrl Pts',(-53.5746342413594,-2.38153781877884,
-2.97336043415339));
#43920=CARTESIAN_POINT('Ctrl Pts',(-53.3761610896312,1.20646915281294,-3.61292403145259));
#43921=CARTESIAN_POINT('Ctrl Pts',(-53.1776879379031,3.68992516100066,-0.945826390348501));
#43922=CARTESIAN_POINT('Ctrl Pts',(-52.979214786175,2.79562367813024,2.58745046926129));
#43923=CARTESIAN_POINT('Ctrl Pts',(-52.7807416344468,-0.657876967632621,
3.75194409668105));
#43924=CARTESIAN_POINT('Ctrl Pts',(-52.5822684827187,-3.50912696830559,
1.48193681013123));
#43925=CARTESIAN_POINT('Ctrl Pts',(-52.3837953309905,-3.14806834501192,
-2.14471257454507));
#43926=CARTESIAN_POINT('Ctrl Pts',(-52.1853221792625,0.0947938145258543,
-3.80802701948498));
#43927=CARTESIAN_POINT('Ctrl Pts',(-51.9868490275343,3.25087740482292,-1.98541860413584));
#43928=CARTESIAN_POINT('Ctrl Pts',(-51.7883758758062,3.43105052559699,1.65468502690142));
#43929=CARTESIAN_POINT('Ctrl Pts',(-51.5899027240781,0.47037738033959,3.78005636351393));
#43930=CARTESIAN_POINT('Ctrl Pts',(-51.3914295723498,-2.92088733377907,
2.44509787357924));
#43931=CARTESIAN_POINT('Ctrl Pts',(-51.1929564206218,-3.63831927756816,
-1.12814835451757));
#43932=CARTESIAN_POINT('Ctrl Pts',(-50.9944832688937,-1.02516800960105,
-3.66866668622662));
#43933=CARTESIAN_POINT('Ctrl Pts',(-50.7960101171655,2.52644049755188,-2.85082162384731));
#43934=CARTESIAN_POINT('Ctrl Pts',(-50.5975369654374,3.76529981837076,0.576717135381059));
#43935=CARTESIAN_POINT('Ctrl Pts',(-50.3990638137093,1.55733573647028,3.47631854666922));
#43936=CARTESIAN_POINT('Ctrl Pts',(-50.2005906619811,-2.07624156883218,
3.19363527997699));
#43937=CARTESIAN_POINT('Ctrl Pts',(-50.002117510253,-3.80918988593932,-0.0125593633857515));
#43938=CARTESIAN_POINT('Ctrl Pts',(-49.8036443585249,-2.05513705304844,
-3.20725692790933));
#43939=CARTESIAN_POINT('Ctrl Pts',(-49.6051712067968,1.58022531640166,-3.46597364026232));
#43940=CARTESIAN_POINT('Ctrl Pts',(-49.4066980550686,3.7690209209745,-0.551875545371135));
#43941=CARTESIAN_POINT('Ctrl Pts',(-49.2082249033405,2.50758677259566,2.8674193792543));
#43942=CARTESIAN_POINT('Ctrl Pts',(-49.0097517516124,-1.04933754975442,
3.66182687025214));
#43943=CARTESIAN_POINT('Ctrl Pts',(-48.8112785998842,-3.64567934673634,
1.10413197621781));
#43944=CARTESIAN_POINT('Ctrl Pts',(-48.6128054481561,-2.90470049343726,
-2.46430524964014));
#43945=CARTESIAN_POINT('Ctrl Pts',(-48.414332296428,0.495293598847041,-3.77687298849846));
#43946=CARTESIAN_POINT('Ctrl Pts',(-48.2158591446999,3.44188699455041,-1.63202305036004));
#43947=CARTESIAN_POINT('Ctrl Pts',(-48.0173859929717,3.23771493607145,2.00681023340388));
#43948=CARTESIAN_POINT('Ctrl Pts',(-47.8189128412436,0.0696802094731201,
3.80857322216686));
#43949=CARTESIAN_POINT('Ctrl Pts',(-47.6204396895155,-3.1621410380659,2.12389956814232));
#43950=CARTESIAN_POINT('Ctrl Pts',(-47.4219665377873,-3.4992813272385,-1.50503007046925));
#43951=CARTESIAN_POINT('Ctrl Pts',(-47.2234933860592,-0.633116354570043,
-3.75622802845598));
#43952=CARTESIAN_POINT('Ctrl Pts',(-47.025020234331,2.81261475191178,-2.56890707841041));
#43953=CARTESIAN_POINT('Ctrl Pts',(-46.826547082603,3.68362756861194,0.970037760059602));
#43954=CARTESIAN_POINT('Ctrl Pts',(-46.6280739308748,1.18258124809755,3.62099253131349));
#43955=CARTESIAN_POINT('Ctrl Pts',(-46.4296007791467,-2.40102128334473,
2.95722540857222));
#43956=CARTESIAN_POINT('Ctrl Pts',(-46.2311276274185,-3.7866856122015,-0.41363920815822));
#43957=CARTESIAN_POINT('Ctrl Pts',(-46.0326544756905,-1.70594961134342,
-3.40585103076117));
#43958=CARTESIAN_POINT('Ctrl Pts',(-45.8341813239623,1.93644344289748,-3.28028537061014));
#43959=CARTESIAN_POINT('Ctrl Pts',(-45.6357081722341,3.80618123172504,-0.151887298493708));
#43960=CARTESIAN_POINT('Ctrl Pts',(-45.4372350205061,2.19167204898115,3.11555114705157));
#43961=CARTESIAN_POINT('Ctrl Pts',(-45.2387618687778,-1.42913327008184,
3.53095786105198));
#43962=CARTESIAN_POINT('Ctrl Pts',(-45.0402887170499,-3.74168420894083,
0.714062042642285));
#43963=CARTESIAN_POINT('Ctrl Pts',(-44.8418155653216,-2.62902991455607,
-2.75649905288374));
#43964=CARTESIAN_POINT('Ctrl Pts',(-44.6433424135935,0.890285797212397,
-3.70371118197161));
#43965=CARTESIAN_POINT('Ctrl Pts',(-44.4448692618654,3.5946178274591,-1.26047927182198));
#43966=CARTESIAN_POINT('Ctrl Pts',(-44.2463961101372,3.00837184347797,2.33661810562801));
#43967=CARTESIAN_POINT('Ctrl Pts',(-44.0479229584092,-0.331792003801605,
3.79473311135223));
#43968=CARTESIAN_POINT('Ctrl Pts',(-43.8494498066809,-3.36822746452892,
1.77908096144407));
#43969=CARTESIAN_POINT('Ctrl Pts',(-43.6509766549529,-3.32132673384483,
-1.86517399918272));
#43970=CARTESIAN_POINT('Ctrl Pts',(-43.4525035032247,-0.234023586811988,
-3.80201502903332));
#43971=CARTESIAN_POINT('Ctrl Pts',(-43.2540303514966,3.06750897389918,-2.25842290442415));
#43972=CARTESIAN_POINT('Ctrl Pts',(-43.0555571997685,3.5609884751578,1.35257029391188));
#43973=CARTESIAN_POINT('Ctrl Pts',(-42.8570840480403,0.794674878034206,
3.72539624179777));
#43974=CARTESIAN_POINT('Ctrl Pts',(-42.6586108963122,-2.69909844015994,
2.68792725543417));
#43975=CARTESIAN_POINT('Ctrl Pts',(-42.460137744584,-3.72206834843915,-0.810118836793174));
#43976=CARTESIAN_POINT('Ctrl Pts',(-42.261664592856,-1.33778973609199,-3.56656752945834));
#43977=CARTESIAN_POINT('Ctrl Pts',(-42.0631914411278,2.27112573740255,-3.05811595677589));
#43978=CARTESIAN_POINT('Ctrl Pts',(-41.8647182893997,3.80101173467418,0.249790138013328));
#43979=CARTESIAN_POINT('Ctrl Pts',(-41.6662451376716,1.8513830112441,3.32903383369054));
#43980=CARTESIAN_POINT('Ctrl Pts',(-41.4677719859434,-1.7930351237828,3.36081989476688));
#43981=CARTESIAN_POINT('Ctrl Pts',(-41.2692988342154,-3.7960765561218,0.316050787441167));
#43982=CARTESIAN_POINT('Ctrl Pts',(-41.0708256824871,-2.32412101924758,
-3.0180369129736));
#43983=CARTESIAN_POINT('Ctrl Pts',(-40.8723525307591,1.27537683100426,-3.58935917109407));
#43984=CARTESIAN_POINT('Ctrl Pts',(-40.6738793790308,3.70737171949489,-0.874917283901245));
#43985=CARTESIAN_POINT('Ctrl Pts',(-40.4754062273029,2.74557164665491,2.64043967044588));
#43986=CARTESIAN_POINT('Ctrl Pts',(-40.2769330755746,-0.72957424780644,
3.73869051101015));
#43987=CARTESIAN_POINT('Ctrl Pts',(-40.0784599238466,-3.5368547126692,1.41447660342944));
#43988=CARTESIAN_POINT('Ctrl Pts',(-39.8799867721184,-3.10643456075901,
-2.20457470726251));
#43989=CARTESIAN_POINT('Ctrl Pts',(-39.6815136203903,0.16767183512014,-3.80551855545168));
#43990=CARTESIAN_POINT('Ctrl Pts',(-39.4830404686621,3.28828840795416,-1.92282205788625));
#43991=CARTESIAN_POINT('Ctrl Pts',(-39.284567316934,3.39874644404531,1.72006044349292));
#43992=CARTESIAN_POINT('Ctrl Pts',(-39.0860941652058,0.397930664244868,
3.78836858114853));
#43993=CARTESIAN_POINT('Ctrl Pts',(-38.8876210134778,-2.96715802516744,
2.38873576895062));
#43994=CARTESIAN_POINT('Ctrl Pts',(-38.6891478617496,-3.61605672415252,
-1.19758886429816));
#43995=CARTESIAN_POINT('Ctrl Pts',(-38.4906747100216,-0.954751856070833,
-3.68761904397796));
#43996=CARTESIAN_POINT('Ctrl Pts',(-38.2922015582933,2.58055008692402,-2.80193621787794));
#43997=CARTESIAN_POINT('Ctrl Pts',(-38.0937284065653,3.7535699214344,0.648689575284357));
#43998=CARTESIAN_POINT('Ctrl Pts',(-37.895255254837,1.4905041270395,3.50549322741577));
#43999=CARTESIAN_POINT('Ctrl Pts',(-37.696782103109,-2.13699603728643,3.1533051322068));
#44000=CARTESIAN_POINT('Ctrl Pts',(-37.4983089513808,-3.80825147287653,
-0.0854753737247307));
#44001=CARTESIAN_POINT('Ctrl Pts',(-37.2998357996528,-1.99336480079335,
-3.24601018038109));
#44002=CARTESIAN_POINT('Ctrl Pts',(-37.1013626479246,1.64628397471009,-3.43508870260906));
#44003=CARTESIAN_POINT('Ctrl Pts',(-36.9028894961965,3.77889469710683,-0.479625049760291));
#44004=CARTESIAN_POINT('Ctrl Pts',(-36.7044163444683,2.45223703403194,2.9148960271512));
#44005=CARTESIAN_POINT('Ctrl Pts',(-36.5059431927402,-1.11924265385457,
3.64106868954325));
#44006=CARTESIAN_POINT('Ctrl Pts',(-36.3074700410121,-3.66614742275361,
1.03414138047787));
#44007=CARTESIAN_POINT('Ctrl Pts',(-36.108996889284,-2.85699469533783,-2.51945760650804));
#44008=CARTESIAN_POINT('Ctrl Pts',(-35.9105237375558,0.567502522785501,
-3.76669964382771));
#44009=CARTESIAN_POINT('Ctrl Pts',(-35.7120505858277,3.472497692532,-1.5658368674736));
#44010=CARTESIAN_POINT('Ctrl Pts',(-35.5135774340996,3.19870582288421,2.06842122857658));
#44011=CARTESIAN_POINT('Ctrl Pts',(-35.3151042823714,-0.00323906886257519,
3.80920921302736));
#44012=CARTESIAN_POINT('Ctrl Pts',(-35.1166311306433,-3.2022188585325,2.062978357191));
#44013=CARTESIAN_POINT('Ctrl Pts',(-34.9181579789152,-3.46982972988793,
-1.57174010757682));
#44014=CARTESIAN_POINT('Ctrl Pts',(-34.719684827187,-0.56109586298945,-3.76765932015034));
#44015=CARTESIAN_POINT('Ctrl Pts',(-34.521211675459,2.86127528031798,-2.51459521402966));
#44016=CARTESIAN_POINT('Ctrl Pts',(-34.3227385237307,3.66438340819573,1.04037471995407));
#44017=CARTESIAN_POINT('Ctrl Pts',(-34.1242653720026,1.1130488505117,3.64296686459735));
#44018=CARTESIAN_POINT('Ctrl Pts',(-33.9257922202745,-2.45719070682964,
2.91072141409131));
#44019=CARTESIAN_POINT('Ctrl Pts',(-33.7273190685464,-3.77807355790493,
-0.486050934819766));
#44020=CARTESIAN_POINT('Ctrl Pts',(-33.5288459168183,-1.64043970914924,
-3.43788348854727));
#44021=CARTESIAN_POINT('Ctrl Pts',(-33.3303727650901,1.99888224657508,-3.24261546972602));
#44022=CARTESIAN_POINT('Ctrl Pts',(-33.131899613362,3.80839132946346,-0.0789987458582374));
#44023=CARTESIAN_POINT('Ctrl Pts',(-32.9334264616339,2.13163027743554,3.15693485528285));
#44024=CARTESIAN_POINT('Ctrl Pts',(-32.7349533099058,-1.49646358995037,
3.50295333170919));
#44025=CARTESIAN_POINT('Ctrl Pts',(-32.5364801581776,-3.75466768753454,
0.642305127150348));
#44026=CARTESIAN_POINT('Ctrl Pts',(-32.3380070064495,-2.5757812413192,-2.8063207794277));
#44027=CARTESIAN_POINT('Ctrl Pts',(-32.1395338547213,0.961021826073252,
-3.68599001219353));
#44028=CARTESIAN_POINT('Ctrl Pts',(-31.9410607029932,3.61808817488804,-1.19143748426638));
#44029=CARTESIAN_POINT('Ctrl Pts',(-31.7425875512651,2.96309132998079,2.39377841296397));
#44030=CARTESIAN_POINT('Ctrl Pts',(-31.5441143995369,-0.404372779207533,
3.78768636183299));
#44031=CARTESIAN_POINT('Ctrl Pts',(-31.3456412478088,-3.40166675051695,
1.7142778767187));
#44032=CARTESIAN_POINT('Ctrl Pts',(-31.1471680960807,-3.28501360470175,
-1.92841150616356));
#44033=CARTESIAN_POINT('Ctrl Pts',(-30.9486949443525,-0.16119973612574,
-3.80579820343283));
#44034=CARTESIAN_POINT('Ctrl Pts',(-30.7502217926245,3.11017927930475,-2.19928856014008));
#44035=CARTESIAN_POINT('Ctrl Pts',(-30.5517486408963,3.53444406784637,1.42048951120562));
#44036=CARTESIAN_POINT('Ctrl Pts',(-30.3532754891682,0.723214987379329,
3.73992585517541));
#44037=CARTESIAN_POINT('Ctrl Pts',(-30.1548023374401,-2.75005814095598,
2.63576659466299));
#44038=CARTESIAN_POINT('Ctrl Pts',(-29.9563291857119,-3.70587842984033,
-0.881220961747833));
#44039=CARTESIAN_POINT('Ctrl Pts',(-29.7578560339838,-1.26927074168613,
-3.59152295057115));
#44040=CARTESIAN_POINT('Ctrl Pts',(-29.5593828822556,2.32925028389996,-3.01408003130834));
#44041=CARTESIAN_POINT('Ctrl Pts',(-29.3609097305275,3.79553357470212,0.322506129381382));
#44042=CARTESIAN_POINT('Ctrl Pts',(-29.1624365787994,1.78731695127927,3.36386436050109));
#44043=CARTESIAN_POINT('Ctrl Pts',(-28.9639634270713,-1.85704185655309,
3.32588046435669));
#44044=CARTESIAN_POINT('Ctrl Pts',(-28.7654902753432,-3.80143104369453,
0.243325584793488));
#44045=CARTESIAN_POINT('Ctrl Pts',(-28.567017123615,-2.26592166709176,-3.06197392522923));
#44046=CARTESIAN_POINT('Ctrl Pts',(-28.3685439718869,1.34385328587831,-3.56428725921659));
#44047=CARTESIAN_POINT('Ctrl Pts',(-28.1700708201588,3.72344069482658,-0.803787728376804));
#44048=CARTESIAN_POINT('Ctrl Pts',(-27.9715976684306,2.69452331250517,2.69251359115343));
#44049=CARTESIAN_POINT('Ctrl Pts',(-27.7731245167025,-0.801009325330438,
3.72403939035468));
#44050=CARTESIAN_POINT('Ctrl Pts',(-27.5746513649744,-3.56328357475288,
1.3465123415981));
#44051=CARTESIAN_POINT('Ctrl Pts',(-27.3761782132462,-3.063663750215,-2.26363639876154));
#44052=CARTESIAN_POINT('Ctrl Pts',(-27.1777050615181,0.240489146638442,
-3.80161153861474));
#44053=CARTESIAN_POINT('Ctrl Pts',(-26.9792319097899,3.32449393969521,-1.85952288641721));
#44054=CARTESIAN_POINT('Ctrl Pts',(-26.7807587580619,3.36519699902431,1.78480656597217));
#44055=CARTESIAN_POINT('Ctrl Pts',(-26.5822856063336,0.325338009741355,
3.79529188595517));
#44056=CARTESIAN_POINT('Ctrl Pts',(-26.3838124546056,-3.01234126348658,
2.33149853795273));
#44057=CARTESIAN_POINT('Ctrl Pts',(-26.1853393028774,-3.59246899472296,
-1.26659063715707));
#44058=CARTESIAN_POINT('Ctrl Pts',(-25.9868661511494,-0.883985791987881,
-3.70521989087602));
#44059=CARTESIAN_POINT('Ctrl Pts',(-25.7883929994212,2.63371395382021,-2.75202400600582));
#44060=CARTESIAN_POINT('Ctrl Pts',(-25.5899198476931,3.74046442819159,0.720424306650572));
#44061=CARTESIAN_POINT('Ctrl Pts',(-25.3914466959649,1.42312627862469,3.53338321092794));
#44062=CARTESIAN_POINT('Ctrl Pts',(-25.1929735442368,-2.19696734278675,
3.11181937376001));
#44063=CARTESIAN_POINT('Ctrl Pts',(-24.9945003925087,-3.80591742039044,
-0.158360062352112));
#44064=CARTESIAN_POINT('Ctrl Pts',(-24.7960272407805,-1.93086202407817,
-3.28357384021623));
#44065=CARTESIAN_POINT('Ctrl Pts',(-24.5975540890524,1.71173930615894,-3.40294488170616));
#44066=CARTESIAN_POINT('Ctrl Pts',(-24.3990809373243,3.78738359192001,-0.407198781720557));
#44067=CARTESIAN_POINT('Ctrl Pts',(-24.2006077855962,2.3959886047388,2.9613044298318));
#44068=CARTESIAN_POINT('Ctrl Pts',(-24.002134633868,-1.18873758023125,3.6189761377392));
#44069=CARTESIAN_POINT('Ctrl Pts',(-23.8036614821399,-3.6852719367642,0.963771794709725));
#44070=CARTESIAN_POINT('Ctrl Pts',(-23.6051883304118,-2.80824187180781,
-2.57368663780286));
#44071=CARTESIAN_POINT('Ctrl Pts',(-23.4067151786836,0.639503469586358,
-3.7551458869885));
#44072=CARTESIAN_POINT('Ctrl Pts',(-23.2082420269555,3.50183579684358,-1.4990768399667));
#44073=CARTESIAN_POINT('Ctrl Pts',(-23.0097688752274,3.15852445469445,2.12927419307066));
#44074=CARTESIAN_POINT('Ctrl Pts',(-22.8112957234992,-0.0761571601507046,
3.80844921288671));
#44075=CARTESIAN_POINT('Ctrl Pts',(-22.6128225717711,-3.24112313654785,
2.00130111025649));
#44076=CARTESIAN_POINT('Ctrl Pts',(-22.414349420043,-3.43910651661478,-1.63787413666537));
#44077=CARTESIAN_POINT('Ctrl Pts',(-22.2158762683149,-0.488869742173803,
-3.77770984795902));
#44078=CARTESIAN_POINT('Ctrl Pts',(-22.0174031165867,2.90888721456023,-2.45936180606832));
#44079=CARTESIAN_POINT('Ctrl Pts',(-21.8189299648586,3.64379633223308,1.11033040550302));
#44080=CARTESIAN_POINT('Ctrl Pts',(-21.6204568131305,1.04310854511736,3.66360613102486));
#44081=CARTESIAN_POINT('Ctrl Pts',(-21.4219836614024,-2.51245962421763,
2.8631507045309));
#44082=CARTESIAN_POINT('Ctrl Pts',(-21.2235105096742,-3.76807692313431,
-0.558284534554106));
#44083=CARTESIAN_POINT('Ctrl Pts',(-21.0250373579461,-1.57432862205077,
-3.46865603800252));
#44084=CARTESIAN_POINT('Ctrl Pts',(-20.8265642062179,2.06058850407911,-3.20375722192501));
#44085=CARTESIAN_POINT('Ctrl Pts',(-20.6280910544898,3.80920573593449,-0.00608124192798155));
#44086=CARTESIAN_POINT('Ctrl Pts',(-20.4296179027617,2.07080731049629,3.19716161664916));
#44087=CARTESIAN_POINT('Ctrl Pts',(-20.2311447510336,-1.56324548898088,
3.47366504737583));
#44088=CARTESIAN_POINT('Ctrl Pts',(-20.0326715993054,-3.76627516338849,
0.570312821022469));
#44089=CARTESIAN_POINT('Ctrl Pts',(-19.8341984475773,-2.52158860117499,
-2.8551140514179));
#44090=CARTESIAN_POINT('Ctrl Pts',(-19.6357252958492,1.03140566167082,-3.66691800852612));
#44091=CARTESIAN_POINT('Ctrl Pts',(-19.437252144121,3.64023257295061,-1.12195906120018));
#44092=CARTESIAN_POINT('Ctrl Pts',(-19.2387789923929,2.9167249089872,2.45006145340748));
#44093=CARTESIAN_POINT('Ctrl Pts',(-19.0403058406648,-0.476805360925414,
3.77925150895946));
#44094=CARTESIAN_POINT('Ctrl Pts',(-18.8418326889367,-3.43385940080828,
1.64884654703227));
#44095=CARTESIAN_POINT('Ctrl Pts',(-18.6433595372085,-3.24749659066223,
-1.9909422929399));
#44096=CARTESIAN_POINT('Ctrl Pts',(-18.4448863854804,-0.088316809298266,
-3.80818663688835));
#44097=CARTESIAN_POINT('Ctrl Pts',(-18.2464132337523,3.15170977273075,-2.13934822519688));
#44098=CARTESIAN_POINT('Ctrl Pts',(-18.0479400820241,3.50660436488545,1.48788815048238));
#44099=CARTESIAN_POINT('Ctrl Pts',(-17.849466930296,0.651490054412623,3.7530848683691));
#44100=CARTESIAN_POINT('Ctrl Pts',(-17.6509937785678,-2.80001000621206,
2.58263998367796));
#44101=CARTESIAN_POINT('Ctrl Pts',(-17.4525206268398,-3.68833038868658,
-0.952000138692661));
#44102=CARTESIAN_POINT('Ctrl Pts',(-17.2540474751116,-1.2002865876007,-3.61516215788525));
#44103=CARTESIAN_POINT('Ctrl Pts',(-17.0555743233835,2.38652121163826,-2.96893951211207));
#44104=CARTESIAN_POINT('Ctrl Pts',(-16.8571011716553,3.78866443554566,0.395103929379446));
#44105=CARTESIAN_POINT('Ctrl Pts',(-16.6586280199273,1.72259587914657,3.39746210535554));
#44106=CARTESIAN_POINT('Ctrl Pts',(-16.4601548681991,-1.92036802451838,
3.28972217224905));
#44107=CARTESIAN_POINT('Ctrl Pts',(-16.261681716471,-3.80539239079082,0.170511208695819));
#44108=CARTESIAN_POINT('Ctrl Pts',(-16.0632085647428,-2.20689190471551,
-3.10478879170239));
#44109=CARTESIAN_POINT('Ctrl Pts',(-15.8647354130147,1.41183724821851,-3.53790911481943));
#44110=CARTESIAN_POINT('Ctrl Pts',(-15.6662622612865,3.73814511142124,-0.732363602411441));
#44111=CARTESIAN_POINT('Ctrl Pts',(-15.4677891095585,2.64248749510294,2.7436007651268));
#44112=CARTESIAN_POINT('Ctrl Pts',(-15.2693159578303,-0.872150850636688,
3.70802349155361));
#44113=CARTESIAN_POINT('Ctrl Pts',(-15.0708428061022,-3.58840657214504,
1.27805461274778));
#44114=CARTESIAN_POINT('Ctrl Pts',(-14.8723696543741,-3.01977017460503,
-2.32186851754045));
#44115=CARTESIAN_POINT('Ctrl Pts',(-14.6738965026459,0.313218324198597,
-3.79631131515394));
#44116=CARTESIAN_POINT('Ctrl Pts',(-14.4754233509178,3.35948111786941,-1.79554224090064));
#44117=CARTESIAN_POINT('Ctrl Pts',(-14.2769501991897,3.33041428366469,1.84889859628423));
#44118=CARTESIAN_POINT('Ctrl Pts',(-14.0784770474615,0.252626126046346,
3.80082430015101));
#44119=CARTESIAN_POINT('Ctrl Pts',(-13.8800038957334,-3.05642054529701,
2.27340686426031));
#44120=CARTESIAN_POINT('Ctrl Pts',(-13.6815307440053,-3.5675647047904,-1.33512823253552));
#44121=CARTESIAN_POINT('Ctrl Pts',(-13.4830575922771,-0.812895766645905,
-3.72146285655909));
#44122=CARTESIAN_POINT('Ctrl Pts',(-13.284584440549,2.68591262275001,-2.70110323814768));
#44123=CARTESIAN_POINT('Ctrl Pts',(-13.0861112888209,3.72598813738973,0.791895018427709));
#44124=CARTESIAN_POINT('Ctrl Pts',(-12.8876381370928,1.35522688587594,3.55997828757123));
#44125=CARTESIAN_POINT('Ctrl Pts',(-12.6891649853646,-2.25613350830277,
3.06919320227532));
#44126=CARTESIAN_POINT('Ctrl Pts',(-12.4906918336365,-3.80218858326998,
-0.231186715515902));
#44127=CARTESIAN_POINT('Ctrl Pts',(-12.2922186819084,-1.86765162909789,
-3.31993414279675));
#44128=CARTESIAN_POINT('Ctrl Pts',(-12.0937455301802,1.77656732297672,-3.36955395669975));
#44129=CARTESIAN_POINT('Ctrl Pts',(-11.8952723784521,3.7944844943374,-0.334623284325299));
#44130=CARTESIAN_POINT('Ctrl Pts',(-11.696799226724,2.33886209856671,3.00662757987545));
#44131=CARTESIAN_POINT('Ctrl Pts',(-11.4983260749959,-1.2577968605525,3.59555731114996));
#44132=CARTESIAN_POINT('Ctrl Pts',(-11.2998529232677,-3.70304588004417,
0.893049007875609));
#44133=CARTESIAN_POINT('Ctrl Pts',(-11.1013797715396,-2.75845988968622,
-2.62697246981617));
#44134=CARTESIAN_POINT('Ctrl Pts',(-10.9029066198115,0.711270052496804,
-3.74221595216));
#44135=CARTESIAN_POINT('Ctrl Pts',(-10.7044334680833,3.52989055571641,-1.43176743392344));
#44136=CARTESIAN_POINT('Ctrl Pts',(-10.5059603163552,3.11718555708669,2.18934682562397));
#44137=CARTESIAN_POINT('Ctrl Pts',(-10.3074871646271,-0.14904734152245,
3.80629350026567));
#44138=CARTESIAN_POINT('Ctrl Pts',(-10.1090140128989,-3.27883961455344,
1.9388904306883));
#44139=CARTESIAN_POINT('Ctrl Pts',(-9.91054086117081,-3.40712294679801,
-1.70340792107529));
#44140=CARTESIAN_POINT('Ctrl Pts',(-9.71206770944269,-0.416464461400303,
-3.78637592858529));
#44141=CARTESIAN_POINT('Ctrl Pts',(-9.51359455771457,2.95543310591665,-2.40322709635013));
#44142=CARTESIAN_POINT('Ctrl Pts',(-9.31512140598641,3.62187388543242,1.17987917949349));
#44143=CARTESIAN_POINT('Ctrl Pts',(-9.11664825425831,0.972785963491132,
3.6829027667608));
#44144=CARTESIAN_POINT('Ctrl Pts',(-8.91817510253016,-2.56680778067166,
2.81453071350504));
#44145=CARTESIAN_POINT('Ctrl Pts',(-8.71970195080203,-3.75669937143538,
-0.630313535343016));
#44146=CARTESIAN_POINT('Ctrl Pts',(-8.52122879907392,-1.50764057830064,
-3.49815740166747));
#44147=CARTESIAN_POINT('Ctrl Pts',(-8.32275564734576,2.12153960142961,-3.1637248678963));
#44148=CARTESIAN_POINT('Ctrl Pts',(-8.12428249561765,3.80862415267616,0.0668384906429997));
#44149=CARTESIAN_POINT('Ctrl Pts',(-7.92580934388952,2.00922543843686,3.23621668893135));
#44150=CARTESIAN_POINT('Ctrl Pts',(-7.72733619216139,-1.62945449308302,
3.44310374156095));
#44151=CARTESIAN_POINT('Ctrl Pts',(-7.52886304043325,-3.77650238261931,
0.498111507848026));
#44152=CARTESIAN_POINT('Ctrl Pts',(-7.33038988870514,-2.46647185452845,
-2.90286098719837));
#44153=CARTESIAN_POINT('Ctrl Pts',(-7.131916736977,1.10141150988432,-3.6465021604372));
#44154=CARTESIAN_POINT('Ctrl Pts',(-6.93344358524887,3.6610429062145,-1.05206946493042));
#44155=CARTESIAN_POINT('Ctrl Pts',(-6.73497043352074,2.86928957276539,2.50544660046798));
#44156=CARTESIAN_POINT('Ctrl Pts',(-6.5364972817926,-0.549063204013273,
3.76943164391853));
#44157=CARTESIAN_POINT('Ctrl Pts',(-6.3380241300645,-3.4647936175104,1.58281095152196));
#44158=CARTESIAN_POINT('Ctrl Pts',(-6.13955097833634,-3.20878944087819,
-2.05274344336138));
#44159=CARTESIAN_POINT('Ctrl Pts',(-5.94107782660823,-0.0154015163207855,
-3.80917945408937));
#44160=CARTESIAN_POINT('Ctrl Pts',(-5.74260467488009,3.19208523418617,-2.07862386640746));
#44161=CARTESIAN_POINT('Ctrl Pts',(-5.54413152315197,3.47747956887825,1.55474151163881));
#44162=CARTESIAN_POINT('Ctrl Pts',(-5.34565837142383,0.57952636479995,3.76486845887453));
#44163=CARTESIAN_POINT('Ctrl Pts',(-5.14718521969571,-2.84893572979317,
2.52856689224015));
#44164=CARTESIAN_POINT('Ctrl Pts',(-4.94871206796758,-3.6694306557177,-1.02243042868416));
#44165=CARTESIAN_POINT('Ctrl Pts',(-4.75023891623944,-1.13086255544314,
-3.6374764880366));
#44166=CARTESIAN_POINT('Ctrl Pts',(-4.55176576451131,2.44291753292778,-2.92271094241356));
#44167=CARTESIAN_POINT('Ctrl Pts',(-4.35329261278319,3.78040683298627,0.467556932945782));
#44168=CARTESIAN_POINT('Ctrl Pts',(-4.15481946105505,1.65724351676092,3.42981475460483));
#44169=CARTESIAN_POINT('Ctrl Pts',(-3.95634630932692,-1.98299042591341,
3.25235827122354));
#44170=CARTESIAN_POINT('Ctrl Pts',(-3.7578731575988,-3.80795913442598,0.0976343410155721));
#44171=CARTESIAN_POINT('Ctrl Pts',(-3.55940000587067,-2.14705338671746,
-3.1464658159672));
#44172=CARTESIAN_POINT('Ctrl Pts',(-3.36092685414253,1.47930384451711,-3.51023441585637));
#44173=CARTESIAN_POINT('Ctrl Pts',(-3.16245370241441,3.75147950180274,-0.66067106043193));
#44174=CARTESIAN_POINT('Ctrl Pts',(-2.96398055068628,2.58948341482026,2.79368243000086));
#44175=CARTESIAN_POINT('Ctrl Pts',(-2.76550739895815,-0.942973039578199,
3.69064876067085));
#44176=CARTESIAN_POINT('Ctrl Pts',(-2.56703424723002,-3.61221394765404,
1.20912835863316));
#44177=CARTESIAN_POINT('Ctrl Pts',(-2.36856109550189,-2.97477097222353,
-2.37924944263257));
#44178=CARTESIAN_POINT('Ctrl Pts',(-2.17008794377376,0.385834726766185,
-3.78962036336862));
#44179=CARTESIAN_POINT('Ctrl Pts',(-1.97161479204564,3.39323327108378,-1.73090254387995));
#44180=CARTESIAN_POINT('Ctrl Pts',(-1.77314164031749,3.29441840747864,1.91231108576612));
#44181=CARTESIAN_POINT('Ctrl Pts',(-1.57466848858938,0.179807578872998,
3.80496754565549));
#44182=CARTESIAN_POINT('Ctrl Pts',(-1.37619533686123,-3.09935278363057,
2.21447486591351));
#44183=CARTESIAN_POINT('Ctrl Pts',(-1.1777221851331,-3.54140449397235,-1.40316281688026));
#44184=CARTESIAN_POINT('Ctrl Pts',(-0.979249033404971,-0.741409307439854,
-3.73636822239283));
#44185=CARTESIAN_POINT('Ctrl Pts',(-0.780775881676852,2.73693851524025,
-2.64914239661277));
#44186=CARTESIAN_POINT('Ctrl Pts',(-0.58230272994871,3.7105068394527,0.862979517739233));
#44187=CARTESIAN_POINT('Ctrl Pts',(-0.383829578220586,1.28614089123481,
3.58545256094235));
#44188=CARTESIAN_POINT('Ctrl Pts',(-0.185356426492456,-2.31314908170687,
3.02508848610542));
#44189=CARTESIAN_POINT('Ctrl Pts',(0.0131167252356648,-3.79963544752816,
-0.303233139382865));
#44190=CARTESIAN_POINT('Ctrl Pts',(0.211589876963805,-1.79851093142999,
-3.35657563863806));
#44191=CARTESIAN_POINT('Ctrl Pts',(0.343905311449222,0.619074511407565,
-3.33937494959071));
#44192=CARTESIAN_POINT('Ctrl Pts',(0.410063028691932,1.55734592416918,-2.82148741534915));
#44193=CARTESIAN_POINT('',(0.,1.9005636551884,-3.44330463255532));
#44194=CARTESIAN_POINT('Ctrl Pts',(3.88578058618805E-15,-3.22782252806242,
-0.0460729527342081));
#44195=CARTESIAN_POINT('Ctrl Pts',(4.73555566111894E-15,-3.23478024525164,
-0.117033456944334));
#44196=CARTESIAN_POINT('Ctrl Pts',(8.03715949314405E-15,-3.23920846232986,
-0.188120433263497));
#44197=CARTESIAN_POINT('Ctrl Pts',(8.04911692853238E-15,-3.24105490347623,
-0.259217854133791));
#44198=CARTESIAN_POINT('Ctrl Pts',(8.01201932747411E-15,-3.24372057254421,
-0.361859736871017));
#44199=CARTESIAN_POINT('Ctrl Pts',(4.97629665024702E-15,-3.24100807231244,
-0.464523059622032));
#44200=CARTESIAN_POINT('Ctrl Pts',(6.38378239159465E-15,-3.2331868370857,
-0.566908454444247));
#44201=CARTESIAN_POINT('Ctrl Pts',(7.27024547280655E-15,-3.228260864428,
-0.631392853752119));
#44202=CARTESIAN_POINT('Ctrl Pts',(5.05793373854853E-15,-3.22130734435912,
-0.695767345230122));
#44203=CARTESIAN_POINT('Ctrl Pts',(7.88258347483861E-15,-3.21238338916487,
-0.759959157634126));
#44204=CARTESIAN_POINT('Ctrl Pts',(9.67722682972631E-15,-3.20671354745568,
-0.800743474389926));
#44205=CARTESIAN_POINT('Ctrl Pts',(1.25174804097342E-15,-3.20024814307216,
-0.841454073881994));
#44206=CARTESIAN_POINT('Ctrl Pts',(3.60822483003176E-15,-3.19300024485765,
-0.88207239965212));
#44207=CARTESIAN_POINT('Ctrl Pts',(4.76004307358495E-15,-3.18945755713433,
-0.901926161361911));
#44208=CARTESIAN_POINT('Ctrl Pts',(-5.96198962811207E-15,-3.18572918223731,
-0.921750470983836));
#44209=CARTESIAN_POINT('Ctrl Pts',(-6.21724893790088E-15,-3.18181839014642,
-0.94153660922562));
#44210=CARTESIAN_POINT('Ctrl Pts',(-7.56115075084112E-15,-3.16122865892243,
-1.04570764641999));
#44211=CARTESIAN_POINT('Ctrl Pts',(-1.36291055847055E-14,-3.13557667564011,
-1.14887664494683));
#44212=CARTESIAN_POINT('Ctrl Pts',(-1.38222766565832E-14,-3.10513969145318,
-1.25072883011327));
#44213=CARTESIAN_POINT('Ctrl Pts',(-1.40056860216817E-14,-3.07624080979882,
-1.34743401704262));
#44214=CARTESIAN_POINT('Ctrl Pts',(-1.64583170794824E-14,-3.04302772710359,
-1.44295273829285));
#44215=CARTESIAN_POINT('Ctrl Pts',(-1.72639680329212E-14,-3.00569631404638,
-1.5370185109656));
#44216=CARTESIAN_POINT('Ctrl Pts',(-1.76197494419365E-14,-2.98921048642918,
-1.57855865064864));
#44217=CARTESIAN_POINT('Ctrl Pts',(-1.1736135794431E-14,-2.97192100533988,
-1.6198154265008));
#44218=CARTESIAN_POINT('Ctrl Pts',(-1.15463194561016E-14,-2.95384239793326,
-1.66076562713157));
#44219=CARTESIAN_POINT('Ctrl Pts',(-1.14658401134983E-14,-2.94617733362913,
-1.67812791140723));
#44220=CARTESIAN_POINT('Ctrl Pts',(-4.64785945728864E-15,-2.93837039609743,
-1.69543508116795));
#44221=CARTESIAN_POINT('Ctrl Pts',(-4.94049245958195E-15,-2.93042261817385,
-1.71268534926259));
#44222=CARTESIAN_POINT('Ctrl Pts',(-5.23462946247637E-15,-2.92243399228478,
-1.73002427589328));
#44223=CARTESIAN_POINT('Ctrl Pts',(1.03171797750105E-14,-2.91430646083762,
-1.7472982787437));
#44224=CARTESIAN_POINT('Ctrl Pts',(1.02140518265514E-14,-2.90604442083402,
-1.76449962417443));
#44225=CARTESIAN_POINT('Ctrl Pts',(9.61224345561637E-15,-2.85783086757843,
-1.8648789473961));
#44226=CARTESIAN_POINT('Ctrl Pts',(-2.77542935576527E-15,-2.80501130232528,
-1.96284871204576));
#44227=CARTESIAN_POINT('Ctrl Pts',(-3.5527136788005E-15,-2.74787578078745,
-2.0580753587026));
#44228=CARTESIAN_POINT('Ctrl Pts',(-4.34191077239773E-15,-2.6898645920853,
-2.15476146254826));
#44229=CARTESIAN_POINT('Ctrl Pts',(5.09332848748403E-16,-2.62740391916529,
-2.24862058887149));
#44230=CARTESIAN_POINT('Ctrl Pts',(4.44089209850063E-16,-2.56074398374797,
-2.33929898513567));
#44231=CARTESIAN_POINT('Ctrl Pts',(3.79051966108302E-16,-2.49429492387408,
-2.42969052459493));
#44232=CARTESIAN_POINT('Ctrl Pts',(-2.96184435993952E-15,-2.42367274126983,
-2.51692230201439));
#44233=CARTESIAN_POINT('Ctrl Pts',(-3.63598040564739E-15,-2.34907746971602,
-2.60062625818245));
#44234=CARTESIAN_POINT('Ctrl Pts',(-4.06933452632506E-15,-2.3011254746896,
-2.65443357875728));
#44235=CARTESIAN_POINT('Ctrl Pts',(8.7125606268543E-15,-2.25153073404126,
-2.70678271127021));
#44236=CARTESIAN_POINT('Ctrl Pts',(8.90953977261688E-15,-2.20033702360218,
-2.75756942711216));
#44237=CARTESIAN_POINT('Ctrl Pts',(8.96738040010056E-15,-2.1853045879423,
-2.77248235355806));
#44238=CARTESIAN_POINT('Ctrl Pts',(1.50797221210893E-14,-2.17013423829745,
-2.78726052273648));
#44239=CARTESIAN_POINT('Ctrl Pts',(1.47659662275146E-14,-2.15482697246737,
-2.8019011892954));
#44240=CARTESIAN_POINT('Ctrl Pts',(1.45500706766672E-14,-2.14429403697187,
-2.81197543757644));
#44241=CARTESIAN_POINT('Ctrl Pts',(1.23807284931021E-14,-2.13369842184177,
-2.82198247550803));
#44242=CARTESIAN_POINT('Ctrl Pts',(1.20459198171829E-14,-2.12304672770763,
-2.8319158305085));
#44243=CARTESIAN_POINT('Ctrl Pts',(9.38291716989935E-15,-2.03832523833943,
-2.91092379107002));
#44244=CARTESIAN_POINT('Ctrl Pts',(1.9478406166701E-14,-1.94994848897902,
-2.98537883656598));
#44245=CARTESIAN_POINT('Ctrl Pts',(1.82354131794682E-14,-1.8581826378662,
-3.05491944709952));
#44246=CARTESIAN_POINT('Ctrl Pts',(1.75414617624024E-14,-1.80695061719345,
-3.09374332279233));
#44247=CARTESIAN_POINT('Ctrl Pts',(9.03667999584674E-15,-1.75466135551627,
-3.13103514774695));
#44248=CARTESIAN_POINT('Ctrl Pts',(9.79771819231701E-15,-1.7013548304381,
-3.16672887515648));
#44249=CARTESIAN_POINT('Ctrl Pts',(1.1086530334245E-14,-1.60913652867894,
-3.22847769334214));
#44250=CARTESIAN_POINT('Ctrl Pts',(1.24667943883469E-15,-1.51387584437434,
-3.28544626009495));
#44251=CARTESIAN_POINT('Ctrl Pts',(8.04911692853238E-16,-1.41595740939529,
-3.33768974045716));
#44252=CARTESIAN_POINT('Ctrl Pts',(3.54779253464665E-16,-1.31618492849516,
-3.39092242996767));
#44253=CARTESIAN_POINT('Ctrl Pts',(-6.5005489732385E-16,-1.21365248296573,
-3.43924970726973));
#44254=CARTESIAN_POINT('Ctrl Pts',(-1.41553435639707E-15,-1.10873353044733,
-3.48268730307254));
#44255=CARTESIAN_POINT('Ctrl Pts',(-1.66306814692421E-15,-1.07480579312247,
-3.49673375802702));
#44256=CARTESIAN_POINT('Ctrl Pts',(-3.87488146035897E-15,-1.04062828456681,
-3.51026855829844));
#44257=CARTESIAN_POINT('Ctrl Pts',(-3.7470027081099E-15,-1.0062130758155,
-3.52329122523045));
#44258=CARTESIAN_POINT('Ctrl Pts',(-3.6710391470737E-15,-0.985769477762066,
-3.53102705418518));
#44259=CARTESIAN_POINT('Ctrl Pts',(2.81238272578907E-15,-0.965237687041626,
-3.53858360073728));
#44260=CARTESIAN_POINT('Ctrl Pts',(3.24740234702858E-15,-0.94464775261746,
-3.54595111805713));
#44261=CARTESIAN_POINT('Ctrl Pts',(5.51531576371633E-15,-0.837305034612612,
-3.58436063009195));
#44262=CARTESIAN_POINT('Ctrl Pts',(-7.28433529689487E-15,-0.728255688796531,
-3.61768684857147));
#44263=CARTESIAN_POINT('Ctrl Pts',(-4.71844785465692E-15,-0.617912626483569,
-3.64600997081435));
#44264=CARTESIAN_POINT('Ctrl Pts',(-2.07020700373184E-15,-0.504028049778018,
-3.67524213747709));
#44265=CARTESIAN_POINT('Ctrl Pts',(2.29237048498726E-14,-0.388764785234235,
-3.6991452721761));
#44266=CARTESIAN_POINT('Ctrl Pts',(2.96290769696839E-14,-0.272542535137063,
-3.71776398168584));
#44267=CARTESIAN_POINT('Ctrl Pts',(3.63968142768708E-14,-0.155239327521797,
-3.73655585970681));
#44268=CARTESIAN_POINT('Ctrl Pts',(8.3301433537551E-15,-0.0369584030558998,
-3.74996479689759));
#44269=CARTESIAN_POINT('Ctrl Pts',(4.26048085699904E-15,0.0818921458507452,
-3.75798853653923));
#44270=CARTESIAN_POINT('Ctrl Pts',(1.60898338187825E-15,0.159326559784058,
-3.76321622444156));
#44271=CARTESIAN_POINT('Ctrl Pts',(1.07137817972841E-14,0.237003225132265,
-3.7661569708165));
#44272=CARTESIAN_POINT('Ctrl Pts',(9.54791801177635E-15,0.314812005453235,
-3.7667985805642));
#44273=CARTESIAN_POINT('Ctrl Pts',(9.15843836140906E-15,0.340805553697568,
-3.76701292287701));
#44274=CARTESIAN_POINT('Ctrl Pts',(-7.73214731083006E-15,0.366813855211389,
-3.76697059853649));
#44275=CARTESIAN_POINT('Ctrl Pts',(-8.49320613838245E-15,0.392832820121125,
-3.76667091810736));
#44276=CARTESIAN_POINT('Ctrl Pts',(-8.96735202530461E-15,0.409042848501716,
-3.76648421474395));
#44277=CARTESIAN_POINT('Ctrl Pts',(4.5316324873848E-15,0.425257015824682,
-3.76619761904271));
#44278=CARTESIAN_POINT('Ctrl Pts',(4.30211422042248E-15,0.441474332786118,
-3.76581094080709));
#44279=CARTESIAN_POINT('Ctrl Pts',(4.06095880866029E-15,0.458513907898259,
-3.76540465702687));
#44280=CARTESIAN_POINT('Ctrl Pts',(5.76983320580279E-15,0.475547853604313,
-3.76488808759821));
#44281=CARTESIAN_POINT('Ctrl Pts',(5.49560397189452E-15,0.492571736322231,
-3.76426150826196));
#44282=CARTESIAN_POINT('Ctrl Pts',(3.52265966451042E-15,0.615050189910908,
-3.75975357846556));
#44283=CARTESIAN_POINT('Ctrl Pts',(1.24955252947878E-14,0.737059901364942,
-3.74955414102053));
#44284=CARTESIAN_POINT('Ctrl Pts',(1.08801856413265E-14,0.858161021353391,
-3.73371021053407));
#44285=CARTESIAN_POINT('Ctrl Pts',(9.26218533919139E-15,0.979461608700677,
-3.71784018328675));
#44286=CARTESIAN_POINT('Ctrl Pts',(2.79921898071093E-16,1.09985150954407,
-3.69630721138857));
#44287=CARTESIAN_POINT('Ctrl Pts',(-1.64451785522601E-15,1.21890371977399,
-3.66910833103822));
#44288=CARTESIAN_POINT('Ctrl Pts',(-3.53245504367798E-15,1.33569776057229,
-3.64242535610503));
#44289=CARTESIAN_POINT('Ctrl Pts',(-9.40696534928934E-15,1.45120524179666,
-3.61028936199537));
#44290=CARTESIAN_POINT('Ctrl Pts',(-1.27606258892854E-14,1.56502432695476,
-3.57264846725809));
#44291=CARTESIAN_POINT('Ctrl Pts',(-1.61097959296429E-14,1.6786910101167,
-3.5350579730972));
#44292=CARTESIAN_POINT('Ctrl Pts',(-1.6278834459108E-16,1.79067467066081,
-3.49197745284248));
#44293=CARTESIAN_POINT('Ctrl Pts',(0.,1.9005636551884,-3.44330463255532));
#44294=CARTESIAN_POINT('Ctrl Pts',(0.,1.9005636551884,-3.44330463255532));
#44295=CARTESIAN_POINT('Ctrl Pts',(-0.0661577172427078,0.755510062327915,
-4.07532749258862));
#44296=CARTESIAN_POINT('Ctrl Pts',(-0.132315434485407,-0.719684033813403,
-4.08582323535868));
#44297=CARTESIAN_POINT('Ctrl Pts',(-0.198473151728118,-1.86430524457212,
-3.47002820603423));
#44298=CARTESIAN_POINT('Ctrl Pts',(-0.264630868970832,-3.00892645533091,
-2.85423317670973));
#44299=CARTESIAN_POINT('Ctrl Pts',(-0.330788586213552,-3.82297478070687,
-1.61214737529056));
#44300=CARTESIAN_POINT('Ctrl Pts',(-0.396946303456264,-3.92765100675819,
-0.314131446729717));
#44301=CARTESIAN_POINT('Ctrl Pts',(-0.402243028292546,-3.9360316037528,
-0.210209584047015));
#44302=CARTESIAN_POINT('Ctrl Pts',(-0.407539753128828,-3.93986516986432,
-0.105929212740074));
#44303=CARTESIAN_POINT('Ctrl Pts',(-0.41283647796511,-3.93929521061115,
-0.00160796147817999));
#44304=CARTESIAN_POINT('Origin',(4.677207419323,0.,0.));
#44305=CARTESIAN_POINT('',(4.53252091062694,6.5,-3.75277674973257));
#44306=CARTESIAN_POINT('',(4.53252091062694,-1.37874781034238E-15,-7.50555349946513));
#44307=CARTESIAN_POINT('Ctrl Pts',(4.53252091062694,6.5,-3.75277674973257));
#44308=CARTESIAN_POINT('Ctrl Pts',(5.61727242352805,3.24999999999854,-5.6291651245997));
#44309=CARTESIAN_POINT('Ctrl Pts',(4.53252091062694,-1.37874781034238E-15,
-7.50555349946513));
#44310=CARTESIAN_POINT('',(4.53252091062694,6.5,3.75277674973257));
#44311=CARTESIAN_POINT('Ctrl Pts',(4.53252091062694,6.5,3.75277674973257));
#44312=CARTESIAN_POINT('Ctrl Pts',(5.61727242352805,6.5,-1.69086966650411E-12));
#44313=CARTESIAN_POINT('Ctrl Pts',(4.53252091062694,6.5,-3.75277674973257));
#44314=CARTESIAN_POINT('',(4.53252091062694,4.5958260344746E-16,7.50555349946513));
#44315=CARTESIAN_POINT('Ctrl Pts',(4.53252091062694,4.5958260344746E-16,
7.50555349946513));
#44316=CARTESIAN_POINT('Ctrl Pts',(5.61727242352806,3.25000000000146,5.62916512459801));
#44317=CARTESIAN_POINT('Ctrl Pts',(4.53252091062694,6.5,3.75277674973257));
#44318=CARTESIAN_POINT('',(4.53252091062694,-6.5,3.75277674973257));
#44319=CARTESIAN_POINT('Ctrl Pts',(4.53252091062694,-6.5,3.75277674973257));
#44320=CARTESIAN_POINT('Ctrl Pts',(5.61727242352806,-3.24999999999854,5.6291651245997));
#44321=CARTESIAN_POINT('Ctrl Pts',(4.53252091062694,4.5958260344746E-16,
7.50555349946513));
#44322=CARTESIAN_POINT('',(5.11383749436743,-6.5,-8.18813977659918E-16));
#44323=CARTESIAN_POINT('Ctrl Pts',(5.11383749436743,-6.5,-8.41607535874056E-16));
#44324=CARTESIAN_POINT('Ctrl Pts',(5.11383749436757,-6.5,1.74166975080303));
#44325=CARTESIAN_POINT('Ctrl Pts',(4.53252091062694,-6.5,3.75277674973257));
#44326=CARTESIAN_POINT('',(5.3,-6.17797863635533,-7.56584176221328E-16));
#44327=CARTESIAN_POINT('',(4.677207419323,-7.25527674973257,-8.8851514484882E-16));
#44328=CARTESIAN_POINT('Origin',(5.3,0.,0.));
#44329=CARTESIAN_POINT('',(4.53252091062694,-6.5,-3.75277674973257));
#44330=CARTESIAN_POINT('Ctrl Pts',(4.53252091062694,-6.5,-3.75277674973257));
#44331=CARTESIAN_POINT('Ctrl Pts',(5.11383749436729,-6.5,-1.74166975080219));
#44332=CARTESIAN_POINT('Ctrl Pts',(5.11383749436743,-6.5,-8.41607535874056E-16));
#44333=CARTESIAN_POINT('Ctrl Pts',(4.53252091062694,-1.37874781034238E-15,
-7.50555349946513));
#44334=CARTESIAN_POINT('Ctrl Pts',(5.61727242352805,-3.25000000000146,-5.629165124598));
#44335=CARTESIAN_POINT('Ctrl Pts',(4.53252091062694,-6.5,-3.75277674973257));
#44336=CARTESIAN_POINT('Origin',(0.,4.5958260344746E-16,7.50555349946513));
#44337=CARTESIAN_POINT('',(0.,4.5958260344746E-16,7.50555349946513));
#44338=CARTESIAN_POINT('',(0.,4.5958260344746E-16,7.50555349946513));
#44339=CARTESIAN_POINT('',(0.,-6.5,3.75277674973257));
#44340=CARTESIAN_POINT('',(0.,4.5958260344746E-16,7.50555349946513));
#44341=CARTESIAN_POINT('',(0.,-6.5,3.75277674973257));
#44342=CARTESIAN_POINT('Origin',(0.,6.5,3.75277674973257));
#44343=CARTESIAN_POINT('',(0.,6.5,3.75277674973257));
#44344=CARTESIAN_POINT('',(0.,6.5,3.75277674973257));
#44345=CARTESIAN_POINT('',(0.,6.5,3.75277674973257));
#44346=CARTESIAN_POINT('Origin',(0.,6.5,-3.75277674973257));
#44347=CARTESIAN_POINT('',(0.,6.5,-3.75277674973257));
#44348=CARTESIAN_POINT('',(0.,6.5,-3.75277674973257));
#44349=CARTESIAN_POINT('',(0.,6.5,-3.75277674973257));
#44350=CARTESIAN_POINT('Origin',(0.,0.,-1.11022302462516E-15));
#44351=CARTESIAN_POINT('',(0.,-1.37874781034238E-15,-7.50555349946513));
#44352=CARTESIAN_POINT('',(0.,-1.37874781034238E-15,-7.50555349946513));
#44353=CARTESIAN_POINT('',(0.,-6.5,-3.75277674973257));
#44354=CARTESIAN_POINT('',(0.,-6.5,-3.75277674973257));
#44355=CARTESIAN_POINT('',(0.,-6.5,3.75277674973257));
#44356=CARTESIAN_POINT('Origin',(0.,0.,0.));
#44357=CARTESIAN_POINT('Origin',(0.,-1.37874781034238E-15,-7.50555349946513));
#44358=CARTESIAN_POINT('',(0.,-1.37874781034238E-15,-7.50555349946513));
#44359=CARTESIAN_POINT('Origin',(0.,-6.5,-3.75277674973257));
#44360=CARTESIAN_POINT('',(0.,-6.5,-3.75277674973257));
#44361=CARTESIAN_POINT('Origin',(0.,-6.5,3.75277674973257));
#44362=CARTESIAN_POINT('Origin',(5.3,0.,-1.11022302462516E-15));
#44363=CARTESIAN_POINT('Origin',(-55.,3.5,0.));
#44364=CARTESIAN_POINT('',(-55.,-3.5,-4.28626379701573E-16));
#44365=CARTESIAN_POINT('Origin',(-55.,0.,0.));
#44366=CARTESIAN_POINT('Origin',(-54.75,0.,0.));
#44367=CARTESIAN_POINT('',(-54.75,-3.75,-4.59242549680257E-16));
#44368=CARTESIAN_POINT('Origin',(-27.25,0.,0.));
#56614=UNCERTAINTY_MEASURE_WITH_UNIT(LENGTH_MEASURE(0.01),#56640,
'DISTANCE_ACCURACY_VALUE',
'Maximum model space distance between geometric entities at asserted c
onnectivities');
#56617=UNCERTAINTY_MEASURE_WITH_UNIT(LENGTH_MEASURE(0.01),#56640,
'DISTANCE_ACCURACY_VALUE',
'Maximum model space distance between geometric entities at asserted c
onnectivities');
#56636=(
GEOMETRIC_REPRESENTATION_CONTEXT(3)
GLOBAL_UNCERTAINTY_ASSIGNED_CONTEXT((#56614))
GLOBAL_UNIT_ASSIGNED_CONTEXT((#56640,#56642,#56643))
REPRESENTATION_CONTEXT('','3D')
);
#56639=(
GEOMETRIC_REPRESENTATION_CONTEXT(3)
GLOBAL_UNCERTAINTY_ASSIGNED_CONTEXT((#56617))
GLOBAL_UNIT_ASSIGNED_CONTEXT((#56640,#56642,#56643))
REPRESENTATION_CONTEXT('','3D')
);
#56640=(
LENGTH_UNIT()
NAMED_UNIT(*)
SI_UNIT(.MILLI.,.METRE.)
);
#56642=(
NAMED_UNIT(*)
PLANE_ANGLE_UNIT()
SI_UNIT($,.RADIAN.)
);
#56643=(
NAMED_UNIT(*)
SI_UNIT($,.STERADIAN.)
SOLID_ANGLE_UNIT()
);
#56662=SHAPE_DEFINITION_REPRESENTATION(#56683,#56762);
#56683=PRODUCT_DEFINITION_SHAPE('',$,#56784);
#56762=SHAPE_REPRESENTATION('',(#18375),#56636);
#56765=PRODUCT_DEFINITION_CONTEXT('part definition',#56830,'design');
#56784=PRODUCT_DEFINITION('2026-10-26-00-02-56-247',
'18_Manifold_Bolt_ISO_4017_M8x55',#56805,#56765);
#56805=PRODUCT_DEFINITION_FORMATION('',$,#56850);
#56830=APPLICATION_CONTEXT(
'Core Data for Automotive Mechanical Design Process');
#56831=PRODUCT_CONTEXT('part definition',#56830,'mechanical');
#56850=PRODUCT('2026-10-26-00-02-56-247',
'18_Manifold_Bolt_ISO_4017_M8x55',$,(#56831));
#56916=COLOUR_RGB('Black',0.12,0.14,0.17);
#56917=FILL_AREA_STYLE_COLOUR('',#56916);
#56918=FILL_AREA_STYLE('',(#56917));
#56919=SURFACE_STYLE_FILL_AREA(#56918);
#56920=SURFACE_SIDE_STYLE('',(#56919));
#56921=SURFACE_STYLE_USAGE(.BOTH.,#56920);
#56922=PRESENTATION_STYLE_ASSIGNMENT((#56921));
ENDSEC;
END-ISO-10303-21;
